ISO-10303-21;
HEADER;
FILE_DESCRIPTION (('STEP AP203'),
    '1' );
FILE_NAME ('94902A107_High-Strength Steel Flange Nut_94902A107.step',
    '2026-10-07T20:09:13',
    ( '' ),
    ( '' ),
    'SwSTEP 2.0',
    'SolidWorks 2024',
    '' );
FILE_SCHEMA (( 'AUTOMOTIVE_DESIGN' ));
ENDSEC;

DATA;
#15=CARTESIAN_POINT ( 'NONE',  ( 0.3155070326520292845, -5.795770164686806123E-17, 0.03451388888889012074 ) ) ;
#16=CARTESIAN_POINT ( 'NONE',  ( 0.3124999999999999445, -0.1294417382415923856, 0.03625000000000165590 ) ) ;
#28=CARTESIAN_POINT ( 'NONE',  ( -0.1899274842524383000, 0.4207833852643000361, 0.4343212420608417168 ) ) ;
#36=ORIENTED_EDGE ( 'NONE', *, *, #677, .F. ) ;
#38=ORIENTED_EDGE ( 'NONE', *, *, #20394, .F. ) ;
#41=CARTESIAN_POINT ( 'NONE',  ( 0.4208308994021709992, -0.2864083541825031554, 0.4065068718547069082 ) ) ;
#43=EDGE_LOOP ( 'NONE', ( #17199, #17644, #7483, #15061 ) ) ;
#53=CARTESIAN_POINT ( 'NONE',  ( 0.4500000000000003442, 0.2598076211353318454, 0.3779506566538942125 ) ) ;
#54=CARTESIAN_POINT ( 'NONE',  ( -0.2764156081756484196, 1.692557448933383907E-17, 0.2550000000000032241 ) ) ;
#57=CARTESIAN_POINT ( 'NONE',  ( -0.1504789989860494670, -0.4433647533406467889, 0.4295860435587943171 ) ) ;
#58=CARTESIAN_POINT ( 'NONE',  ( -0.3886629897678103851, 0.3298823763122804564, 0.06108558933789665774 ) ) ;
#75=CARTESIAN_POINT ( 'NONE',  ( 0.2732891327808320558, -0.3834823229876774264, 0.4280258002685559671 ) ) ;
#78=CARTESIAN_POINT ( 'NONE',  ( -0.2764156081756484196, 1.692557448933383907E-17, 0.08833333333333522053 ) ) ;
#80=CARTESIAN_POINT ( 'NONE',  ( 0.1144950937579609085, -0.2764156081756484751, 0.2793055555555589153 ) ) ;
#85=EDGE_CURVE ( 'NONE', #8682, #18897, #14418, .T. ) ;
#96=ORIENTED_EDGE ( 'NONE', *, *, #12472, .T. ) ;
#98=CARTESIAN_POINT ( 'NONE',  ( -0.009374999999999907713, -0.5358532185916218271, 0.3779506566538943235 ) ) ;
#100=CARTESIAN_POINT ( 'NONE',  ( 0.3125000000000000000, 3.827021247335477694E-17, 1.326383476483184332 ) ) ;
#102=CARTESIAN_POINT ( 'NONE',  ( -3.385114897866767815E-17, -0.2764156081756484196, 0.2133333333333362336 ) ) ;
#108=CARTESIAN_POINT ( 'NONE',  ( 0.4687500000000002776, -0.2172231356220941378, 0.07046374828496694553 ) ) ;
#111=CARTESIAN_POINT ( 'NONE',  ( 0.2764156081756483641, -0.1144950937579611167, -0.04708333333333256793 ) ) ;
#114=CARTESIAN_POINT ( 'NONE',  ( 0.4687500000000003331, -0.1769877694293681969, 0.4113775649628997333 ) ) ;
#118=VECTOR ( 'NONE', #23345, 39.37007874015748143 ) ;
#123=CARTESIAN_POINT ( 'NONE',  ( -0.4719654084974831409, -0.2800274776536547106, 0.04212966708837322799 ) ) ;
#128=( NAMED_UNIT ( * ) PLANE_ANGLE_UNIT ( ) SI_UNIT ( $, .RADIAN. ) );
#141=CARTESIAN_POINT ( 'NONE',  ( -0.1306872919485614903, 0.3155070326520293400, 0.05187500000000137834 ) ) ;
#142=CARTESIAN_POINT ( 'NONE',  ( -0.009374999999999892100, -0.5358532185916218271, 0.06112444011295370405 ) ) ;
#149=( BOUNDED_CURVE ( )  B_SPLINE_CURVE ( 2, ( #23578, #18111, #14462, #1644, #20183, #18233, #14334, #18593, #6894 ),
 .UNSPECIFIED., .F., .F. ) 
 B_SPLINE_CURVE_WITH_KNOTS ( ( 3, 2, 2, 2, 3 ),
 ( 0.02744854538997967483, 0.03125000000000000000, 0.04166666666666667823, 0.05208333333333335646, 0.06250000000000002776 ),
 .UNSPECIFIED. ) 
 CURVE ( )  GEOMETRIC_REPRESENTATION_ITEM ( )  RATIONAL_B_SPLINE_CURVE ( ( 0.9647168388458802202, 0.9722206238030204339, 1.000000000000000000, 0.9238795325112867385, 1.000000000000000000, 0.9238795325112867385, 1.000000000000000000, 0.9238795325112865164, 1.000000000000000222 ) ) 
 REPRESENTATION_ITEM ( '' )  );
#152=CARTESIAN_POINT ( 'NONE',  ( 0.3125000000000000000, -5.740531871003217465E-17, 0.3175000000000038347 ) ) ;
#156=AXIS2_PLACEMENT_3D ( 'NONE', #2067, #15007, #355 ) ;
#158=CARTESIAN_POINT ( 'NONE',  ( 0.05458059743777703143, -0.3010824892324204249, -0.09469801875939774793 ) ) ;
#164=CARTESIAN_POINT ( 'NONE',  ( -1.916134881958141055E-16, 0.5412658773652744282, 0.4425000000000000044 ) ) ;
#165=EDGE_CURVE ( 'NONE', #15529, #11169, #6067, .T. ) ;
#175=VERTEX_POINT ( 'NONE', #18914 ) ;
#176=CYLINDRICAL_SURFACE ( 'NONE', #2581, 0.01874999999999997155 ) ;
#181=CARTESIAN_POINT ( 'NONE',  ( -0.2720287551442893137, -0.3842100023554003152, 0.4182004018663288414 ) ) ;
#182=CARTESIAN_POINT ( 'NONE',  ( 0.2723623684625768870, -0.3840173906162817064, 0.09139303015897912164 ) ) ;
#195=CARTESIAN_POINT ( 'NONE',  ( 0.4570242136016807732, 0.2774028246161672207, 0.04874733047933993424 ) ) ;
#203=CARTESIAN_POINT ( 'NONE',  ( -0.2764156081756484196, -0.1144950937579609362, 0.2584722222222254340 ) ) ;
#205=CARTESIAN_POINT ( 'NONE',  ( 0.1954553509668047195, 0.1954553509668046085, -0.09916666666666627827 ) ) ;
#211=CARTESIAN_POINT ( 'NONE',  ( -0.4587679311106390156, 0.1778692279407495247, 0.4165783083332769698 ) ) ;
#223=CARTESIAN_POINT ( 'NONE',  ( -0.4226370775080299236, -0.2972562468964969895, 0.3901966308178843601 ) ) ;
#226=EDGE_CURVE ( 'NONE', #20003, #8247, #7693, .T. ) ;
#227=CARTESIAN_POINT ( 'NONE',  ( -0.2230971623002953874, 0.2230971623002954152, -0.1634027777777777302 ) ) ;
#228=EDGE_CURVE ( 'NONE', #4857, #5916, #14256, .T. ) ;
#238=CARTESIAN_POINT ( 'NONE',  ( 0.000000000000000000, 0.2764156081756484196, 0.08138888888889070361 ) ) ;
#241=CARTESIAN_POINT ( 'NONE',  ( 0.4687500000000002776, 0.02218466657066830647, 0.4181373467287273216 ) ) ;
#249=CARTESIAN_POINT ( 'NONE',  ( -0.4648120342697260043, -0.2865046371989117269, 0.04342012612512782810 ) ) ;
#257=CARTESIAN_POINT ( 'NONE',  ( 0.000000000000000000, 0.2764156081756484196, 0.02583333333333468970 ) ) ;
#264=CARTESIAN_POINT ( 'NONE',  ( -0.2230971623002953874, 0.2230971623002954152, 0.05534722222222363680 ) ) ;
#266=CARTESIAN_POINT ( 'NONE',  ( -0.3125000000000000000, 1.913510623667739771E-17, 0.01194444444444589179 ) ) ;
#267=FACE_OUTER_BOUND ( 'NONE', #5733, .T. ) ;
#280=VERTEX_POINT ( 'NONE', #11359 ) ;
#290=CARTESIAN_POINT ( 'NONE',  ( 0.07990078027837828334, 0.4951351403631162329, 0.4110703004652723758 ) ) ;
#294=EDGE_CURVE ( 'NONE', #17172, #5916, #19316, .T. ) ;
#295=( BOUNDED_SURFACE ( )  B_SPLINE_SURFACE ( 1, 2, ( 
 ( #11604, #5858, #4030, #20737, #17207, #9647, #17082, #11849, #19034, #19147, #372, #19266, #15255, #22685, #2335, #22805, #3045, #10254, #21459, #13912, #4742, #14142, #14385, #6459, #2799, #21571, #8525, #6578, #2687, #6946, #19389, #23628, #23268, #21341, #17922, #2920, #14028, #19505, #4865, #12331, #1334, #21813, #4628, #17801, #19746, #14263, #10379, #12448, #6822, #8764, #12214, #10492, #12095, #1093, #10139, #19622, #17563, #16093, #15968, #1217, #11976, #23389, #6696, #21698, #17681, #15850, #23149, #19864, #971, #854, #8645, #8283, #23507, #4983, #10609, #3159, #18038, #16216, #8400, #15736, #7188, #21927, #12568, #14631, #16456, #3524, #10973, #23997, #14758, #10852, #16576, #18518, #22053, #12939, #11088, #24115, #16694, #23746, #14993, #16819, #13054, #1808, #5102, #18160, #102, #5590, #19988, #20350, #9253, #5220, #5348, #7430, #14877, #12816, #18400, #22294, #7307, #3401, #20233, #20473, #3769, #3641, #11210, #18639, #1930, #3275, #9377, #10729, #23868, #7543, #1457, #1694, #8892, #16333, #7070, #14508, #9130, #22175, #18280, #12693, #5474, #1576, #20110, #9013, #22660, #16930, #2540, #9497, #2424, #5829, #15114, #9865, #706, #17178, #22415, #15347, #9742, #21068, #13406, #17050, #19119, #17293, #22540, #4122, #19236, #5718, #13652, #11695, #3885, #2057, #464, #11579, #20949, #7896, #4360, #4243, #17413, #9989, #15230 ),
 ( #11816, #19007, #227, #11453, #22774, #6069, #2187, #13536, #9618, #8134, #2304, #20830, #344, #585, #13177, #20590, #18760, #11330, #22894, #8016, #15468, #18885, #6188, #7784, #7663, #5949, #13294, #20709, #4003, #4954, #19834, #13884, #19476, #12300, #2770, #21312, #23238, #10344, #14113, #10223, #12419, #8491, #2884, #14231, #6546, #17649, #19714, #3017, #15705, #21427, #3132, #15585, #6792, #4832, #21190, #19360, #17771, #4715, #21544, #1063, #21668, #10464, #10584, #18012, #8367, #938, #15819, #4479, #11945, #17893, #1307, #12186, #2658, #4603, #15934, #23358, #13997, #6668, #19592, #23009, #1186, #8621, #16062, #23477, #6311, #13764, #10110, #17533, #825, #8253, #23120, #12063, #6429, #18250, #14353, #16429, #12787, #9099, #22146, #22266, #13029, #7040, #12662, #5444, #20080, #14479, #23838, #3491, #7281, #3373, #5563, #3249, #18614, #20443, #16666, #12908, #8732, #21785, #3740, #9229, #16187, #16547, #20322, #8858, #1547, #14730, #3609, #8984, #14601, #11062, #20205, #21903, #7160, #24089, #18491, #1784, #23969, #7401, #14851, #6914, #11186, #23599, #10824, #5071, #12541, #22024, #19961, #10697, #18133, #1431, #5322, #1666, #5193, #16302, #10943, #18371, #23715, #15086, #2155, #20563, #6157, #13150, #6039, #9468, #18734, #13506, #4331, #20802, #1905, #3974, #9711, #7869, #20920, #4213, #2031, #22635, #17022, #13379, #2275 ) ),
 .UNSPECIFIED., .F., .F., .F. ) 
 B_SPLINE_SURFACE_WITH_KNOTS ( ( 2, 2 ),
 ( 3, 2, 2, 2, 2, 2, 2, 2, 2, 2, 2, 2, 2, 2, 2, 2, 2, 2, 2, 2, 2, 2, 2, 2, 2, 2, 2, 2, 2, 2, 2, 2, 2, 2, 2, 2, 2, 2, 2, 2, 2, 2, 2, 2, 2, 2, 2, 2, 2, 2, 2, 2, 2, 2, 2, 2, 2, 2, 2, 2, 2, 2, 2, 2, 2, 2, 2, 2, 2, 2, 2, 2, 2, 2, 2, 2, 2, 2, 2, 2, 2, 2, 2, 2, 2, 2, 2, 2, 2, 3 ),
 ( 0.000000000000000000, 1.000000000000000000 ),
 ( 0.000000000000000000, 0.01041666666666666609, 0.02083333333333333218, 0.03125000000000000000, 0.04166666666666666435, 0.05208333333333333565, 0.06250000000000000000, 0.07291666666666667129, 0.08333333333333332871, 0.09375000000000000000, 0.1041666666666666713, 0.1145833333333333287, 0.1250000000000000000, 0.1354166666666666574, 0.1458333333333333426, 0.1562500000000000000, 0.1666666666666666574, 0.1770833333333333426, 0.1875000000000000000, 0.1979166666666666574, 0.2083333333333333426, 0.2187500000000000000, 0.2291666666666666574, 0.2395833333333333426, 0.2500000000000000000, 0.2604166666666666852, 0.2708333333333333148, 0.2812500000000000000, 0.2916666666666666852, 0.3020833333333333148, 0.3125000000000000000, 0.3229166666666666852, 0.3333333333333333148, 0.3437500000000000000, 0.3541666666666666852, 0.3645833333333333148, 0.3750000000000000000, 0.3854166666666666852, 0.3958333333333333148, 0.4062500000000000000, 0.4166666666666666852, 0.4270833333333333148, 0.4375000000000000000, 0.4479166666666666852, 0.4583333333333333148, 0.4687500000000000000, 0.4791666666666666852, 0.4895833333333333148, 0.5000000000000000000, 0.5104166666666666297, 0.5208333333333333703, 0.5312500000000000000, 0.5416666666666666297, 0.5520833333333333703, 0.5625000000000000000, 0.5729166666666666297, 0.5833333333333333703, 0.5937500000000000000, 0.6041666666666666297, 0.6145833333333333703, 0.6250000000000000000, 0.6354166666666666297, 0.6458333333333333703, 0.6562500000000000000, 0.6666666666666666297, 0.6770833333333333703, 0.6875000000000000000, 0.6979166666666666297, 0.7083333333333333703, 0.7187500000000000000, 0.7291666666666666297, 0.7395833333333333703, 0.7500000000000000000, 0.7604166666666666297, 0.7708333333333333703, 0.7812500000000000000, 0.7916666666666666297, 0.8020833333333333703, 0.8125000000000000000, 0.8229166666666666297, 0.8333333333333333703, 0.8437500000000000000, 0.8541666666666666297, 0.8645833333333333703, 0.8750000000000000000, 0.8854166666666666297, 0.8958333333333333703, 0.9062500000000000000, 0.9166666666666666297, 0.9270833333333333703 ),
 .UNSPECIFIED. ) 
 GEOMETRIC_REPRESENTATION_ITEM ( )  RATIONAL_B_SPLINE_SURFACE ( (
 ( 1.000000000000000000, 0.9238795325112867385, 1.000000000000000000, 0.9238795325112867385, 1.000000000000000000, 0.9238795325112867385, 1.000000000000000000, 0.9238795325112867385, 1.000000000000000000, 0.9238795325112867385, 1.000000000000000000, 0.9238795325112867385, 1.000000000000000000, 0.9238795325112867385, 1.000000000000000000, 0.9238795325112867385, 1.000000000000000000, 0.9238795325112867385, 1.000000000000000000, 0.9238795325112867385, 1.000000000000000000, 0.9238795325112867385, 1.000000000000000000, 0.9238795325112867385, 1.000000000000000000, 0.9238795325112867385, 1.000000000000000000, 0.9238795325112867385, 1.000000000000000000, 0.9238795325112867385, 1.000000000000000000, 0.9238795325112867385, 1.000000000000000000, 0.9238795325112867385, 1.000000000000000000, 0.9238795325112867385, 1.000000000000000000, 0.9238795325112867385, 1.000000000000000000, 0.9238795325112867385, 1.000000000000000000, 0.9238795325112867385, 1.000000000000000000, 0.9238795325112867385, 1.000000000000000000, 0.9238795325112867385, 1.000000000000000000, 0.9238795325112867385, 1.000000000000000000, 0.9238795325112867385, 1.000000000000000000, 0.9238795325112867385, 1.000000000000000000, 0.9238795325112867385, 1.000000000000000000, 0.9238795325112867385, 1.000000000000000000, 0.9238795325112867385, 1.000000000000000000, 0.9238795325112867385, 1.000000000000000000, 0.9238795325112867385, 1.000000000000000000, 0.9238795325112867385, 1.000000000000000000, 0.9238795325112867385, 1.000000000000000000, 0.9238795325112867385, 1.000000000000000000, 0.9238795325112867385, 1.000000000000000000, 0.9238795325112867385, 1.000000000000000000, 0.9238795325112867385, 1.000000000000000000, 0.9238795325112867385, 1.000000000000000000, 0.9238795325112867385, 1.000000000000000000, 0.9238795325112867385, 1.000000000000000000, 0.9238795325112867385, 1.000000000000000000, 0.9238795325112867385, 1.000000000000000000, 0.9238795325112867385, 1.000000000000000000, 0.9238795325112867385, 1.000000000000000000, 0.9238795325112867385, 1.000000000000000000, 0.9238795325112867385, 1.000000000000000000, 0.9238795325112867385, 1.000000000000000000, 0.9238795325112867385, 1.000000000000000000, 0.9238795325112867385, 1.000000000000000000, 0.9238795325112867385, 1.000000000000000000, 0.9238795325112867385, 1.000000000000000000, 0.9238795325112867385, 1.000000000000000000, 0.9238795325112867385, 1.000000000000000000, 0.9238795325112867385, 1.000000000000000000, 0.9238795325112867385, 1.000000000000000000, 0.9238795325112867385, 1.000000000000000000, 0.9238795325112867385, 1.000000000000000000, 0.9238795325112867385, 1.000000000000000000, 0.9238795325112867385, 1.000000000000000000, 0.9238795325112867385, 1.000000000000000000, 0.9238795325112867385, 1.000000000000000000, 0.9238795325112867385, 1.000000000000000000, 0.9238795325112867385, 1.000000000000000000, 0.9238795325112867385, 1.000000000000000000, 0.9238795325112867385, 1.000000000000000000, 0.9238795325112867385, 1.000000000000000000, 0.9238795325112867385, 1.000000000000000000, 0.9238795325112867385, 1.000000000000000000, 0.9238795325112867385, 1.000000000000000000, 0.9238795325112867385, 1.000000000000000000, 0.9238795325112867385, 1.000000000000000000, 0.9238795325112867385, 1.000000000000000000, 0.9238795325112867385, 1.000000000000000000, 0.9238795325112867385, 1.000000000000000000, 0.9238795325112867385, 1.000000000000000000, 0.9238795325112867385, 1.000000000000000000, 0.9238795325112867385, 1.000000000000000000, 0.9238795325112867385, 1.000000000000000000, 0.9238795325112867385, 1.000000000000000000, 0.9238795325112867385, 1.000000000000000000, 0.9238795325112867385, 1.000000000000000000, 0.9238795325112867385, 1.000000000000000000, 0.9238795325112867385, 1.000000000000000000, 0.9238795325112867385, 1.000000000000000000, 0.9238795325112867385, 1.000000000000000000, 0.9238795325112867385, 1.000000000000000000, 0.9238795325112867385, 1.000000000000000000, 0.9238795325112867385, 1.000000000000000000, 0.9238795325112867385, 1.000000000000000000),
 ( 1.000000000000000000, 0.9238795325112867385, 1.000000000000000000, 0.9238795325112867385, 1.000000000000000000, 0.9238795325112867385, 1.000000000000000000, 0.9238795325112867385, 1.000000000000000000, 0.9238795325112867385, 1.000000000000000000, 0.9238795325112867385, 1.000000000000000000, 0.9238795325112867385, 1.000000000000000000, 0.9238795325112867385, 1.000000000000000000, 0.9238795325112867385, 1.000000000000000000, 0.9238795325112867385, 1.000000000000000000, 0.9238795325112867385, 1.000000000000000000, 0.9238795325112867385, 1.000000000000000000, 0.9238795325112867385, 1.000000000000000000, 0.9238795325112867385, 1.000000000000000000, 0.9238795325112867385, 1.000000000000000000, 0.9238795325112867385, 1.000000000000000000, 0.9238795325112867385, 1.000000000000000000, 0.9238795325112867385, 1.000000000000000000, 0.9238795325112867385, 1.000000000000000000, 0.9238795325112867385, 1.000000000000000000, 0.9238795325112867385, 1.000000000000000000, 0.9238795325112867385, 1.000000000000000000, 0.9238795325112867385, 1.000000000000000000, 0.9238795325112867385, 1.000000000000000000, 0.9238795325112867385, 1.000000000000000000, 0.9238795325112867385, 1.000000000000000000, 0.9238795325112867385, 1.000000000000000000, 0.9238795325112867385, 1.000000000000000000, 0.9238795325112867385, 1.000000000000000000, 0.9238795325112867385, 1.000000000000000000, 0.9238795325112867385, 1.000000000000000000, 0.9238795325112867385, 1.000000000000000000, 0.9238795325112867385, 1.000000000000000000, 0.9238795325112867385, 1.000000000000000000, 0.9238795325112867385, 1.000000000000000000, 0.9238795325112867385, 1.000000000000000000, 0.9238795325112867385, 1.000000000000000000, 0.9238795325112867385, 1.000000000000000000, 0.9238795325112867385, 1.000000000000000000, 0.9238795325112867385, 1.000000000000000000, 0.9238795325112867385, 1.000000000000000000, 0.9238795325112867385, 1.000000000000000000, 0.9238795325112867385, 1.000000000000000000, 0.9238795325112867385, 1.000000000000000000, 0.9238795325112867385, 1.000000000000000000, 0.9238795325112867385, 1.000000000000000000, 0.9238795325112867385, 1.000000000000000000, 0.9238795325112867385, 1.000000000000000000, 0.9238795325112867385, 1.000000000000000000, 0.9238795325112867385, 1.000000000000000000, 0.9238795325112867385, 1.000000000000000000, 0.9238795325112867385, 1.000000000000000000, 0.9238795325112867385, 1.000000000000000000, 0.9238795325112867385, 1.000000000000000000, 0.9238795325112867385, 1.000000000000000000, 0.9238795325112867385, 1.000000000000000000, 0.9238795325112867385, 1.000000000000000000, 0.9238795325112867385, 1.000000000000000000, 0.9238795325112867385, 1.000000000000000000, 0.9238795325112867385, 1.000000000000000000, 0.9238795325112867385, 1.000000000000000000, 0.9238795325112867385, 1.000000000000000000, 0.9238795325112867385, 1.000000000000000000, 0.9238795325112867385, 1.000000000000000000, 0.9238795325112867385, 1.000000000000000000, 0.9238795325112867385, 1.000000000000000000, 0.9238795325112867385, 1.000000000000000000, 0.9238795325112867385, 1.000000000000000000, 0.9238795325112867385, 1.000000000000000000, 0.9238795325112867385, 1.000000000000000000, 0.9238795325112867385, 1.000000000000000000, 0.9238795325112867385, 1.000000000000000000, 0.9238795325112867385, 1.000000000000000000, 0.9238795325112867385, 1.000000000000000000, 0.9238795325112867385, 1.000000000000000000, 0.9238795325112867385, 1.000000000000000000, 0.9238795325112867385, 1.000000000000000000, 0.9238795325112867385, 1.000000000000000000, 0.9238795325112867385, 1.000000000000000000, 0.9238795325112867385, 1.000000000000000000, 0.9238795325112867385, 1.000000000000000000, 0.9238795325112867385, 1.000000000000000000, 0.9238795325112867385, 1.000000000000000000, 0.9238795325112867385, 1.000000000000000000, 0.9238795325112867385, 1.000000000000000000, 0.9238795325112867385, 1.000000000000000000, 0.9238795325112867385, 1.000000000000000000, 0.9238795325112867385, 1.000000000000000000, 0.9238795325112867385, 1.000000000000000000) ) ) 
 REPRESENTATION_ITEM ( '' )  SURFACE ( )  );
#301=CARTESIAN_POINT ( 'NONE',  ( -0.3874422277197493436, -0.3175760028958487524, 0.4114235598616964862 ) ) ;
#307=ADVANCED_FACE ( 'NONE', ( #10137 ), #17850, .F. ) ;
#314=VERTEX_POINT ( 'NONE', #21339 ) ;
#320=CARTESIAN_POINT ( 'NONE',  ( 0.1954553509668046640, -0.1954553509668047195, 0.3383333333333371495 ) ) ;
#322=CIRCLE ( 'NONE', #10458, 1.200750000000023299 ) ;
#323=CARTESIAN_POINT ( 'NONE',  ( 0.2764156081756483641, 0.1144950937579610195, 0.3418055555555594149 ) ) ;
#325=CARTESIAN_POINT ( 'NONE',  ( 0.1954553509668046640, -0.1954553509668047195, -0.05749999999999928085 ) ) ;
#340=CARTESIAN_POINT ( 'NONE',  ( -0.4620259694561524855, 0.2880908832651556950, 0.04413116910601659615 ) ) ;
#344=CARTESIAN_POINT ( 'NONE',  ( 0.3155070326520292845, -5.795770164686806123E-17, -0.1286805555555552150 ) ) ;
#345=B_SPLINE_CURVE_WITH_KNOTS ( 'NONE', 3,
 ( #21694, #10489, #23503, #6818, #14260, #4977 ),
 .UNSPECIFIED., .F., .F.,
 ( 4, 2, 4 ),
 ( 0.000000000000000000, 0.0002551367231383054124, 0.0005102734462766108248 ),
 .UNSPECIFIED. ) ;
#351=CARTESIAN_POINT ( 'NONE',  ( 0.1144950937579611444, 0.2764156081756483641, -0.08874999999999956535 ) ) ;
#353=CARTESIAN_POINT ( 'NONE',  ( 0.08325293014416497439, 0.4931997757357156065, 0.4003306813560891242 ) ) ;
#354=CARTESIAN_POINT ( 'NONE',  ( 0.2764156081756483641, 0.1144950937579610056, 0.1265277777777799595 ) ) ;
#355=DIRECTION ( 'NONE',  ( 0.000000000000000000, 0.000000000000000000, -1.000000000000000000 ) ) ;
#362=FACE_OUTER_BOUND ( 'NONE', #13312, .T. ) ;
#367=CARTESIAN_POINT ( 'NONE',  ( 0.05485615681475830563, -0.5228774440028900461, 0.05347937985141015815 ) ) ;
#372=CARTESIAN_POINT ( 'NONE',  ( 0.1954553509668046640, -0.1954553509668047195, -0.1130555555555552844 ) ) ;
#373=AXIS2_PLACEMENT_3D ( 'NONE', #16147, #5038, #21752 ) ;
#377=CARTESIAN_POINT ( 'NONE',  ( 0.2764156081756483641, -0.1144950937579611028, 0.008472222222223454655 ) ) ;
#381=CARTESIAN_POINT ( 'NONE',  ( -0.3125000000000000000, 0.000000000000000000, 1.326383476483184332 ) ) ;
#383=CARTESIAN_POINT ( 'NONE',  ( -3.863846776457871776E-17, -0.3155070326520292845, 0.1317361111111131078 ) ) ;
#384=CARTESIAN_POINT ( 'NONE',  ( 0.4687500000000003886, 0.1745743740738040783, 0.4003190680884846642 ) ) ;
#386=CARTESIAN_POINT ( 'NONE',  ( -0.2782766723721450952, -0.03026958819837442111, -0.06867859833352769894 ) ) ;
#405=CARTESIAN_POINT ( 'NONE',  ( 0.08610082984204511791, 0.2741627315343106996, 0.3988756756980814111 ) ) ;
#407=CYLINDRICAL_SURFACE ( 'NONE', #2541, 0.3125000000000000000 ) ;
#421=CARTESIAN_POINT ( 'NONE',  ( 0.2764156081756484196, -5.077672346800151106E-17, 0.4494444444444492537 ) ) ;
#424=CARTESIAN_POINT ( 'NONE',  ( 0.4593750000000003664, -0.2760455974562899817, 0.3779506566538943235 ) ) ;
#425=CARTESIAN_POINT ( 'NONE',  ( -0.4500000000000003997, 0.2598076211353315679, 0.3779506566538943235 ) ) ;
#434=ORIENTED_EDGE ( 'NONE', *, *, #12786, .F. ) ;
#438=DIRECTION ( 'NONE',  ( 0.000000000000000000, 0.000000000000000000, -1.000000000000000000 ) ) ;
#444=CARTESIAN_POINT ( 'NONE',  ( 0.2764156081756483641, 0.1144950937579610195, 0.2862500000000035572 ) ) ;
#446=CARTESIAN_POINT ( 'NONE',  ( 0.000000000000000000, 0.2764156081756484196, -0.09222222222222178911 ) ) ;
#449=CARTESIAN_POINT ( 'NONE',  ( 0.006583558500310691085, -0.5374648580928945707, 0.05971062996525675765 ) ) ;
#451=CARTESIAN_POINT ( 'NONE',  ( -0.1458082941847503033, 0.2460910087212002384, -0.07505195856086301076 ) ) ;
#454=CARTESIAN_POINT ( 'NONE',  ( 0.2195630361086305937, -0.1679215936616662852, 0.3880822748423153334 ) ) ;
#464=CARTESIAN_POINT ( 'NONE',  ( 0.1954553509668046640, -0.1954553509668047195, 0.4425000000000047229 ) ) ;
#465=DIRECTION ( 'NONE',  ( -1.000000000000000000, 0.000000000000000000, 0.000000000000000000 ) ) ;
#467=EDGE_CURVE ( 'NONE', #10173, #22264, #19322, .T. ) ;
#473=CARTESIAN_POINT ( 'NONE',  ( 0.1954553509668046640, -0.1954553509668047195, 0.1161111111111132049 ) ) ;
#479=EDGE_CURVE ( 'NONE', #5967, #549, #1001, .T. ) ;
#487=AXIS2_PLACEMENT_3D ( 'NONE', #15948, #3030, #21441 ) ;
#488=CARTESIAN_POINT ( 'NONE',  ( 0.01172578639831932910, 0.5344959914317446437, 0.04874733047933995506 ) ) ;
#490=CARTESIAN_POINT ( 'NONE',  ( 0.4805070082343983473, -0.2560807851245830435, 0.04413116910601658921 ) ) ;
#495=CARTESIAN_POINT ( 'NONE',  ( 0.000000000000000000, 0.2764156081756484196, -0.02972222222222129645 ) ) ;
#501=CARTESIAN_POINT ( 'NONE',  ( 0.3155070326520292290, 0.1306872919485615736, 0.2046527777777804036 ) ) ;
#503=CARTESIAN_POINT ( 'NONE',  ( 0.3125000000000000000, -5.740531871003217465E-17, 0.03277777777777902274 ) ) ;
#513=CARTESIAN_POINT ( 'NONE',  ( 0.2209708691207961095, -0.2209708691207961651, 0.2480555555555585268 ) ) ;
#517=CARTESIAN_POINT ( 'NONE',  ( 0.2774634594257791576, -0.1150700753240518487, -0.08907806777757856787 ) ) ;
#520=CARTESIAN_POINT ( 'NONE',  ( -0.3065849364905382513, 4.708020935245015622E-15, -0.09575160315720471216 ) ) ;
#521=EDGE_CURVE ( 'NONE', #8592, #18897, #11168, .T. ) ;
#523=ORIENTED_EDGE ( 'NONE', *, *, #20352, .F. ) ;
#526=ADVANCED_FACE ( 'NONE', ( #16455 ), #6821, .T. ) ;
#533=ORIENTED_EDGE ( 'NONE', *, *, #294, .F. ) ;
#546=EDGE_LOOP ( 'NONE', ( #12242, #17366, #3544, #9068 ) ) ;
#549=VERTEX_POINT ( 'NONE', #12692 ) ;
#553=CARTESIAN_POINT ( 'NONE',  ( 0.3124999999999989453, 0.1294417382415933571, 0.2584722222222253230 ) ) ;
#556=CARTESIAN_POINT ( 'NONE',  ( -0.4687500000000002776, -0.1098280991662788780, 0.4107862666565998966 ) ) ;
#557=LINE ( 'NONE', #17027, #4020 ) ;
#559=CARTESIAN_POINT ( 'NONE',  ( -0.1954553509668046640, 0.1954553509668046918, 0.1369444444444467002 ) ) ;
#561=CARTESIAN_POINT ( 'NONE',  ( 0.1954553509668046640, -0.1954553509668047195, 0.4494444444444491427 ) ) ;
#562=EDGE_CURVE ( 'NONE', #15146, #13004, #700, .T. ) ;
#581=( BOUNDED_CURVE ( )  B_SPLINE_CURVE ( 2, ( #7062, #19982, #3270, #7304, #10723, #20106, #16572, #22169, #3395 ),
 .UNSPECIFIED., .F., .F. ) 
 B_SPLINE_CURVE_WITH_KNOTS ( ( 3, 2, 2, 2, 3 ),
 ( 0.3541666666666666852, 0.3645833333333333703, 0.3750000000000000555, 0.3854166666666667407, 0.3958333333333334259 ),
 .UNSPECIFIED. ) 
 CURVE ( )  GEOMETRIC_REPRESENTATION_ITEM ( )  RATIONAL_B_SPLINE_CURVE ( ( 1.000000000000000000, 0.9238795325112867385, 1.000000000000000000, 0.9238795325112867385, 1.000000000000000000, 0.9238795325112867385, 1.000000000000000000, 0.9238795325112859613, 1.000000000000000888 ) ) 
 REPRESENTATION_ITEM ( '' )  );
#584=SPHERICAL_SURFACE ( 'NONE', #1430, 0.01874999999999999931 ) ;
#585=CARTESIAN_POINT ( 'NONE',  ( 0.3155070326520292290, 0.1306872919485615736, -0.1252083333333329496 ) ) ;
#593=CARTESIAN_POINT ( 'NONE',  ( -0.2107770390571470920, -0.2008625216908039579, -0.07979188311515521270 ) ) ;
#594=CARTESIAN_POINT ( 'NONE',  ( -0.1954553509668046918, -0.1954553509668046640, 0.2133333333333361503 ) ) ;
#597=DIRECTION ( 'NONE',  ( 0.000000000000000000, 0.000000000000000000, 1.000000000000000000 ) ) ;
#607=ORIENTED_EDGE ( 'NONE', *, *, #85, .F. ) ;
#608=CARTESIAN_POINT ( 'NONE',  ( 0.2998642343065497373, 0.08796414601275419354, 0.4241666666666771834 ) ) ;
#615=CARTESIAN_POINT ( 'NONE',  ( -1.856450067443490846E-16, 0.5196152422706634688, 0.3779506566538943790 ) ) ;
#628=CARTESIAN_POINT ( 'NONE',  ( 0.2230971623002953874, -0.2230971623002954429, 0.1386805555555576386 ) ) ;
#641=CARTESIAN_POINT ( 'NONE',  ( -0.009375000000000190473, 0.5358532185916217161, 0.3779506566538943790 ) ) ;
#642=VECTOR ( 'NONE', #11209, 39.37007874015748143 ) ;
#643=EDGE_CURVE ( 'NONE', #17766, #11636, #18399, .T. ) ;
#653=CARTESIAN_POINT ( 'NONE',  ( 0.07411063262685617381, 0.4869405031891889668, 0.4162703459413902851 ) ) ;
#654=FACE_OUTER_BOUND ( 'NONE', #10954, .T. ) ;
#667=ORIENTED_EDGE ( 'NONE', *, *, #19117, .F. ) ;
#677=EDGE_CURVE ( 'NONE', #3460, #23837, #22893, .T. ) ;
#679=CARTESIAN_POINT ( 'NONE',  ( -0.3834923435458895136, -0.3083291687941427384, 0.4165495381634257144 ) ) ;
#680=CARTESIAN_POINT ( 'NONE',  ( 0.2209708691207961651, 0.2209708691207959985, 0.2619444444444474773 ) ) ;
#683=DIRECTION ( 'NONE',  ( -0.8459207832372985791, 0.4883925919151526074, 0.2142211582677925885 ) ) ;
#684=CARTESIAN_POINT ( 'NONE',  ( 0.05482159418621733449, -0.5228976771666083989, 0.05347049744908469182 ) ) ;
#685=CARTESIAN_POINT ( 'NONE',  ( 0.1954553509668046640, -0.1954553509668047195, 0.1647222222222247123 ) ) ;
#687=CARTESIAN_POINT ( 'NONE',  ( 0.000000000000000000, 0.2764156081756484196, 0.4147222222222267107 ) ) ;
#688=ORIENTED_EDGE ( 'NONE', *, *, #165, .T. ) ;
#692=CARTESIAN_POINT ( 'NONE',  ( 0.4582856249906270274, -0.2428769834202093303, 0.4003459333743809578 ) ) ;
#700=B_SPLINE_CURVE_WITH_KNOTS ( 'NONE', 3,
 ( #1333, #5472, #3158, #14757, #22052, #8763, #3400, #16215, #7069, #14507, #7187, #23627 ),
 .UNSPECIFIED., .F., .F.,
 ( 4, 2, 2, 2, 2, 4 ),
 ( 0.000000000000000000, 0.001386135995484534143, 0.002079203993226801106, 0.002772271990969068286, 0.004158407986453602212, 0.005544543981938136572 ),
 .UNSPECIFIED. ) ;
#703=CARTESIAN_POINT ( 'NONE',  ( 0.4500000000000003442, 0.2598076211353319009, 0.3779506566538943235 ) ) ;
#706=CARTESIAN_POINT ( 'NONE',  ( -3.385114897866767815E-17, -0.2764156081756484196, 0.3800000000000042233 ) ) ;
#709=ORIENTED_EDGE ( 'NONE', *, *, #14837, .F. ) ;
#715=CARTESIAN_POINT ( 'NONE',  ( 0.2764156081756484196, -5.077672346800151106E-17, 0.2897222222222257115 ) ) ;
#718=CARTESIAN_POINT ( 'NONE',  ( 0.01294618724694471777, 0.5474118055169124863, 0.04270874187135767497 ) ) ;
#723=PLANE ( 'NONE',  #3425 ) ;
#724=CARTESIAN_POINT ( 'NONE',  ( -0.3118573088780928759, 0.3612149761357835165, 0.4243809486557250099 ) ) ;
#734=CARTESIAN_POINT ( 'NONE',  ( -0.4687500000000003331, -0.2570931668155775340, 0.04874733047933996893 ) ) ;
#739=CARTESIAN_POINT ( 'NONE',  ( -0.1144950937579609779, 0.2764156081756484196, -0.02624999999999906228 ) ) ;
#746=CARTESIAN_POINT ( 'NONE',  ( 0.1306872919485614071, -0.3155070326520293955, 0.2463194444444473108 ) ) ;
#756=CARTESIAN_POINT ( 'NONE',  ( 0.3125000000000000000, -5.740531871003217465E-17, 0.2550000000000030020 ) ) ;
#759=CARTESIAN_POINT ( 'NONE',  ( -0.2722827744214833534, 0.3840633442573329615, 0.4172182224143142215 ) ) ;
#765=CARTESIAN_POINT ( 'NONE',  ( 0.2663171304906554182, 0.09313777201924491878, 0.3936412650000162827 ) ) ;
#785=ADVANCED_FACE ( 'NONE', ( #4602 ), #584, .T. ) ;
#791=CONICAL_SURFACE ( 'NONE', #3127, 0.3308333333333332571, 0.7853981633974427279 ) ;
#796=CARTESIAN_POINT ( 'NONE',  ( 0.1294417382415924134, 0.3124999999999999445, 0.05013888888889062728 ) ) ;
#797=CARTESIAN_POINT ( 'NONE',  ( 0.1294417382415924134, 0.3124999999999999445, 0.2654166666666697427 ) ) ;
#801=CARTESIAN_POINT ( 'NONE',  ( -0.4687500000000004441, -0.1747720533650699848, 0.4002708887178494379 ) ) ;
#805=CARTESIAN_POINT ( 'NONE',  ( -3.385114897866767815E-17, -0.2764156081756484196, 0.1577777777777801815 ) ) ;
#812=DIRECTION ( 'NONE',  ( -1.000000000000000000, 0.000000000000000000, 0.000000000000000000 ) ) ;
#817=ADVANCED_FACE ( 'NONE', ( #13763 ), #15213, .F. ) ;
#825=CARTESIAN_POINT ( 'NONE',  ( -3.863846776457871776E-17, -0.3155070326520292845, 0.1352083333333357895 ) ) ;
#827=CARTESIAN_POINT ( 'NONE',  ( -0.1963876315374235015, -0.4278814254316300469, 0.09139303015897908000 ) ) ;
#833=CARTESIAN_POINT ( 'NONE',  ( 0.000000000000000000, 3.738758431839877614E-19, -0.1012499999999999928 ) ) ;
#834=CARTESIAN_POINT ( 'NONE',  ( -0.1975560007913283733, -0.2122688852238888424, -0.07862277518649050945 ) ) ;
#835=CARTESIAN_POINT ( 'NONE',  ( 0.000000000000000000, 0.2764156081756484196, 0.4702777777777826795 ) ) ;
#838=CARTESIAN_POINT ( 'NONE',  ( 0.000000000000000000, 3.738758431839877614E-19, 0.4425000000000000044 ) ) ;
#843=EDGE_CURVE ( 'NONE', #4460, #20446, #15558, .T. ) ;
#844=DIRECTION ( 'NONE',  ( 1.000000000000000000, -1.821231995776178240E-15, 0.000000000000000000 ) ) ;
#845=CARTESIAN_POINT ( 'NONE',  ( -1.975393552757948877E-16, 0.5289902422706634910, 0.3941886329748526263 ) ) ;
#849=CARTESIAN_POINT ( 'NONE',  ( -0.3125000000000000000, 1.913510623667739771E-17, 0.1230555555555578606 ) ) ;
#853=CARTESIAN_POINT ( 'NONE',  ( -0.4687500000000003886, 0.04414795829722523157, 0.09139193563994604808 ) ) ;
#854=CARTESIAN_POINT ( 'NONE',  ( -0.2764156081756484196, -0.1144950937579609362, 0.09180555555555744429 ) ) ;
#857=CARTESIAN_POINT ( 'NONE',  ( 0.4805070082343983473, 0.2560807851245830991, 0.04413116910601658921 ) ) ;
#858=CARTESIAN_POINT ( 'NONE',  ( -0.1144950937579609779, 0.2764156081756484196, 0.3070833333333368720 ) ) ;
#863=CARTESIAN_POINT ( 'NONE',  ( -0.3125000000000000000, 1.913510623667739771E-17, 0.005000000000001014917 ) ) ;
#864=CARTESIAN_POINT ( 'NONE',  ( 0.000000000000000000, 0.3155070326520292845, 0.3817361111111151062 ) ) ;
#874=ADVANCED_FACE ( 'NONE', ( #10250 ), #21693, .F. ) ;
#875=CARTESIAN_POINT ( 'NONE',  ( 0.04643634559190757544, -0.5144558407376040865, 0.07050986311825921393 ) ) ;
#884=VECTOR ( 'NONE', #16865, 39.37007874015748143 ) ;
#887=ORIENTED_EDGE ( 'NONE', *, *, #19117, .T. ) ;
#905=ORIENTED_EDGE ( 'NONE', *, *, #22479, .F. ) ;
#917=CARTESIAN_POINT ( 'NONE',  ( -0.4592305972001431980, 0.09034966327427822186, 0.4304950168282474232 ) ) ;
#921=CARTESIAN_POINT ( 'NONE',  ( 0.000000000000000000, 0.2764156081756484196, -0.03666666666666578561 ) ) ;
#928=CARTESIAN_POINT ( 'NONE',  ( 0.3125000000000000000, -5.740531871003217465E-17, 0.03277777777777902274 ) ) ;
#938=CARTESIAN_POINT ( 'NONE',  ( -0.1306872919485614903, 0.3155070326520293400, 0.05534722222222404620 ) ) ;
#940=EDGE_CURVE ( 'NONE', #1752, #2863, #22250, .T. ) ;
#943=CARTESIAN_POINT ( 'NONE',  ( 0.1144950937579611444, 0.2764156081756483641, 0.1334722222222244348 ) ) ;
#944=CARTESIAN_POINT ( 'NONE',  ( -0.2209708691207961373, -0.2209708691207961095, 0.4077777777777823465 ) ) ;
#945=CARTESIAN_POINT ( 'NONE',  ( -0.2353592251390640433, -0.1755526922479207774, -0.08225883004808118293 ) ) ;
#946=CARTESIAN_POINT ( 'NONE',  ( 0.1144950937579611444, 0.2764156081756483641, 0.3556944444444484210 ) ) ;
#950=CARTESIAN_POINT ( 'NONE',  ( 0.2195630361086305937, -0.1679215936616662852, 0.3880822748423153334 ) ) ;
#955=FACE_OUTER_BOUND ( 'NONE', #1634, .T. ) ;
#956=CARTESIAN_POINT ( 'NONE',  ( -0.2491691211423121832, 0.3865828334249355458, 0.4343841983240315785 ) ) ;
#960=VERTEX_POINT ( 'NONE', #13561 ) ;
#966=ADVANCED_FACE ( 'NONE', ( #4385 ), #20199, .F. ) ;
#970=CARTESIAN_POINT ( 'NONE',  ( -0.4687500000000003886, -0.2172202243938534394, 0.07046438675350588654 ) ) ;
#971=CARTESIAN_POINT ( 'NONE',  ( -0.2764156081756484196, 1.692557448933383907E-17, 0.08833333333333522053 ) ) ;
#974=CARTESIAN_POINT ( 'NONE',  ( 0.2209708691207961651, 0.2209708691207959985, -0.07138888888888847428 ) ) ;
#977=CARTESIAN_POINT ( 'NONE',  ( 0.1144950937579611444, 0.2764156081756483641, 0.2445833333333364279 ) ) ;
#981=CARTESIAN_POINT ( 'NONE',  ( -0.04489076912979070993, 0.2868701433674720191, 0.4014144183689973833 ) ) ;
#982=CARTESIAN_POINT ( 'NONE',  ( 0.4593750000000003664, -0.2760455974562899262, 0.4425000000000000044 ) ) ;
#985=CARTESIAN_POINT ( 'NONE',  ( 0.1306872919485614071, -0.3155070326520293955, 0.4129861111111153837 ) ) ;
#992=CIRCLE ( 'NONE', #6430, 0.3308333333333332571 ) ;
#1001=B_SPLINE_CURVE_WITH_KNOTS ( 'NONE', 3,
 ( #12567, #23506, #8644, #1456, #19987, #23744 ),
 .UNSPECIFIED., .F., .F.,
 ( 4, 2, 4 ),
 ( 0.000000000000000000, 0.0002551367231383059545, 0.0005102734462766119090 ),
 .UNSPECIFIED. ) ;
#1008=CARTESIAN_POINT ( 'NONE',  ( -0.4687500000000004441, 0.2598076211353315124, 0.06112444011295375262 ) ) ;
#1012=ORIENTED_EDGE ( 'NONE', *, *, #3070, .F. ) ;
#1020=CARTESIAN_POINT ( 'NONE',  ( -0.4620259694561524855, -0.2880908832651560281, 0.04413116910601651982 ) ) ;
#1028=ORIENTED_EDGE ( 'NONE', *, *, #8889, .T. ) ;
#1037=CARTESIAN_POINT ( 'NONE',  ( 0.4687499999999988343, 0.2570931668155638783, 0.04874733047934382002 ) ) ;
#1039=CARTESIAN_POINT ( 'NONE',  ( 0.4581189881604794123, 0.2644951211353319120, 0.3941886329748525153 ) ) ;
#1046=CARTESIAN_POINT ( 'NONE',  ( -0.1954553509668046640, 0.1954553509668046918, 0.3591666666666706864 ) ) ;
#1048=CARTESIAN_POINT ( 'NONE',  ( -0.1144950937579609918, -0.2764156081756484196, 0.04319444444444596465 ) ) ;
#1051=CARTESIAN_POINT ( 'NONE',  ( -3.827021247335479543E-17, -0.3125000000000000000, 0.4077777777777820134 ) ) ;
#1063=CARTESIAN_POINT ( 'NONE',  ( 0.3155070326520292290, -0.1306872919485616569, 0.03451388888889055095 ) ) ;
#1068=SPHERICAL_SURFACE ( 'NONE', #9766, 0.01874999999999999931 ) ;
#1069=CARTESIAN_POINT ( 'NONE',  ( -0.1144950937579609918, -0.2764156081756484196, -0.06097222222222156013 ) ) ;
#1070=CARTESIAN_POINT ( 'NONE',  ( 0.3125000000000000000, -5.740531871003217465E-17, 0.08833333333333501236 ) ) ;
#1071=CARTESIAN_POINT ( 'NONE',  ( 0.000000000000000000, 0.2764156081756484196, 0.3591666666666706309 ) ) ;
#1073=( BOUNDED_SURFACE ( )  B_SPLINE_SURFACE ( 3, 2, ( 
 ( #7988, #195, #5802 ),
 ( #22385, #22508, #3860 ),
 ( #11303, #7637, #2990 ),
 ( #19206, #8102, #14207 ),
 ( #2514, #2856, #15907 ),
 ( #4575, #1037, #6641 ) ),
 .UNSPECIFIED., .F., .F., .F. ) 
 B_SPLINE_SURFACE_WITH_KNOTS ( ( 4, 2, 4 ),
 ( 3, 3 ),
 ( 0.001402224832186925365, 0.001901366090229829938, 0.002400507348272734511 ),
 ( 0.000000000000000000, 1.000000000000000000 ),
 .UNSPECIFIED. ) 
 GEOMETRIC_REPRESENTATION_ITEM ( )  RATIONAL_B_SPLINE_SURFACE ( (
 ( 1.000000000000000000, 0.8285407536241359283, 1.000000000000000000),
 ( 1.000000000000000000, 0.8382697314792391108, 1.000000000000000000),
 ( 1.000000000000000000, 0.8433836253084343593, 1.000000000000000000),
 ( 1.000000000000000000, 0.8433992480894421107, 1.000000000000000000),
 ( 1.000000000000000000, 0.8382827608170027034, 1.000000000000000000),
 ( 1.000000000000000000, 0.8285407536241046200, 1.000000000000000000) ) ) 
 REPRESENTATION_ITEM ( '' )  SURFACE ( )  );
#1083=CARTESIAN_POINT ( 'NONE',  ( -0.2537239961729407800, 0.3947782598749492999, 0.4289714952839164819 ) ) ;
#1093=CARTESIAN_POINT ( 'NONE',  ( -0.2764156081756484196, -0.1144950937579609362, 0.03625000000000147549 ) ) ;
#1098=CARTESIAN_POINT ( 'NONE',  ( -0.2764156081756484196, 1.692557448933383907E-17, 0.2619444444444476994 ) ) ;
#1101=CARTESIAN_POINT ( 'NONE',  ( 0.4687500000000002776, 0.08780953131551477719, 0.08855729252016260322 ) ) ;
#1105=CARTESIAN_POINT ( 'NONE',  ( 0.1306872919485616846, 0.3155070326520292290, 0.3782638888888927853 ) ) ;
#1111=EDGE_CURVE ( 'NONE', #7699, #14213, #18549, .T. ) ;
#1115=ORIENTED_EDGE ( 'NONE', *, *, #8759, .F. ) ;
#1123=CARTESIAN_POINT ( 'NONE',  ( -0.1956796206285029427, 0.4282901957204844345, 0.4181140142936810578 ) ) ;
#1129=ORIENTED_EDGE ( 'NONE', *, *, #21873, .F. ) ;
#1147=CARTESIAN_POINT ( 'NONE',  ( -0.4620259694561523744, -0.2880908832651560281, 0.04413116910601651982 ) ) ;
#1169=CARTESIAN_POINT ( 'NONE',  ( -0.2764156081756484196, 1.692557448933383907E-17, 0.03277777777777921009 ) ) ;
#1172=CARTESIAN_POINT ( 'NONE',  ( -0.3125000000000000000, 1.913510623667739771E-17, 0.3938888888888930628 ) ) ;
#1178=CARTESIAN_POINT ( 'NONE',  ( -0.2209708691207961095, 0.2209708691207961373, 0.1647222222222244903 ) ) ;
#1180=( BOUNDED_CURVE ( )  B_SPLINE_CURVE ( 2, ( #8103, #553, #680, #797, #22868, #6282, #8224, #15675, #6403 ),
 .UNSPECIFIED., .F., .F. ) 
 B_SPLINE_CURVE_WITH_KNOTS ( ( 3, 2, 2, 2, 3 ),
 ( 0.5625000000000001110, 0.5729166666666667407, 0.5833333333333334814, 0.5937500000000001110, 0.6041666666666667407 ),
 .UNSPECIFIED. ) 
 CURVE ( )  GEOMETRIC_REPRESENTATION_ITEM ( )  RATIONAL_B_SPLINE_CURVE ( ( 0.9999999999999992228, 0.9238795325112875156, 1.000000000000000000, 0.9238795325112867385, 1.000000000000000000, 0.9238795325112867385, 1.000000000000000000, 0.9238795325112859613, 1.000000000000000888 ) ) 
 REPRESENTATION_ITEM ( '' )  );
#1186=CARTESIAN_POINT ( 'NONE',  ( 0.000000000000000000, 0.3155070326520292845, 0.1074305555555577912 ) ) ;
#1188=FACE_OUTER_BOUND ( 'NONE', #12604, .T. ) ;
#1192=AXIS2_PLACEMENT_3D ( 'NONE', #1733, #14549, #6863 ) ;
#1194=CARTESIAN_POINT ( 'NONE',  ( 0.2764156081756484196, -5.077672346800151106E-17, -0.04361111111111028865 ) ) ;
#1197=CARTESIAN_POINT ( 'NONE',  ( 0.1144950937579611444, 0.2764156081756483641, 0.4668055555555604141 ) ) ;
#1202=CARTESIAN_POINT ( 'NONE',  ( -0.4593750000000002554, -0.04467892423992274320, 0.4343810118395207143 ) ) ;
#1214=AXIS2_PLACEMENT_3D ( 'NONE', #20619, #3675, #18551 ) ;
#1217=CARTESIAN_POINT ( 'NONE',  ( 0.2764156081756483641, -0.1144950937579611167, 0.05708333333333497073 ) ) ;
#1220=CARTESIAN_POINT ( 'NONE',  ( -0.3124999999999989453, -0.1294417382415932460, 0.2862500000000032796 ) ) ;
#1221=( BOUNDED_CURVE ( )  B_SPLINE_CURVE ( 2, ( #23758, #12458, #4877, #18049, #19876, #6956, #3170, #14398, #1228, #11308, #17934, #10862, #14274, #23517, #18291, #9475, #8902, #6709, #14518, #16346, #5693, #21822, #21582, #14970, #3412, #1345, #8775, #1588, #9024, #21710, #12579, #3867, #14153, #22392, #20121, #12344, #10502, #21940, #20000, #5233, #12706, #5112, #16797, #16908, #8654, #4994, #78, #3287, #16228, #19760, #2036, #3055, #18741, #10741, #16103, #7523, #13156, #20570, #10620, #9843, #559, #15325, #11557, #2520, #13743, #19341, #20689, #15563, #685, #22755, #4337, #20809, #22871, #9718, #5808, #7875, #4221, #7996, #13629, #21168, #4457, #4098, #21047, #18984, #5926, #6046, #19097, #6166, #2284, #11921, #18862, #10087, #2638, #8109, #11788, #203, #13272, #7644, #22985, #15092, #15448, #22515, #17154, #444, #13513, #20928, #2403, #17274, #13386, #11674, #19213, #9962, #17392, #6290, #3980, #11431, #17029, #2164, #9597, #323, #7762, #15206, #22641, #6650, #1046, #16047, #3000, #23100, #17751, #10449, #23219, #15684, #4697, #6528, #8474 ),
 .UNSPECIFIED., .F., .F. ) 
 B_SPLINE_CURVE_WITH_KNOTS ( ( 3, 2, 2, 2, 2, 2, 2, 2, 2, 2, 2, 2, 2, 2, 2, 2, 2, 2, 2, 2, 2, 2, 2, 2, 2, 2, 2, 2, 2, 2, 2, 2, 2, 2, 2, 2, 2, 2, 2, 2, 2, 2, 2, 2, 2, 2, 2, 2, 2, 2, 2, 2, 2, 2, 2, 2, 2, 2, 2, 2, 2, 2, 2, 2, 2, 2, 2, 3 ),
 ( 0.1232176476950136990, 0.1250000000000000000, 0.1354166666666666574, 0.1458333333333333426, 0.1562500000000000000, 0.1666666666666666574, 0.1770833333333333426, 0.1875000000000000000, 0.1979166666666666574, 0.2083333333333333426, 0.2187500000000000000, 0.2291666666666666574, 0.2395833333333333426, 0.2500000000000000000, 0.2604166666666666852, 0.2708333333333333148, 0.2812500000000000000, 0.2916666666666666852, 0.3020833333333333148, 0.3125000000000000000, 0.3229166666666666852, 0.3333333333333333148, 0.3437500000000000000, 0.3541666666666666852, 0.3645833333333333148, 0.3750000000000000000, 0.3854166666666666852, 0.3958333333333333148, 0.4062500000000000000, 0.4166666666666666852, 0.4270833333333333148, 0.4375000000000000000, 0.4479166666666666852, 0.4583333333333333148, 0.4687500000000000000, 0.4791666666666666852, 0.4895833333333333148, 0.5000000000000000000, 0.5104166666666666297, 0.5208333333333333703, 0.5312500000000000000, 0.5416666666666665186, 0.5520833333333333703, 0.5625000000000000000, 0.5729166666666666297, 0.5833333333333333703, 0.5937500000000000000, 0.6041666666666665186, 0.6145833333333333703, 0.6250000000000000000, 0.6354166666666667407, 0.6458333333333334814, 0.6562500000000000000, 0.6666666666666667407, 0.6770833333333334814, 0.6875000000000000000, 0.6979166666666667407, 0.7083333333333334814, 0.7187500000000000000, 0.7291666666666667407, 0.7395833333333334814, 0.7500000000000000000, 0.7604166666666667407, 0.7708333333333334814, 0.7812500000000000000, 0.7916666666666667407, 0.8020833333333334814, 0.8038656856383126215 ),
 .UNSPECIFIED. ) 
 CURVE ( )  GEOMETRIC_REPRESENTATION_ITEM ( )  RATIONAL_B_SPLINE_CURVE ( ( 0.9784078784059425660, 0.9869753448942262253, 1.000000000000000000, 0.9238795325112867385, 1.000000000000000000, 0.9238795325112867385, 1.000000000000000000, 0.9238795325112867385, 1.000000000000000000, 0.9238795325112867385, 1.000000000000000000, 0.9238795325112867385, 1.000000000000000000, 0.9238795325112867385, 1.000000000000000000, 0.9238795325112867385, 1.000000000000000000, 0.9238795325112867385, 1.000000000000000000, 0.9238795325112867385, 1.000000000000000000, 0.9238795325112867385, 1.000000000000000000, 0.9238795325112867385, 1.000000000000000000, 0.9238795325112867385, 1.000000000000000000, 0.9238795325112867385, 1.000000000000000000, 0.9238795325112867385, 1.000000000000000000, 0.9238795325112867385, 1.000000000000000000, 0.9238795325112867385, 1.000000000000000000, 0.9238795325112867385, 1.000000000000000000, 0.9238795325112867385, 1.000000000000000000, 0.9238795325112867385, 1.000000000000000000, 0.9238795325112867385, 1.000000000000000000, 0.9238795325112867385, 1.000000000000000000, 0.9238795325112867385, 1.000000000000000000, 0.9238795325112867385, 1.000000000000000000, 0.9238795325112867385, 1.000000000000000000, 0.9238795325112867385, 1.000000000000000000, 0.9238795325112867385, 1.000000000000000000, 0.9238795325112867385, 1.000000000000000000, 0.9238795325112867385, 1.000000000000000000, 0.9238795325112867385, 1.000000000000000000, 0.9238795325112867385, 1.000000000000000000, 0.9238795325112867385, 1.000000000000000000, 0.9238795325112867385, 1.000000000000000000, 0.9238795325112867385, 1.000000000000000000, 0.9238795325112867385, 1.000000000000000000, 0.9238795325112867385, 1.000000000000000000, 0.9238795325112867385, 1.000000000000000000, 0.9238795325112867385, 1.000000000000000000, 0.9238795325112867385, 1.000000000000000000, 0.9238795325112867385, 1.000000000000000000, 0.9238795325112867385, 1.000000000000000000, 0.9238795325112867385, 1.000000000000000000, 0.9238795325112867385, 1.000000000000000000, 0.9238795325112867385, 1.000000000000000000, 0.9238795325112867385, 1.000000000000000000, 0.9238795325112867385, 1.000000000000000000, 0.9238795325112867385, 1.000000000000000000, 0.9238795325112867385, 1.000000000000000000, 0.9238795325112867385, 1.000000000000000000, 0.9238795325112867385, 1.000000000000000000, 0.9238795325112867385, 1.000000000000000000, 0.9238795325112867385, 1.000000000000000000, 0.9238795325112867385, 1.000000000000000000, 0.9238795325112867385, 1.000000000000000000, 0.9238795325112867385, 1.000000000000000000, 0.9238795325112867385, 1.000000000000000000, 0.9238795325112867385, 1.000000000000000000, 0.9238795325112867385, 1.000000000000000000, 0.9238795325112867385, 1.000000000000000000, 0.9238795325112867385, 1.000000000000000000, 0.9238795325112867385, 1.000000000000000000, 0.9238795325112867385, 1.000000000000000000, 0.9238795325112867385, 1.000000000000000000, 0.9238795325112867385, 1.000000000000000000, 0.9238795325112867385, 1.000000000000000000, 0.9238795325112867385, 1.000000000000000000, 0.9869753448942777396, 0.9784078784060102896 ) ) 
 REPRESENTATION_ITEM ( '' )  );
#1222=CARTESIAN_POINT ( 'NONE',  ( -0.1144950937579609918, -0.2764156081756484196, 0.2723611111111143845 ) ) ;
#1225=CARTESIAN_POINT ( 'NONE',  ( 0.000000000000000000, 0.3125000000000000000, -0.05749999999999910738 ) ) ;
#1228=CARTESIAN_POINT ( 'NONE',  ( 0.1954553509668047195, 0.1954553509668046085, -0.04361111111111028865 ) ) ;
#1229=CARTESIAN_POINT ( 'NONE',  ( -3.863846776457871776E-17, -0.3155070326520292845, 0.4095138888888931183 ) ) ;
#1231=ORIENTED_EDGE ( 'NONE', *, *, #14841, .T. ) ;
#1232=EDGE_LOOP ( 'NONE', ( #23381, #15668, #18294, #13077 ) ) ;
#1241=VERTEX_POINT ( 'NONE', #23751 ) ;
#1242=CARTESIAN_POINT ( 'NONE',  ( -0.3125000000000000000, 1.913510623667739771E-17, 0.4008333333333378712 ) ) ;
#1255=DIRECTION ( 'NONE',  ( 0.000000000000000000, 0.000000000000000000, -1.000000000000000000 ) ) ;
#1261=CARTESIAN_POINT ( 'NONE',  ( -0.3125000000000000000, 0.000000000000000000, 1.326383476483184332 ) ) ;
#1264=B_SPLINE_CURVE_WITH_KNOTS ( 'NONE', 3,
 ( #2931, #10389, #21230, #4519, #17811, #8535 ),
 .UNSPECIFIED., .F., .F.,
 ( 4, 2, 4 ),
 ( 0.000000000000000000, 0.003274885906227550415, 0.006549771812455102565 ),
 .UNSPECIFIED. ) ;
#1278=EDGE_CURVE ( 'NONE', #5917, #13125, #17965, .T. ) ;
#1283=ORIENTED_EDGE ( 'NONE', *, *, #4380, .F. ) ;
#1290=FACE_OUTER_BOUND ( 'NONE', #16990, .T. ) ;
#1292=CARTESIAN_POINT ( 'NONE',  ( -0.1954553509668046918, -0.1954553509668046640, 0.1508333333333357063 ) ) ;
#1295=CARTESIAN_POINT ( 'NONE',  ( 0.1294417382415921358, -0.3125000000000002220, 0.4112500000000042788 ) ) ;
#1301=EDGE_CURVE ( 'NONE', #18764, #15529, #10420, .T. ) ;
#1303=DIRECTION ( 'NONE',  ( -0.8459207832372989122, 0.4883925919151526629, -0.2142211582677917558 ) ) ;
#1307=CARTESIAN_POINT ( 'NONE',  ( -0.2230971623002954152, -0.2230971623002953874, 0.07270833333333528992 ) ) ;
#1308=DIRECTION ( 'NONE',  ( -0.000000000000000000, -0.000000000000000000, -1.000000000000000000 ) ) ;
#1314=CARTESIAN_POINT ( 'NONE',  ( 0.1144950937579611444, 0.2764156081756483641, 0.07791666666666842433 ) ) ;
#1316=CARTESIAN_POINT ( 'NONE',  ( -0.2764156081756484196, -0.1144950937579609362, 0.3765277777777819579 ) ) ;
#1317=VERTEX_POINT ( 'NONE', #19910 ) ;
#1320=CARTESIAN_POINT ( 'NONE',  ( -0.4584510057643288450, -0.2214217964837244257, 0.4064568219641767066 ) ) ;
#1333=CARTESIAN_POINT ( 'NONE',  ( -0.03651601414465285855, -0.2739930093161157543, -0.06558227484231510251 ) ) ;
#1334=CARTESIAN_POINT ( 'NONE',  ( -3.385114897866767815E-17, -0.2764156081756484196, -0.008888888888887782128 ) ) ;
#1337=CARTESIAN_POINT ( 'NONE',  ( -0.1294417382415922191, 0.3125000000000000000, -0.06097222222222172666 ) ) ;
#1339=CARTESIAN_POINT ( 'NONE',  ( 0.1144950937579609085, -0.2764156081756484751, 0.2237500000000029188 ) ) ;
#1342=CARTESIAN_POINT ( 'NONE',  ( -0.3125000000000000000, 1.913510623667739771E-17, -0.04361111111111011518 ) ) ;
#1345=CARTESIAN_POINT ( 'NONE',  ( 0.1144950937579611444, 0.2764156081756483641, 0.01541666666666797678 ) ) ;
#1346=CARTESIAN_POINT ( 'NONE',  ( -0.1306872919485615459, -0.3155070326520293400, 0.3504861111111148286 ) ) ;
#1355=PRODUCT ( '94902A107_High-Strength Steel Flange Nut_94902A107', '94902A107_High-Strength Steel Flange Nut_94902A107', '', ( #21098 ) ) ;
#1357=EDGE_CURVE ( 'NONE', #11906, #2863, #13132, .T. ) ;
#1362=VECTOR ( 'NONE', #20588, 39.37007874015748143 ) ;
#1365=( BOUNDED_CURVE ( )  B_SPLINE_CURVE ( 2, ( #10894, #5148, #12614 ),
 .UNSPECIFIED., .F., .T. ) 
 B_SPLINE_CURVE_WITH_KNOTS ( ( 3, 3 ),
 ( 0.8125000000000001110, 0.8163014546100183511 ),
 .UNSPECIFIED. ) 
 CURVE ( )  GEOMETRIC_REPRESENTATION_ITEM ( )  RATIONAL_B_SPLINE_CURVE ( ( 0.9999999999999992228, 0.9722206238030344227, 0.9647168388458877697 ) ) 
 REPRESENTATION_ITEM ( '' )  );
#1373=EDGE_LOOP ( 'NONE', ( #10622, #6711, #23887, #607 ) ) ;
#1377=LINE ( 'NONE', #18077, #19336 ) ;
#1390=CARTESIAN_POINT ( 'NONE',  ( -0.4687500000000004441, -0.2598076211353211873, 0.06112444011295848495 ) ) ;
#1398=ADVANCED_FACE ( 'NONE', ( #21379 ), #10296, .F. ) ;
#1399=EDGE_LOOP ( 'NONE', ( #14770, #23212, #11213, #18691 ) ) ;
#1402=CARTESIAN_POINT ( 'NONE',  ( 0.3124999999999993339, -0.1294417382415928852, 0.2584722222222255450 ) ) ;
#1415=CARTESIAN_POINT ( 'NONE',  ( -0.1954553509668046918, -0.1954553509668046640, 0.2063888888888917028 ) ) ;
#1418=CARTESIAN_POINT ( 'NONE',  ( 0.2816345655934815451, 0.09282869753838597637, -0.08510099145262348119 ) ) ;
#1419=B_SPLINE_CURVE_WITH_KNOTS ( 'NONE', 3,
 ( #13511, #19339, #801, #556, #8106, #6407, #2752, #17628, #15799, #23218, #21406, #15561 ),
 .UNSPECIFIED., .F., .F.,
 ( 4, 2, 2, 2, 2, 4 ),
 ( 0.000000000000000000, 0.003341087407395306689, 0.005011631111092960250, 0.006682174814790614245, 0.01002326222218592224, 0.01336434962958123196 ),
 .UNSPECIFIED. ) ;
#1423=EDGE_CURVE ( 'NONE', #15906, #17792, #1377, .T. ) ;
#1430=AXIS2_PLACEMENT_3D ( 'NONE', #14112, #13650, #12062 ) ;
#1431=CARTESIAN_POINT ( 'NONE',  ( -0.3155070326520293400, -0.1306872919485614626, 0.3470138888888930073 ) ) ;
#1434=DIRECTION ( 'NONE',  ( -1.000000000000000000, -1.224646799147353700E-16, 0.000000000000000000 ) ) ;
#1437=CARTESIAN_POINT ( 'NONE',  ( -0.2764156081756484196, -0.1144950937579609362, 0.09875000000000193345 ) ) ;
#1442=CARTESIAN_POINT ( 'NONE',  ( 0.2209708691207961651, 0.2209708691207959985, 0.3175000000000035016 ) ) ;
#1451=CARTESIAN_POINT ( 'NONE',  ( 0.000000000000000000, 3.738758431839877614E-19, -0.1016666666666665164 ) ) ;
#1456=CARTESIAN_POINT ( 'NONE',  ( -0.4679241437345806331, -0.2662683654317171134, 0.05892738626661206403 ) ) ;
#1457=CARTESIAN_POINT ( 'NONE',  ( -0.1954553509668046640, 0.1954553509668046918, 0.3036111111111147176 ) ) ;
#1459=CARTESIAN_POINT ( 'NONE',  ( 0.000000000000000000, 0.3125000000000000000, -0.06444444444444397124 ) ) ;
#1464=CARTESIAN_POINT ( 'NONE',  ( 0.3125000000000009437, 0.1294417382415912476, -0.06791666666666591745 ) ) ;
#1467=DIRECTION ( 'NONE',  ( 0.000000000000000000, 0.000000000000000000, -1.000000000000000000 ) ) ;
#1468=CARTESIAN_POINT ( 'NONE',  ( 0.2764156081756484196, -5.077672346800151106E-17, 0.01194444444444569750 ) ) ;
#1479=ORIENTED_EDGE ( 'NONE', *, *, #20943, .T. ) ;
#1493=AXIS2_PLACEMENT_3D ( 'NONE', #19854, #21805, #844 ) ;
#1496=DIRECTION ( 'NONE',  ( 0.000000000000000000, 0.000000000000000000, -1.000000000000000000 ) ) ;
#1511=CARTESIAN_POINT ( 'NONE',  ( -0.4254231800974379030, 0.3089306822179725964, 0.05347271648849764164 ) ) ;
#1514=( BOUNDED_CURVE ( )  B_SPLINE_CURVE ( 2, ( #24064, #7492, #20301, #14938, #20542, #23943, #12887, #9204, #3837 ),
 .UNSPECIFIED., .F., .F. ) 
 B_SPLINE_CURVE_WITH_KNOTS ( ( 3, 2, 2, 2, 3 ),
 ( 0.3645833333333334259, 0.3750000000000000000, 0.3854166666666667407, 0.3958333333333333703, 0.4062499999999999445 ),
 .UNSPECIFIED. ) 
 CURVE ( )  GEOMETRIC_REPRESENTATION_ITEM ( )  RATIONAL_B_SPLINE_CURVE ( ( 0.9999999999999995559, 0.9238795325112871826, 1.000000000000000000, 0.9238795325112867385, 1.000000000000000000, 0.9238795325112867385, 1.000000000000000000, 0.9238795325112871826, 0.9999999999999995559 ) ) 
 REPRESENTATION_ITEM ( '' )  );
#1518=ORIENTED_EDGE ( 'NONE', *, *, #23286, .T. ) ;
#1532=ORIENTED_EDGE ( 'NONE', *, *, #12511, .F. ) ;
#1533=AXIS2_PLACEMENT_3D ( 'NONE', #5580, #13046, #20462 ) ;
#1535=CARTESIAN_POINT ( 'NONE',  ( 0.2764156081756483641, -0.1144950937579611167, 0.2237500000000029743 ) ) ;
#1536=EDGE_CURVE ( 'NONE', #4238, #3680, #5511, .T. ) ;
#1539=CARTESIAN_POINT ( 'NONE',  ( -0.07411063262681885644, -0.4869405031891911872, 0.4162703459413940599 ) ) ;
#1540=DIRECTION ( 'NONE',  ( 0.000000000000000000, 0.000000000000000000, 1.000000000000000000 ) ) ;
#1547=CARTESIAN_POINT ( 'NONE',  ( 0.3155070326520292845, -5.795770164686806123E-17, 0.2602083333333368165 ) ) ;
#1548=CARTESIAN_POINT ( 'NONE',  ( -1.803446527067423865E-16, 0.5196152422706634688, 0.3779506566538943790 ) ) ;
#1554=CARTESIAN_POINT ( 'NONE',  ( 0.1954553509668047195, 0.1954553509668046085, 0.3522222222222262111 ) ) ;
#1563=CARTESIAN_POINT ( 'NONE',  ( -0.2209708691207961095, 0.2209708691207961373, 0.3313888888888925632 ) ) ;
#1565=AXIS2_PLACEMENT_3D ( 'NONE', #1660, #16543, #23964 ) ;
#1569=CARTESIAN_POINT ( 'NONE',  ( -0.006542161132013071811, 0.5374887588746248834, 0.3892820121258429578 ) ) ;
#1576=CARTESIAN_POINT ( 'NONE',  ( 0.2764156081756483641, 0.1144950937579610056, 0.3418055555555594704 ) ) ;
#1577=AXIS2_PLACEMENT_3D ( 'NONE', #19875, #22301, #2196 ) ;
#1585=CARTESIAN_POINT ( 'NONE',  ( 0.1294417382415924134, 0.3124999999999999445, 0.1612500000000026412 ) ) ;
#1588=CARTESIAN_POINT ( 'NONE',  ( -0.1144950937579609779, 0.2764156081756484196, 0.02236111111111246594 ) ) ;
#1589=CARTESIAN_POINT ( 'NONE',  ( -0.2764156081756484196, 1.692557448933383907E-17, 0.03972222222222369925 ) ) ;
#1602=AXIS2_PLACEMENT_3D ( 'NONE', #22121, #10804, #16647 ) ;
#1627=DIRECTION ( 'NONE',  ( -0.000000000000000000, -0.000000000000000000, -1.000000000000000000 ) ) ;
#1634=EDGE_LOOP ( 'NONE', ( #14741, #21650, #3722 ) ) ;
#1635=VERTEX_POINT ( 'NONE', #3805 ) ;
#1644=CARTESIAN_POINT ( 'NONE',  ( -0.1294417382415922746, -0.3125000000000000000, -0.09569444444444420717 ) ) ;
#1645=CARTESIAN_POINT ( 'NONE',  ( 0.000000000000000000, 0.000000000000000000, -0.1019043464467004889 ) ) ;
#1650=CARTESIAN_POINT ( 'NONE',  ( -0.1954553509668046918, -0.1954553509668046640, 0.2619444444444477549 ) ) ;
#1653=CARTESIAN_POINT ( 'NONE',  ( -0.4687500000000003886, 0.2170121405309672902, 0.07051002209705402313 ) ) ;
#1660=CARTESIAN_POINT ( 'NONE',  ( 0.000000000000000000, 0.000000000000000000, 1.326383476483184332 ) ) ;
#1662=CARTESIAN_POINT ( 'NONE',  ( 0.2236587330425323095, -0.2167494423012602534, 0.4226684177326948677 ) ) ;
#1665=ADVANCED_FACE ( 'NONE', ( #1976 ), #5143, .F. ) ;
#1666=CARTESIAN_POINT ( 'NONE',  ( -0.1306872919485615459, -0.3155070326520293400, 0.3539583333333376491 ) ) ;
#1668=TOROIDAL_SURFACE ( 'NONE', #18418, 0.6209078282299125284, 0.01874999999999999931 ) ;
#1669=CARTESIAN_POINT ( 'NONE',  ( 0.2688280863486493533, -0.3751924628947166940, 0.4334272443489663451 ) ) ;
#1672=CARTESIAN_POINT ( 'NONE',  ( -3.385114897866767815E-17, -0.2764156081756484196, 0.1647222222222247123 ) ) ;
#1675=EDGE_LOOP ( 'NONE', ( #3593, #18958, #2487, #18412, #23544 ) ) ;
#1680=CARTESIAN_POINT ( 'NONE',  ( -0.4805070082343984583, 0.2560807851245828770, 0.04413116910601658921 ) ) ;
#1685=CARTESIAN_POINT ( 'NONE',  ( 0.01298578716746627733, 0.5473886244374734922, 0.04271891838948498055 ) ) ;
#1692=EDGE_CURVE ( 'NONE', #6549, #4536, #5723, .T. ) ;
#1693=DIRECTION ( 'NONE',  ( -1.000000000000000000, 0.000000000000000000, 0.000000000000000000 ) ) ;
#1694=CARTESIAN_POINT ( 'NONE',  ( -0.2764156081756484196, 0.1144950937579609918, 0.3070833333333369830 ) ) ;
#1697=CARTESIAN_POINT ( 'NONE',  ( 0.3308333333333332571, 3.738758431839877614E-19, 0.4425000000000000044 ) ) ;
#1703=CARTESIAN_POINT ( 'NONE',  ( -0.1954553509668046640, 0.1954553509668046918, -0.1338888888888887796 ) ) ;
#1705=ORIENTED_EDGE ( 'NONE', *, *, #18713, .F. ) ;
#1706=EDGE_LOOP ( 'NONE', ( #20611, #10289, #4801, #22116 ) ) ;
#1708=DIRECTION ( 'NONE',  ( 0.000000000000000000, 0.000000000000000000, -1.000000000000000000 ) ) ;
#1725=VERTEX_POINT ( 'NONE', #4038 ) ;
#1726=CARTESIAN_POINT ( 'NONE',  ( -0.4570242136016682832, 0.2774028246161723832, 0.04874733047934379920 ) ) ;
#1727=CARTESIAN_POINT ( 'NONE',  ( -1.889944503261478141E-16, 0.5289902422706634910, 0.3941886329748526263 ) ) ;
#1733=CARTESIAN_POINT ( 'NONE',  ( -0.4500000000000003997, -0.2598076211353319009, 0.3779506566538942125 ) ) ;
#1752=VERTEX_POINT ( 'NONE', #2579 ) ;
#1753=ORIENTED_EDGE ( 'NONE', *, *, #10794, .F. ) ;
#1755=CARTESIAN_POINT ( 'NONE',  ( -0.1484667313405303724, -0.2653928060427109825, 0.4153036484830501807 ) ) ;
#1769=CARTESIAN_POINT ( 'NONE',  ( -0.2764156081756484196, 1.692557448933383907E-17, 0.3105555555555591929 ) ) ;
#1772=CARTESIAN_POINT ( 'NONE',  ( -0.009374999999999756792, -0.5358532185916218271, 0.3779506566538943235 ) ) ;
#1782=CARTESIAN_POINT ( 'NONE',  ( 0.000000000000000000, 3.738758431839877614E-19, 0.4425000000000000044 ) ) ;
#1784=CARTESIAN_POINT ( 'NONE',  ( -0.1306872919485615459, -0.3155070326520293400, 0.2984027777777815138 ) ) ;
#1787=AXIS2_PLACEMENT_3D ( 'NONE', #13488, #19074, #18716 ) ;
#1791=CARTESIAN_POINT ( 'NONE',  ( -0.2764156081756484196, -0.1144950937579609362, 0.2098611111111139405 ) ) ;
#1803=CARTESIAN_POINT ( 'NONE',  ( -0.01172578639831981309, 0.5344959914317445326, 0.04874733047933996199 ) ) ;
#1806=LINE ( 'NONE', #13175, #1362 ) ;
#1808=CARTESIAN_POINT ( 'NONE',  ( -0.2764156081756484196, -0.1144950937579609362, 0.2029166666666694652 ) ) ;
#1809=DIRECTION ( 'NONE',  ( -1.000000000000000000, 0.000000000000000000, 0.000000000000000000 ) ) ;
#1811=CARTESIAN_POINT ( 'NONE',  ( 0.01571427698143865528, -0.5457913482617615664, 0.04342012612512788361 ) ) ;
#1814=AXIS2_PLACEMENT_3D ( 'NONE', #4160, #18796, #5754 ) ;
#1816=CARTESIAN_POINT ( 'NONE',  ( -0.1294417382415922191, 0.3125000000000000000, 0.1681944444444471720 ) ) ;
#1818=CARTESIAN_POINT ( 'NONE',  ( 0.1964672255785170629, 0.4278354717905788474, 0.4172182224143142215 ) ) ;
#1819=CARTESIAN_POINT ( 'NONE',  ( -0.1954553509668046640, 0.1954553509668046918, -0.07833333333333279691 ) ) ;
#1843=ADVANCED_FACE ( 'NONE', ( #15266 ), #11492, .F. ) ;
#1850=CARTESIAN_POINT ( 'NONE',  ( 0.2230971623002953874, -0.2230971623002954429, -0.02798611111111037192 ) ) ;
#1856=AXIS2_PLACEMENT_3D ( 'NONE', #4592, #6657, #12051 ) ;
#1870=ORIENTED_EDGE ( 'NONE', *, *, #19160, .T. ) ;
#1871=LINE ( 'NONE', #7600, #3677 ) ;
#1877=CARTESIAN_POINT ( 'NONE',  ( 0.000000000000000000, 3.738758431839877614E-19, 0.4425000000000000044 ) ) ;
#1881=ORIENTED_EDGE ( 'NONE', *, *, #22586, .T. ) ;
#1884=CARTESIAN_POINT ( 'NONE',  ( -0.4687500000000002220, 0.2630787017013380136, 0.3892820121258430133 ) ) ;
#1889=PLANE ( 'NONE',  #13473 ) ;
#1890=CARTESIAN_POINT ( 'NONE',  ( -0.2764156081756484196, -0.1144950937579609362, 0.3140277777777815138 ) ) ;
#1894=CARTESIAN_POINT ( 'NONE',  ( -0.04549985820534920705, -0.5149965219823262608, 0.3899922761138021055 ) ) ;
#1895=DIRECTION ( 'NONE',  ( 0.5000000000000012212, 0.8660254037844380415, -1.821231995776176268E-15 ) ) ;
#1905=CARTESIAN_POINT ( 'NONE',  ( -3.863846776457871776E-17, -0.3155070326520292845, 0.4129861111111157168 ) ) ;
#1912=CARTESIAN_POINT ( 'NONE',  ( -0.1144950937579609918, -0.2764156081756484196, 0.3279166666666703533 ) ) ;
#1919=DIRECTION ( 'NONE',  ( 0.000000000000000000, 0.000000000000000000, -1.000000000000000000 ) ) ;
#1926=AXIS2_PLACEMENT_3D ( 'NONE', #3996, #16814, #7891 ) ;
#1927=SPHERICAL_SURFACE ( 'NONE', #1926, 0.01874999999999999931 ) ;
#1930=CARTESIAN_POINT ( 'NONE',  ( 0.2764156081756484196, -5.077672346800151106E-17, 0.2827777777777812362 ) ) ;
#1931=LINE ( 'NONE', #16820, #13848 ) ;
#1941=CARTESIAN_POINT ( 'NONE',  ( -0.1294417382415922746, -0.3125000000000000000, 0.07097222222222378252 ) ) ;
#1942=CARTESIAN_POINT ( 'NONE',  ( -0.1144950937579609918, -0.2764156081756484196, -0.06097222222222156013 ) ) ;
#1949=ORIENTED_EDGE ( 'NONE', *, *, #23147, .F. ) ;
#1958=( BOUNDED_CURVE ( )  B_SPLINE_CURVE ( 2, ( #3386, #12680, #1442, #8876, #12926, #16318, #1563, #22161, #11076 ),
 .UNSPECIFIED., .F., .F. ) 
 B_SPLINE_CURVE_WITH_KNOTS ( ( 3, 2, 2, 2, 3 ),
 ( 0.6458333333333333703, 0.6562500000000000000, 0.6666666666666667407, 0.6770833333333334814, 0.6875000000000001110 ),
 .UNSPECIFIED. ) 
 CURVE ( )  GEOMETRIC_REPRESENTATION_ITEM ( )  RATIONAL_B_SPLINE_CURVE ( ( 1.000000000000000000, 0.9238795325112867385, 1.000000000000000000, 0.9238795325112867385, 1.000000000000000000, 0.9238795325112867385, 1.000000000000000000, 0.9238795325112859613, 1.000000000000000888 ) ) 
 REPRESENTATION_ITEM ( '' )  );
#1976=FACE_OUTER_BOUND ( 'NONE', #16823, .T. ) ;
#1979=CARTESIAN_POINT ( 'NONE',  ( 0.2230971623002954429, 0.2230971623002953319, 0.04145833333333462378 ) ) ;
#1980=CARTESIAN_POINT ( 'NONE',  ( 0.4687500000000002220, -0.08766214734763430605, 0.4143508694870877695 ) ) ;
#1981=VECTOR ( 'NONE', #8238, 39.37007874015748854 ) ;
#1982=DIRECTION ( 'NONE',  ( -0.000000000000000000, -0.000000000000000000, -1.000000000000000000 ) ) ;
#1992=CARTESIAN_POINT ( 'NONE',  ( -0.2725578398252894718, 0.3839045351724006960, 0.09139393128959945323 ) ) ;
#1994=CARTESIAN_POINT ( 'NONE',  ( -0.4225900379021583775, 0.2972834052256090320, 0.3902123106865083568 ) ) ;
#2000=CARTESIAN_POINT ( 'NONE',  ( -0.2256529556066708964, -0.2011140187169780102, 0.4134710460457109438 ) ) ;
#2001=EDGE_CURVE ( 'NONE', #20538, #3958, #8171, .T. ) ;
#2007=CARTESIAN_POINT ( 'NONE',  ( 0.3125000000000000000, 3.827021247335477694E-17, 1.326383476483184332 ) ) ;
#2011=( BOUNDED_SURFACE ( )  B_SPLINE_SURFACE ( 3, 2, ( 
 ( #12039, #8471, #2996 ),
 ( #14092, #16043, #23457 ),
 ( #23097, #10323, #15911 ),
 ( #21519, #4810, #8713 ),
 ( #13974, #6767, #14212 ),
 ( #6526, #21646, #4935 ),
 ( #6406, #16162, #4454 ),
 ( #12400, #3114, #10562 ),
 ( #917, #6286, #19338 ),
 ( #2634, #10083, #4580 ),
 ( #15679, #19453, #2751 ),
 ( #10202, #1884, #18350 ) ),
 .UNSPECIFIED., .F., .F., .F. ) 
 B_SPLINE_SURFACE_WITH_KNOTS ( ( 4, 2, 2, 2, 2, 4 ),
 ( 3, 3 ),
 ( 0.02197974498297192159, 0.02532345735115096308, 0.02699531353524048383, 0.02866716971933000457, 0.03201088208750904607, 0.03535459445568808756 ),
 ( 0.000000000000000000, 1.000000000000000000 ),
 .UNSPECIFIED. ) 
 GEOMETRIC_REPRESENTATION_ITEM ( )  RATIONAL_B_SPLINE_SURFACE ( (
 ( 1.000000000000000000, 0.8464669816041905381, 1.000000000000000000),
 ( 1.000000000000000000, 0.8516228929821839655, 1.000000000000000000),
 ( 1.000000000000000000, 0.8565470209672587654, 1.000000000000000000),
 ( 1.000000000000000000, 0.8619809739981544316, 1.000000000000000000),
 ( 1.000000000000000000, 0.8634611050169099800, 1.000000000000000000),
 ( 1.000000000000000000, 0.8654882157366866613, 1.000000000000000000),
 ( 1.000000000000000000, 0.8660234405451954220, 1.000000000000000000),
 ( 1.000000000000000000, 0.8660293137690006082, 1.000000000000000000),
 ( 1.000000000000000000, 0.8638069272854496106, 1.000000000000000000),
 ( 1.000000000000000000, 0.8565545265013099208, 1.000000000000000000),
 ( 1.000000000000000000, 0.8516246201512510661, 1.000000000000000000),
 ( 1.000000000000000000, 0.8464669816041905381, 1.000000000000000000) ) ) 
 REPRESENTATION_ITEM ( '' )  SURFACE ( )  );
#2012=ORIENTED_EDGE ( 'NONE', *, *, #20943, .F. ) ;
#2018=CARTESIAN_POINT ( 'NONE',  ( 0.1689451345729078013, -0.2321341939677896704, 0.3986378631856341004 ) ) ;
#2028=B_SPLINE_CURVE_WITH_KNOTS ( 'NONE', 3,
 ( #6209, #22674, #3452, #20848, #28, #2441, #11713, #12990, #11595, #7803, #9884, #12868 ),
 .UNSPECIFIED., .F., .F.,
 ( 4, 2, 2, 2, 2, 4 ),
 ( 0.000000000000000000, 0.003384026746073582302, 0.006768053492147164604, 0.008460066865183954454, 0.01015208023822074777, 0.01353610698429432574 ),
 .UNSPECIFIED. ) ;
#2031=CARTESIAN_POINT ( 'NONE',  ( 0.2230971623002954429, 0.2230971623002953319, 0.4338194444444492537 ) ) ;
#2036=CARTESIAN_POINT ( 'NONE',  ( -3.385114897866767815E-17, -0.2764156081756484196, 0.1022222222222241989 ) ) ;
#2038=CARTESIAN_POINT ( 'NONE',  ( -3.385114897866767815E-17, -0.2764156081756484196, 0.3869444444444486431 ) ) ;
#2052=CARTESIAN_POINT ( 'NONE',  ( -0.6398935782932173577, 0.000000000000000000, -0.1019043464467004889 ) ) ;
#2053=VERTEX_POINT ( 'NONE', #12222 ) ;
#2056=CIRCLE ( 'NONE', #9460, 0.6396424860381280109 ) ;
#2057=CARTESIAN_POINT ( 'NONE',  ( 0.1144950937579609085, -0.2764156081756484751, 0.4390277777777825130 ) ) ;
#2066=CARTESIAN_POINT ( 'NONE',  ( -0.2764156081756484196, 0.1144950937579609918, 0.2029166666666694097 ) ) ;
#2067=CARTESIAN_POINT ( 'NONE',  ( -0.3385998376278290256, 3.738758431839877614E-19, -0.1012499999999999928 ) ) ;
#2077=EDGE_LOOP ( 'NONE', ( #709, #23821, #14936, #3516 ) ) ;
#2078=CARTESIAN_POINT ( 'NONE',  ( -0.4673607484394256550, -0.2845795129072106744, 0.04287645741408788874 ) ) ;
#2082=CARTESIAN_POINT ( 'NONE',  ( 0.4796770407326167995, -0.08628433980660102365, 0.07157439050488961785 ) ) ;
#2083=DIRECTION ( 'NONE',  ( 0.000000000000000000, 0.000000000000000000, -1.000000000000000000 ) ) ;
#2087=CARTESIAN_POINT ( 'NONE',  ( -0.1954553509668046640, 0.1954553509668046918, 0.08833333333333517889 ) ) ;
#2092=CARTESIAN_POINT ( 'NONE',  ( 0.3125000000000004996, -0.1294417382415918583, 0.1959722222222248234 ) ) ;
#2094=CARTESIAN_POINT ( 'NONE',  ( 0.1306872919485614071, -0.3155070326520293955, -0.08701388888888861306 ) ) ;
#2095=CARTESIAN_POINT ( 'NONE',  ( 0.4687500000000002220, -0.1526433126687117836, 0.4038658439110331955 ) ) ;
#2102=EDGE_CURVE ( 'NONE', #18764, #6009, #9115, .T. ) ;
#2107=CARTESIAN_POINT ( 'NONE',  ( 0.1294417382415921358, -0.3125000000000002220, 0.2445833333333362336 ) ) ;
#2112=CARTESIAN_POINT ( 'NONE',  ( -0.09493784612928136968, -0.2937490000082879082, -0.09741978624864720826 ) ) ;
#2121=EDGE_LOOP ( 'NONE', ( #8010, #18293, #8192, #17141, #8307, #11387, #13181, #23760, #1870, #434 ) ) ;
#2124=DIRECTION ( 'NONE',  ( 0.000000000000000000, 0.000000000000000000, 1.000000000000000000 ) ) ;
#2129=EDGE_CURVE ( 'NONE', #15581, #20003, #1264, .T. ) ;
#2131=ORIENTED_EDGE ( 'NONE', *, *, #21045, .F. ) ;
#2150=ORIENTED_EDGE ( 'NONE', *, *, #16482, .T. ) ;
#2153=ORIENTED_EDGE ( 'NONE', *, *, #17718, .T. ) ;
#2155=CARTESIAN_POINT ( 'NONE',  ( 0.2230971623002954429, 0.2230971623002953319, 0.3782638888888932849 ) ) ;
#2157=( BOUNDED_SURFACE ( )  B_SPLINE_SURFACE ( 3, 2, ( 
 ( #20225, #1803, #12560 ),
 ( #9120, #23622, #20343 ),
 ( #3515, #18390, #23736 ),
 ( #7060, #14373, #10965 ),
 ( #1685, #16568, #3631 ),
 ( #14499, #23990, #14751 ) ),
 .UNSPECIFIED., .F., .F., .T. ) 
 B_SPLINE_SURFACE_WITH_KNOTS ( ( 4, 2, 4 ),
 ( 3, 3 ),
 ( 0.001790663949227914217, 0.002289857484343688597, 0.002789051019459462544 ),
 ( 0.000000000000000000, 1.000000000000000000 ),
 .UNSPECIFIED. ) 
 GEOMETRIC_REPRESENTATION_ITEM ( )  RATIONAL_B_SPLINE_SURFACE ( (
 ( 1.000000000000000000, 0.8285407536241355952, 1.000000000000000000),
 ( 1.000000000000000000, 0.8382697314792758592, 1.000000000000000000),
 ( 1.000000000000000000, 0.8433836253083885071, 1.000000000000000000),
 ( 1.000000000000000000, 0.8433992480894890731, 1.000000000000000000),
 ( 1.000000000000000000, 0.8382827608169696187, 1.000000000000000000),
 ( 1.000000000000000000, 0.8285407536241035098, 1.000000000000000000) ) ) 
 REPRESENTATION_ITEM ( '' )  SURFACE ( )  );
#2164=CARTESIAN_POINT ( 'NONE',  ( 0.2764156081756483641, -0.1144950937579611028, 0.3348611111111149952 ) ) ;
#2166=CARTESIAN_POINT ( 'NONE',  ( 0.1144950937579609085, -0.2764156081756484751, -0.06097222222222153931 ) ) ;
#2168=FACE_OUTER_BOUND ( 'NONE', #14401, .T. ) ;
#2169=CONICAL_SURFACE ( 'NONE', #10726, 0.3125000000000000000, 0.7853981633974497223 ) ;
#2171=CARTESIAN_POINT ( 'NONE',  ( -0.2784250239278213690, 0.03789337644375285336, -0.06999960198848567683 ) ) ;
#2187=CARTESIAN_POINT ( 'NONE',  ( -0.2230971623002954152, -0.2230971623002953874, -0.1495138888888886963 ) ) ;
#2188=CARTESIAN_POINT ( 'NONE',  ( 0.000000000000000000, 0.000000000000000000, 1.326383476483184332 ) ) ;
#2190=ORIENTED_EDGE ( 'NONE', *, *, #21670, .T. ) ;
#2194=CARTESIAN_POINT ( 'NONE',  ( 0.1954553509668047195, 0.1954553509668046085, -0.09222222222222178911 ) ) ;
#2196=DIRECTION ( 'NONE',  ( -1.000000000000000000, 0.000000000000000000, 0.000000000000000000 ) ) ;
#2197=CARTESIAN_POINT ( 'NONE',  ( 0.1144950937579609085, -0.2764156081756484751, 0.1126388888888909395 ) ) ;
#2200=CARTESIAN_POINT ( 'NONE',  ( 0.006454613307746654219, 0.5491961284534641052, 0.04193467568257214922 ) ) ;
#2215=CARTESIAN_POINT ( 'NONE',  ( 0.4795759075923629045, -0.04315724733464136598, 0.07439896364133659346 ) ) ;
#2220=CARTESIAN_POINT ( 'NONE',  ( 0.2764156081756484196, -5.077672346800151106E-17, 0.01194444444444569750 ) ) ;
#2227=CARTESIAN_POINT ( 'NONE',  ( -0.1306872919485615459, -0.3155070326520293400, 0.1838194444444468667 ) ) ;
#2228=CARTESIAN_POINT ( 'NONE',  ( -0.08339729271158345669, -0.4931164279685558149, 0.07808165802386347887 ) ) ;
#2229=DIRECTION ( 'NONE',  ( 0.4999999999999997224, 0.8660254037844388186, -0.000000000000000000 ) ) ;
#2237=CARTESIAN_POINT ( 'NONE',  ( 0.2209708691207961095, -0.2209708691207961651, 0.3105555555555593039 ) ) ;
#2239=CARTESIAN_POINT ( 'NONE',  ( -0.04810232026111291304, 0.5134939898139645464, 0.05816208736419732628 ) ) ;
#2245=CARTESIAN_POINT ( 'NONE',  ( 0.2759399609360094763, 0.05657080772233213928, 0.3928742422042607596 ) ) ;
#2250=VECTOR ( 'NONE', #8689, 39.37007874015748143 ) ;
#2252=CARTESIAN_POINT ( 'NONE',  ( 0.4224645524279259101, 0.2973558542979368169, 0.3902541392329166858 ) ) ;
#2259=FACE_OUTER_BOUND ( 'NONE', #13993, .T. ) ;
#2260=CARTESIAN_POINT ( 'NONE',  ( 0.1954553509668047195, 0.1954553509668046085, 0.4563888888888936735 ) ) ;
#2262=CARTESIAN_POINT ( 'NONE',  ( -0.1568404389086238138, -0.4507140077415615065, 0.4133480672484174390 ) ) ;
#2269=CIRCLE ( 'NONE', #3021, 0.3253415854805813412 ) ;
#2275=CARTESIAN_POINT ( 'NONE',  ( -0.2230971623002953874, 0.2230971623002954152, 0.4477083333333382598 ) ) ;
#2282=CARTESIAN_POINT ( 'NONE',  ( 0.4206390790005973823, -0.2984097918724726850, 0.05816431335568269384 ) ) ;
#2283=ORIENTED_EDGE ( 'NONE', *, *, #4095, .T. ) ;
#2284=CARTESIAN_POINT ( 'NONE',  ( 0.1954553509668047195, 0.1954553509668046085, 0.2341666666666697150 ) ) ;
#2286=CARTESIAN_POINT ( 'NONE',  ( -0.1954553509668046640, 0.1954553509668046918, 0.4772222222222271548 ) ) ;
#2290=CARTESIAN_POINT ( 'NONE',  ( -0.2759399609360070338, 0.05657080772233105681, -0.07037424220425755883 ) ) ;
#2304=CARTESIAN_POINT ( 'NONE',  ( 0.2230971623002953874, -0.2230971623002954429, -0.1356249999999996902 ) ) ;
#2310=CARTESIAN_POINT ( 'NONE',  ( -0.2764156081756484196, -0.1144950937579609362, -0.1234722222222220528 ) ) ;
#2313=CARTESIAN_POINT ( 'NONE',  ( 0.2764156081756483641, -0.1144950937579611167, 0.1751388888888914530 ) ) ;
#2315=CARTESIAN_POINT ( 'NONE',  ( -0.01848103877824625041, 0.5441716683897389606, 0.04413116910601661003 ) ) ;
#2328=CARTESIAN_POINT ( 'NONE',  ( 0.1583529533612939577, 0.4498407571151590290, 0.08855978515308939036 ) ) ;
#2335=CARTESIAN_POINT ( 'NONE',  ( 0.1954553509668047195, 0.1954553509668046085, -0.09916666666666627827 ) ) ;
#2341=CARTESIAN_POINT ( 'NONE',  ( 0.2764156081756483641, -0.1144950937579611028, 0.06402777777777945989 ) ) ;
#2344=CARTESIAN_POINT ( 'NONE',  ( 0.000000000000000000, 0.000000000000000000, 1.326383476483184332 ) ) ;
#2347=CARTESIAN_POINT ( 'NONE',  ( -0.1306872919485615459, -0.3155070326520293400, 0.1282638888888908979 ) ) ;
#2357=CARTESIAN_POINT ( 'NONE',  ( 0.1294417382415921358, -0.3125000000000002220, 0.3070833333333370940 ) ) ;
#2358=AXIS2_PLACEMENT_3D ( 'NONE', #17220, #1982, #22460 ) ;
#2359=CARTESIAN_POINT ( 'NONE',  ( -0.09134320533038761680, 0.5015400784327411765, 0.06108448616841834905 ) ) ;
#2367=DIRECTION ( 'NONE',  ( 0.000000000000000000, 0.000000000000000000, -1.000000000000000000 ) ) ;
#2371=ORIENTED_EDGE ( 'NONE', *, *, #6180, .T. ) ;
#2373=CONICAL_SURFACE ( 'NONE', #20279, 0.4453125000000000000, 1.047197551196600074 ) ;
#2376=CARTESIAN_POINT ( 'NONE',  ( 0.2091198842963235827, 0.4097039017751566425, 0.4343513344076809224 ) ) ;
#2382=CARTESIAN_POINT ( 'NONE',  ( 0.3125000000000000000, -5.740531871003217465E-17, -0.02277777777777697382 ) ) ;
#2383=CARTESIAN_POINT ( 'NONE',  ( -3.385114897866767815E-17, -0.2764156081756484196, 0.4355555555555601921 ) ) ;
#2385=CARTESIAN_POINT ( 'NONE',  ( -0.2139474665362521011, -0.4177432499681407729, 0.4289390872834994428 ) ) ;
#2392=ORIENTED_EDGE ( 'NONE', *, *, #22273, .F. ) ;
#2401=CARTESIAN_POINT ( 'NONE',  ( -3.827021247335479543E-17, -0.3125000000000000000, -0.08527777777777710566 ) ) ;
#2402=CARTESIAN_POINT ( 'NONE',  ( 0.3096487991955518826, -0.3624900597954727743, 0.07655254331175391502 ) ) ;
#2403=CARTESIAN_POINT ( 'NONE',  ( 0.000000000000000000, 0.2764156081756484196, 0.2966666666666702423 ) ) ;
#2405=CARTESIAN_POINT ( 'NONE',  ( -0.1144950937579609779, 0.2764156081756484196, -0.1443055555555555203 ) ) ;
#2411=CARTESIAN_POINT ( 'NONE',  ( -0.3124999999999989453, -0.1294417382415932460, 0.3418055555555593039 ) ) ;
#2416=EDGE_LOOP ( 'NONE', ( #16813, #7601, #6395 ) ) ;
#2423=CARTESIAN_POINT ( 'NONE',  ( 0.4683396222371035145, -0.2655382811872516458, 0.04698599556840714342 ) ) ;
#2424=CARTESIAN_POINT ( 'NONE',  ( -0.2764156081756484196, 1.692557448933383907E-17, 0.3661111111111152172 ) ) ;
#2432=CARTESIAN_POINT ( 'NONE',  ( 0.1144950937579611444, 0.2764156081756483641, 0.1334722222222244348 ) ) ;
#2441=CARTESIAN_POINT ( 'NONE',  ( -0.2481776206062810408, 0.3871563449089069908, 0.4344098397133764333 ) ) ;
#2451=CARTESIAN_POINT ( 'NONE',  ( 0.3103034095256952396, -0.3621121203451557746, 0.4135550951626320026 ) ) ;
#2454=CARTESIAN_POINT ( 'NONE',  ( -0.3065849364905382513, 4.708020935245015622E-15, -0.09575160315720471216 ) ) ;
#2458=CARTESIAN_POINT ( 'NONE',  ( -0.2084225359521647558, -0.1824881659814446000, -0.06500058086764819165 ) ) ;
#2464=CARTESIAN_POINT ( 'NONE',  ( -3.863846776457871776E-17, -0.3155070326520292845, 0.07618055555555713898 ) ) ;
#2475=ORIENTED_EDGE ( 'NONE', *, *, #2888, .F. ) ;
#2477=CARTESIAN_POINT ( 'NONE',  ( -0.1294417382415922746, -0.3125000000000000000, 0.3001388888888926743 ) ) ;
#2481=EDGE_CURVE ( 'NONE', #1752, #8247, #12905, .T. ) ;
#2487=ORIENTED_EDGE ( 'NONE', *, *, #19919, .F. ) ;
#2490=ORIENTED_EDGE ( 'NONE', *, *, #15292, .T. ) ;
#2493=CARTESIAN_POINT ( 'NONE',  ( 0.1948874010148183844, 0.4287475839277025136, 0.4171140917644197144 ) ) ;
#2494=DIRECTION ( 'NONE',  ( -1.000000000000000000, 0.000000000000000000, 0.000000000000000000 ) ) ;
#2499=CARTESIAN_POINT ( 'NONE',  ( -0.1144950937579609779, 0.2764156081756484196, 0.4668055555555604141 ) ) ;
#2508=ORIENTED_EDGE ( 'NONE', *, *, #3258, .T. ) ;
#2514=CARTESIAN_POINT ( 'NONE',  ( 0.4805453480892175055, 0.2624482906435715024, 0.04271891838947997760 ) ) ;
#2518=CARTESIAN_POINT ( 'NONE',  ( 0.000000000000000000, 0.3125000000000000000, 0.2758333333333368720 ) ) ;
#2520=CARTESIAN_POINT ( 'NONE',  ( -0.2764156081756484196, -0.1144950937579609362, 0.1473611111111134409 ) ) ;
#2522=CARTESIAN_POINT ( 'NONE',  ( 0.1144950937579611444, 0.2764156081756483641, -0.09569444444444404063 ) ) ;
#2536=CARTESIAN_POINT ( 'NONE',  ( 0.08367912913462044466, 0.4929537096338479363, 0.07813342133392807420 ) ) ;
#2540=CARTESIAN_POINT ( 'NONE',  ( -0.1954553509668046640, 0.1954553509668046918, 0.3591666666666706864 ) ) ;
#2541=AXIS2_PLACEMENT_3D ( 'NONE', #3708, #11515, #15740 ) ;
#2543=ORIENTED_EDGE ( 'NONE', *, *, #2129, .F. ) ;
#2549=CARTESIAN_POINT ( 'NONE',  ( -3.385114897866767815E-17, -0.2764156081756484196, 0.2758333333333366499 ) ) ;
#2560=CARTESIAN_POINT ( 'NONE',  ( -0.1953806383670292079, 0.4284628132096496289, 0.4289620446068652670 ) ) ;
#2563=CARTESIAN_POINT ( 'NONE',  ( -0.3125000000000010547, -0.1294417382415911644, 0.1265277777777800983 ) ) ;
#2566=CARTESIAN_POINT ( 'NONE',  ( 0.04626190099493247138, 0.5145565563726263170, 0.07046568677123667135 ) ) ;
#2568=CARTESIAN_POINT ( 'NONE',  ( -0.4687500000000003886, 0.1725697052561470934, 0.06591547745735594488 ) ) ;
#2572=EDGE_CURVE ( 'NONE', #20446, #3858, #3522, .T. ) ;
#2574=CARTESIAN_POINT ( 'NONE',  ( -3.385114897866767815E-17, -0.2764156081756484196, -0.001944444444443294917 ) ) ;
#2575=CARTESIAN_POINT ( 'NONE',  ( -3.827021247335479543E-17, -0.3125000000000000000, 0.3591666666666709085 ) ) ;
#2576=ORIENTED_EDGE ( 'NONE', *, *, #19990, .T. ) ;
#2579=CARTESIAN_POINT ( 'NONE',  ( 0.4620259694561523744, -0.2880908832651558615, 0.04413116910601658921 ) ) ;
#2580=CARTESIAN_POINT ( 'NONE',  ( -0.1963547988595202021, 0.4279003813870556616, 0.09139143879391155301 ) ) ;
#2581=AXIS2_PLACEMENT_3D ( 'NONE', #9693, #15302, #20664 ) ;
#2583=CARTESIAN_POINT ( 'NONE',  ( -0.3155070326520293400, 0.1306872919485614903, 0.1699305555555579161 ) ) ;
#2585=VERTEX_POINT ( 'NONE', #14003 ) ;
#2596=CARTESIAN_POINT ( 'NONE',  ( -0.08337866210075467466, 0.4931271843567329172, 0.07807775719020894345 ) ) ;
#2598=CARTESIAN_POINT ( 'NONE',  ( 0.1688124736067298515, -0.2196335248264128515, 0.3880822748423150559 ) ) ;
#2599=AXIS2_PLACEMENT_3D ( 'NONE', #3199, #10645, #4783 ) ;
#2609=ORIENTED_EDGE ( 'NONE', *, *, #8677, .T. ) ;
#2611=CARTESIAN_POINT ( 'NONE',  ( 0.3852690508742848685, 0.3188306871325746195, 0.4003899297375634325 ) ) ;
#2617=CARTESIAN_POINT ( 'NONE',  ( -0.4253970711649990855, -0.3089455473570085764, 0.05347937985141010958 ) ) ;
#2619=CARTESIAN_POINT ( 'NONE',  ( -0.4251436100157495734, -0.2958090996784975002, 0.4013701042765217553 ) ) ;
#2624=ORIENTED_EDGE ( 'NONE', *, *, #18763, .T. ) ;
#2634=CARTESIAN_POINT ( 'NONE',  ( -0.4587627190187693049, 0.1786642205917136905, 0.4164153136193288751 ) ) ;
#2635=DIRECTION ( 'NONE',  ( -0.4999999999999991673, -0.8660254037844391517, 0.000000000000000000 ) ) ;
#2637=CARTESIAN_POINT ( 'NONE',  ( 0.4224880990050952079, -0.2973422596752695601, 0.07046568677120454427 ) ) ;
#2638=CARTESIAN_POINT ( 'NONE',  ( -0.1954553509668046640, 0.1954553509668046918, 0.2480555555555586933 ) ) ;
#2640=CARTESIAN_POINT ( 'NONE',  ( 0.1954553509668046640, -0.1954553509668047195, 0.1091666666666687158 ) ) ;
#2647=FACE_OUTER_BOUND ( 'NONE', #2077, .T. ) ;
#2655=CARTESIAN_POINT ( 'NONE',  ( -0.3125000000000000000, 1.913510623667739771E-17, 0.06750000000000189182 ) ) ;
#2658=CARTESIAN_POINT ( 'NONE',  ( -3.863846776457871776E-17, -0.3155070326520292845, 0.07965277777777976520 ) ) ;
#2664=CARTESIAN_POINT ( 'NONE',  ( -0.1144950937579609918, -0.2764156081756484196, -0.1165277777777775636 ) ) ;
#2667=CARTESIAN_POINT ( 'NONE',  ( -0.1144950937579609779, 0.2764156081756484196, 0.3070833333333369275 ) ) ;
#2676=CARTESIAN_POINT ( 'NONE',  ( -0.2688280863486467442, 0.3751924628946938234, 0.4334272443489776694 ) ) ;
#2683=CARTESIAN_POINT ( 'NONE',  ( 0.3886629897678103296, -0.3298823763122805675, 0.06108558933789662304 ) ) ;
#2685=CARTESIAN_POINT ( 'NONE',  ( -0.4687500000000003886, 0.2172233302825360146, 0.07046370559340160711 ) ) ;
#2687=CARTESIAN_POINT ( 'NONE',  ( 0.2764156081756484196, -5.077672346800151106E-17, -0.05055555555555477781 ) ) ;
#2691=CARTESIAN_POINT ( 'NONE',  ( 0.2764156081756483641, -0.1144950937579611028, 0.1195833333333354287 ) ) ;
#2697=CARTESIAN_POINT ( 'NONE',  ( 0.1294417382415924134, 0.3124999999999999445, -0.01236111111111022273 ) ) ;
#2698=CARTESIAN_POINT ( 'NONE',  ( 0.1306872919485616846, 0.3155070326520292290, 0.2115972222222248789 ) ) ;
#2702=ADVANCED_FACE ( 'NONE', ( #17900 ), #22080, .T. ) ;
#2707=CARTESIAN_POINT ( 'NONE',  ( 0.009375000000000067307, -0.5358532185916218271, 0.06112444011295370405 ) ) ;
#2736=FACE_OUTER_BOUND ( 'NONE', #9515, .T. ) ;
#2747=CARTESIAN_POINT ( 'NONE',  ( -0.03762146087705336983, -0.5076544266709852593, 0.4065068718547069637 ) ) ;
#2751=CARTESIAN_POINT ( 'NONE',  ( -0.4687500000000003886, 0.2177858881633971400, 0.3900812861337792370 ) ) ;
#2752=CARTESIAN_POINT ( 'NONE',  ( -0.4687500000000004996, -0.02206989609517173018, 0.4181409822411251698 ) ) ;
#2755=CARTESIAN_POINT ( 'NONE',  ( -0.2764156081756484196, -0.1144950937579609362, 0.09180555555555744429 ) ) ;
#2759=CARTESIAN_POINT ( 'NONE',  ( 0.2705345477997488368, 0.1189582700827290229, -0.08454861231499928576 ) ) ;
#2760=LINE ( 'NONE', #8356, #1981 ) ;
#2770=CARTESIAN_POINT ( 'NONE',  ( -0.2230971623002953874, 0.2230971623002954152, -0.05229166666666570235 ) ) ;
#2776=CARTESIAN_POINT ( 'NONE',  ( 0.1954553509668047195, 0.1954553509668046085, 0.1300000000000021694 ) ) ;
#2779=CARTESIAN_POINT ( 'NONE',  ( 0.2764156081756484196, -5.077672346800151106E-17, 0.4563888888888936735 ) ) ;
#2788=DIRECTION ( 'NONE',  ( 1.000000000000000000, 0.000000000000000000, 0.000000000000000000 ) ) ;
#2789=CARTESIAN_POINT ( 'NONE',  ( -0.2732891327808207316, 0.3834823229876400674, 0.4280258002685754515 ) ) ;
#2792=ORIENTED_EDGE ( 'NONE', *, *, #8595, .T. ) ;
#2793=CARTESIAN_POINT ( 'NONE',  ( -0.2209708691207961095, 0.2209708691207961373, 0.1161111111111133992 ) ) ;
#2798=CARTESIAN_POINT ( 'NONE',  ( 0.2111984196243031631, 0.4085062965502690990, 0.4344098397133764333 ) ) ;
#2799=CARTESIAN_POINT ( 'NONE',  ( -3.385114897866767815E-17, -0.2764156081756484196, -0.06444444444444379083 ) ) ;
#2802=CARTESIAN_POINT ( 'NONE',  ( -0.2209708691207961095, 0.2209708691207961373, -0.05749999999999948208 ) ) ;
#2804=CARTESIAN_POINT ( 'NONE',  ( 0.2764156081756483641, 0.1144950937579610195, 0.1820833333333359005 ) ) ;
#2807=CARTESIAN_POINT ( 'NONE',  ( 0.4687500000000002776, -0.04363837962608485554, 0.07944711129966139374 ) ) ;
#2811=CARTESIAN_POINT ( 'NONE',  ( -0.3155070326520292845, 1.931923388228935888E-17, 0.3400694444444480879 ) ) ;
#2831=CARTESIAN_POINT ( 'NONE',  ( -0.4687500000000004441, 0.2570931668155772565, 0.04874733047933996199 ) ) ;
#2842=CYLINDRICAL_SURFACE ( 'NONE', #21055, 0.3125000000000000000 ) ;
#2856=CARTESIAN_POINT ( 'NONE',  ( 0.4692112248683192322, 0.2611554184491500785, 0.04763613967037012842 ) ) ;
#2861=FACE_OUTER_BOUND ( 'NONE', #4905, .T. ) ;
#2863=VERTEX_POINT ( 'NONE', #4787 ) ;
#2867=CARTESIAN_POINT ( 'NONE',  ( -0.1144950937579609779, 0.2764156081756484196, -0.03319444444444354797 ) ) ;
#2871=CARTESIAN_POINT ( 'NONE',  ( -0.01197057051269659507, 0.2890469299669656822, -0.07784597376562178705 ) ) ;
#2880=EDGE_LOOP ( 'NONE', ( #14907, #2508, #5004, #8927 ) ) ;
#2884=CARTESIAN_POINT ( 'NONE',  ( 0.2230971623002953874, -0.2230971623002954429, -0.02451388888888771794 ) ) ;
#2887=EDGE_CURVE ( 'NONE', #2585, #6063, #18083, .T. ) ;
#2888=EDGE_CURVE ( 'NONE', #549, #22264, #8449, .T. ) ;
#2892=CARTESIAN_POINT ( 'NONE',  ( -3.385114897866767815E-17, -0.2764156081756484196, -0.05749999999999930167 ) ) ;
#2893=DIRECTION ( 'NONE',  ( -1.000000000000000000, 0.000000000000000000, 0.000000000000000000 ) ) ;
#2894=CARTESIAN_POINT ( 'NONE',  ( 0.2209708691207961095, -0.2209708691207961651, 0.08138888888889052320 ) ) ;
#2895=CARTESIAN_POINT ( 'NONE',  ( -0.1144950937579609918, -0.2764156081756484196, 0.3834722222222265442 ) ) ;
#2906=CARTESIAN_POINT ( 'NONE',  ( -0.4500000000000003997, -0.2598076211353319009, 0.3779506566538942125 ) ) ;
#2914=CARTESIAN_POINT ( 'NONE',  ( 0.1567390680359450617, -0.2674066423994601593, 0.4211701672829530896 ) ) ;
#2917=CIRCLE ( 'NONE', #12691, 1.200750000000023521 ) ;
#2919=CARTESIAN_POINT ( 'NONE',  ( -0.4805070082343984583, 0.2560807851245828215, 0.04413116910601664472 ) ) ;
#2920=CARTESIAN_POINT ( 'NONE',  ( -0.2764156081756484196, 0.1144950937579609918, -0.02624999999999903799 ) ) ;
#2925=CARTESIAN_POINT ( 'NONE',  ( -0.1144950937579609918, -0.2764156081756484196, 0.1612500000000024192 ) ) ;
#2928=B_SPLINE_CURVE_WITH_KNOTS ( 'NONE', 3,
 ( #6318, #17778, #19601, #15594, #9996, #21319 ),
 .UNSPECIFIED., .F., .F.,
 ( 4, 2, 4 ),
 ( 0.000000000000000000, 0.0002551367231383054666, 0.0005102734462766109333 ),
 .UNSPECIFIED. ) ;
#2930=CARTESIAN_POINT ( 'NONE',  ( -0.2365780681204351643, 0.1757304751630116846, 0.4057683715178541650 ) ) ;
#2931=CARTESIAN_POINT ( 'NONE',  ( 0.4805070082343983473, 0.2560807851245830991, 0.04413116910601658921 ) ) ;
#2934=CARTESIAN_POINT ( 'NONE',  ( -0.2230971623002954152, -0.2230971623002953874, 0.3470138888888926187 ) ) ;
#2943=EDGE_LOOP ( 'NONE', ( #20914, #21292, #523, #8389 ) ) ;
#2952=ORIENTED_EDGE ( 'NONE', *, *, #11723, .T. ) ;
#2968=EDGE_CURVE ( 'NONE', #20369, #23426, #6909, .T. ) ;
#2969=VECTOR ( 'NONE', #1708, 39.37007874015748143 ) ;
#2978=AXIS2_PLACEMENT_3D ( 'NONE', #6692, #10371, #20201 ) ;
#2990=CARTESIAN_POINT ( 'NONE',  ( 0.4645897358368414887, 0.2720347660510105681, 0.05893128447555067567 ) ) ;
#2996=CARTESIAN_POINT ( 'NONE',  ( -0.4687500000000003886, -0.2598076211353318454, 0.3779506566538943235 ) ) ;
#2998=ORIENTED_EDGE ( 'NONE', *, *, #843, .F. ) ;
#3000=CARTESIAN_POINT ( 'NONE',  ( -0.2764156081756484196, 1.692557448933383907E-17, 0.3661111111111152172 ) ) ;
#3002=CARTESIAN_POINT ( 'NONE',  ( 0.000000000000000000, 0.2764156081756484196, 0.01888888888889020401 ) ) ;
#3015=CARTESIAN_POINT ( 'NONE',  ( -0.2209708691207961095, 0.2209708691207961373, 0.2272222222222253785 ) ) ;
#3017=CARTESIAN_POINT ( 'NONE',  ( 0.1306872919485616846, 0.3155070326520292290, -0.007152777777776447334 ) ) ;
#3021=AXIS2_PLACEMENT_3D ( 'NONE', #4971, #21447, #2788 ) ;
#3023=CARTESIAN_POINT ( 'NONE',  ( 0.1954553509668047195, 0.1954553509668046085, -0.03666666666666580643 ) ) ;
#3024=CARTESIAN_POINT ( 'NONE',  ( 0.4805263112511645174, -0.2592867110628498395, 0.04342012612512791137 ) ) ;
#3026=CARTESIAN_POINT ( 'NONE',  ( -0.2764156081756484196, -0.1144950937579609362, 0.4320833333333378157 ) ) ;
#3030=DIRECTION ( 'NONE',  ( 6.827562483166858637E-16, 0.9767851838303066581, -0.2142211582677916726 ) ) ;
#3036=CARTESIAN_POINT ( 'NONE',  ( -0.4622078388679876082, 0.2744100571732864813, 0.3892820121258430133 ) ) ;
#3045=CARTESIAN_POINT ( 'NONE',  ( 0.000000000000000000, 0.2764156081756484196, -0.09222222222222178911 ) ) ;
#3049=CARTESIAN_POINT ( 'NONE',  ( -0.1144950937579609779, 0.2764156081756484196, 0.1404166666666689378 ) ) ;
#3052=CARTESIAN_POINT ( 'NONE',  ( -0.2245903949464531368, 0.1902879574984994715, 0.4054134354953847219 ) ) ;
#3055=CARTESIAN_POINT ( 'NONE',  ( 0.1144950937579609085, -0.2764156081756484751, 0.1056944444444464365 ) ) ;
#3056=CARTESIAN_POINT ( 'NONE',  ( -0.1306872919485615459, -0.3155070326520293400, 0.4060416666666709640 ) ) ;
#3060=CARTESIAN_POINT ( 'NONE',  ( 0.4687499999998496758, 0.2209570500825255579, 0.4011790492569353161 ) ) ;
#3070=EDGE_CURVE ( 'NONE', #9832, #15369, #6743, .T. ) ;
#3078=AXIS2_PLACEMENT_3D ( 'NONE', #15453, #11793, #16912 ) ;
#3092=DIRECTION ( 'NONE',  ( -1.000000000000000000, 0.000000000000000000, 0.000000000000000000 ) ) ;
#3098=CARTESIAN_POINT ( 'NONE',  ( -0.4645897358368417107, -0.2720347660510102905, 0.05893128447555207733 ) ) ;
#3110=ORIENTED_EDGE ( 'NONE', *, *, #8595, .F. ) ;
#3112=CONICAL_SURFACE ( 'NONE', #16747, 0.3125000000000000000, 0.7853981633974497223 ) ;
#3114=CARTESIAN_POINT ( 'NONE',  ( -0.4687500000000386913, 0.04471557274272623672, 0.4289752932571493926 ) ) ;
#3119=CARTESIAN_POINT ( 'NONE',  ( 0.1954553509668047195, 0.1954553509668046085, 0.1230555555555576941 ) ) ;
#3121=CARTESIAN_POINT ( 'NONE',  ( -0.1038682246014046850, 0.2678606782618252469, -0.07599903378259419140 ) ) ;
#3127=AXIS2_PLACEMENT_3D ( 'NONE', #838, #17305, #13306 ) ;
#3132=CARTESIAN_POINT ( 'NONE',  ( -0.2230971623002953874, 0.2230971623002954152, 0.003263888888890301588 ) ) ;
#3140=CARTESIAN_POINT ( 'NONE',  ( -0.2764156081756484196, 1.692557448933383907E-17, -0.01583333333333230425 ) ) ;
#3141=CARTESIAN_POINT ( 'NONE',  ( -0.1954553509668046918, -0.1954553509668046640, 0.4355555555555601921 ) ) ;
#3142=ORIENTED_EDGE ( 'NONE', *, *, #19990, .F. ) ;
#3153=CARTESIAN_POINT ( 'NONE',  ( 0.2209708691207961095, -0.2209708691207961651, -0.02277777777777661300 ) ) ;
#3158=CARTESIAN_POINT ( 'NONE',  ( -0.07226797383944986997, -0.2674160455368901346, -0.06558227484231506088 ) ) ;
#3159=CARTESIAN_POINT ( 'NONE',  ( 0.2764156081756483641, -0.1144950937579611167, 0.1126388888888909395 ) ) ;
#3162=DIRECTION ( 'NONE',  ( 0.8320502943378438321, 0.4803844614152620873, -0.2773500981126135745 ) ) ;
#3163=CARTESIAN_POINT ( 'NONE',  ( 0.2764156081756483641, -0.1144950937579611028, 0.1751388888888914530 ) ) ;
#3166=CARTESIAN_POINT ( 'NONE',  ( 0.4687500000000002776, 0.2570931668155775895, 0.04874733047933993424 ) ) ;
#3170=CARTESIAN_POINT ( 'NONE',  ( 0.2764156081756484196, -5.077672346800151106E-17, -0.05055555555555477781 ) ) ;
#3171=CARTESIAN_POINT ( 'NONE',  ( 0.2230971623002954429, 0.2230971623002953319, 0.3747916666666706309 ) ) ;
#3173=EDGE_LOOP ( 'NONE', ( #2490, #3556 ) ) ;
#3175=CARTESIAN_POINT ( 'NONE',  ( 0.3125000000000000000, -5.740531871003217465E-17, 0.03277777777777902274 ) ) ;
#3199=CARTESIAN_POINT ( 'NONE',  ( 0.01875000000000005482, -0.5520911949125800744, 0.06112444011295372487 ) ) ;
#3203=DIRECTION ( 'NONE',  ( 0.000000000000000000, 0.000000000000000000, -1.000000000000000000 ) ) ;
#3216=( BOUNDED_CURVE ( )  B_SPLINE_CURVE ( 2, ( #11876, #4414, #4174, #11750, #7947, #8187, #5879, #6366, #20641 ),
 .UNSPECIFIED., .F., .F. ) 
 B_SPLINE_CURVE_WITH_KNOTS ( ( 3, 2, 2, 2, 3 ),
 ( 0.3125000000000000555, 0.3229166666666667407, 0.3333333333333333703, 0.3437500000000000000, 0.3541666666666666852 ),
 .UNSPECIFIED. ) 
 CURVE ( )  GEOMETRIC_REPRESENTATION_ITEM ( )  RATIONAL_B_SPLINE_CURVE ( ( 0.9999999999999995559, 0.9238795325112871826, 1.000000000000000000, 0.9238795325112867385, 1.000000000000000000, 0.9238795325112867385, 1.000000000000000000, 0.9238795325112867385, 1.000000000000000000 ) ) 
 REPRESENTATION_ITEM ( '' )  );
#3221=EDGE_CURVE ( 'NONE', #2053, #19970, #1958, .T. ) ;
#3233=CARTESIAN_POINT ( 'NONE',  ( -0.1144950937579609918, -0.2764156081756484196, 0.3765277777777820134 ) ) ;
#3234=B_SPLINE_CURVE_WITH_KNOTS ( 'NONE', 3,
 ( #20599, #18528, #353, #3896, #5840, #1818, #11340, #7673, #7794, #20481, #18769, #9505 ),
 .UNSPECIFIED., .F., .F.,
 ( 4, 2, 2, 2, 2, 4 ),
 ( 0.000000000000000000, 0.003345931539952399971, 0.005018897309928598005, 0.006691863079904796473, 0.01003779461985718907, 0.01338372615980958427 ),
 .UNSPECIFIED. ) ;
#3249=CARTESIAN_POINT ( 'NONE',  ( 0.1306872919485616846, 0.3155070326520292290, 0.2150694444444475051 ) ) ;
#3251=CARTESIAN_POINT ( 'NONE',  ( 0.03741580292204597924, -0.5077710590216990560, 0.4064395341356261682 ) ) ;
#3254=CARTESIAN_POINT ( 'NONE',  ( -0.2764156081756484196, -0.1144950937579609362, 0.04319444444444596465 ) ) ;
#3258=EDGE_CURVE ( 'NONE', #20894, #6009, #6178, .T. ) ;
#3261=CARTESIAN_POINT ( 'NONE',  ( -0.4593750000000003664, -6.734002413227273428E-17, 0.4343810118395207698 ) ) ;
#3265=CIRCLE ( 'NONE', #156, 0.01875000000000000625 ) ;
#3270=CARTESIAN_POINT ( 'NONE',  ( -0.2209708691207961373, -0.2209708691207961095, 0.1230555555555574998 ) ) ;
#3275=CARTESIAN_POINT ( 'NONE',  ( 0.2764156081756483641, 0.1144950937579610056, 0.2862500000000035016 ) ) ;
#3279=CARTESIAN_POINT ( 'NONE',  ( 0.3124999999999996669, 0.1294417382415925521, -0.07486111111111071192 ) ) ;
#3284=CARTESIAN_POINT ( 'NONE',  ( 0.4795759056698289946, 0.04342265654436765904, 0.07439901873394898224 ) ) ;
#3287=CARTESIAN_POINT ( 'NONE',  ( -0.2764156081756484196, -0.1144950937579609362, 0.09180555555555744429 ) ) ;
#3288=CARTESIAN_POINT ( 'NONE',  ( -0.2764156081756484196, 0.1144950937579609918, 0.03625000000000144079 ) ) ;
#3289=VERTEX_POINT ( 'NONE', #16683 ) ;
#3300=ORIENTED_EDGE ( 'NONE', *, *, #11112, .F. ) ;
#3304=B_SPLINE_CURVE_WITH_KNOTS ( 'NONE', 3,
 ( #22158, #20334, #211, #14977, #20456, #11437 ),
 .UNSPECIFIED., .F., .F.,
 ( 4, 2, 4 ),
 ( 0.000000000000000000, 0.003402024485550936284, 0.006804048971101872567 ),
 .UNSPECIFIED. ) ;
#3332=DIRECTION ( 'NONE',  ( -0.000000000000000000, -0.000000000000000000, -1.000000000000000000 ) ) ;
#3338=AXIS2_PLACEMENT_3D ( 'NONE', #18171, #7079, #1467 ) ;
#3339=ORIENTED_EDGE ( 'NONE', *, *, #643, .F. ) ;
#3342=CARTESIAN_POINT ( 'NONE',  ( -0.1031051051773897304, -0.2870977370809309481, 0.4162540920893169072 ) ) ;
#3353=ORIENTED_EDGE ( 'NONE', *, *, #10794, .T. ) ;
#3354=AXIS2_PLACEMENT_3D ( 'NONE', #615, #5620, #9523 ) ;
#3356=CARTESIAN_POINT ( 'NONE',  ( -0.2764156081756484196, -0.1144950937579609362, 0.2584722222222254340 ) ) ;
#3357=B_SPLINE_CURVE_WITH_KNOTS ( 'NONE', 3,
 ( #6404, #6523, #19450, #22979, #8225, #1039 ),
 .UNSPECIFIED., .F., .F.,
 ( 4, 2, 4 ),
 ( 0.006847393025867874912, 0.01026280280047527083, 0.01367821257508266761 ),
 .UNSPECIFIED. ) ;
#3361=CARTESIAN_POINT ( 'NONE',  ( -0.4687500000000004441, -0.2170120125989246918, 0.07051005015414456290 ) ) ;
#3369=CARTESIAN_POINT ( 'NONE',  ( -0.1294417382415922191, 0.3125000000000000000, 0.2168055555555583047 ) ) ;
#3373=CARTESIAN_POINT ( 'NONE',  ( 0.3155070326520292290, 0.1306872919485615736, 0.2081250000000030298 ) ) ;
#3375=CARTESIAN_POINT ( 'NONE',  ( 0.3075813148943679631, -0.3526675668868561875, 0.4297318021118050058 ) ) ;
#3378=CARTESIAN_POINT ( 'NONE',  ( 0.2764156081756483641, -0.1144950937579611167, 0.1751388888888914530 ) ) ;
#3386=CARTESIAN_POINT ( 'NONE',  ( 0.3125000000000000000, -5.740531871003217465E-17, 0.3105555555555590819 ) ) ;
#3394=ORIENTED_EDGE ( 'NONE', *, *, #85, .T. ) ;
#3395=CARTESIAN_POINT ( 'NONE',  ( 0.3125000000000000000, -5.740531871003217465E-17, 0.1438888888888910089 ) ) ;
#3400=CARTESIAN_POINT ( 'NONE',  ( -0.1309139991618845367, -0.2436136748879068614, -0.06558227484231496374 ) ) ;
#3401=CARTESIAN_POINT ( 'NONE',  ( -0.2764156081756484196, -0.1144950937579609362, 0.2584722222222254340 ) ) ;
#3406=CARTESIAN_POINT ( 'NONE',  ( 0.1954553509668047195, 0.1954553509668046085, 0.3522222222222262111 ) ) ;
#3412=CARTESIAN_POINT ( 'NONE',  ( 0.1954553509668047195, 0.1954553509668046085, 0.01194444444444571485 ) ) ;
#3413=CARTESIAN_POINT ( 'NONE',  ( -0.2764156081756484196, -0.1144950937579609362, -0.06791666666666604235 ) ) ;
#3416=CARTESIAN_POINT ( 'NONE',  ( 0.2020650928029222304, 0.4371048157571743031, 0.07438423612653367878 ) ) ;
#3417=CARTESIAN_POINT ( 'NONE',  ( 0.4687500000000002776, 0.04423121237726190119, 0.4171966076993701145 ) ) ;
#3425=AXIS2_PLACEMENT_3D ( 'NONE', #10007, #23026, #6327 ) ;
#3442=CARTESIAN_POINT ( 'NONE',  ( 0.3155070326520292290, -0.1306872919485616569, -0.02451388888888812734 ) ) ;
#3450=CARTESIAN_POINT ( 'NONE',  ( 0.4687500000000003886, 0.1740113748017593776, 0.07813285960791813145 ) ) ;
#3452=CARTESIAN_POINT ( 'NONE',  ( -0.07527472113052315061, 0.4862786960646409140, 0.4165495381634259364 ) ) ;
#3453=CARTESIAN_POINT ( 'NONE',  ( -0.1650087075157100902, 0.4586159948670857078, 0.07156199457777139006 ) ) ;
#3456=EDGE_CURVE ( 'NONE', #15771, #1725, #8758, .T. ) ;
#3460=VERTEX_POINT ( 'NONE', #16917 ) ;
#3478=CARTESIAN_POINT ( 'NONE',  ( -0.2764156081756484196, 0.1144950937579609918, 0.2515277777777809587 ) ) ;
#3481=FACE_OUTER_BOUND ( 'NONE', #43, .T. ) ;
#3485=EDGE_CURVE ( 'NONE', #18897, #23410, #14606, .T. ) ;
#3491=CARTESIAN_POINT ( 'NONE',  ( 0.3155070326520292290, -0.1306872919485616569, 0.2011805555555585268 ) ) ;
#3493=ORIENTED_EDGE ( 'NONE', *, *, #2481, .F. ) ;
#3500=CARTESIAN_POINT ( 'NONE',  ( 0.1144950937579611444, 0.2764156081756483641, 0.1890277777777804036 ) ) ;
#3502=CARTESIAN_POINT ( 'NONE',  ( -0.4796768793270155817, -0.08622052910184242747, 0.07157886890657255696 ) ) ;
#3515=CARTESIAN_POINT ( 'NONE',  ( -0.006494592122000062383, 0.5491884613158956041, 0.04193801346286451376 ) ) ;
#3516=ORIENTED_EDGE ( 'NONE', *, *, #10077, .F. ) ;
#3522=( BOUNDED_CURVE ( )  B_SPLINE_CURVE ( 2, ( #21676, #4608, #6553, #6676, #11953, #15711, #944, #8374, #11823 ),
 .UNSPECIFIED., .F., .F. ) 
 B_SPLINE_CURVE_WITH_KNOTS ( ( 3, 2, 2, 2, 3 ),
 ( 0.03786521205662927991, 0.04166666666666673374, 0.05208333333333335646, 0.06249999999999997224, 0.07291666666666669905 ),
 .UNSPECIFIED. ) 
 CURVE ( )  GEOMETRIC_REPRESENTATION_ITEM ( )  RATIONAL_B_SPLINE_CURVE ( ( 0.9647168388458124966, 0.9722206238028953118, 1.000000000000000000, 0.9238795325112867385, 1.000000000000000000, 0.9238795325112867385, 1.000000000000000000, 0.9238795325112870716, 0.9999999999999996669 ) ) 
 REPRESENTATION_ITEM ( '' )  );
#3524=CARTESIAN_POINT ( 'NONE',  ( -0.2764156081756484196, -0.1144950937579609362, 0.1473611111111134686 ) ) ;
#3527=CARTESIAN_POINT ( 'NONE',  ( -0.1954553509668046918, -0.1954553509668046640, 0.3800000000000041678 ) ) ;
#3530=CARTESIAN_POINT ( 'NONE',  ( 0.4687500000000002776, -0.2570931668155774230, 0.04874733047934001057 ) ) ;
#3533=CARTESIAN_POINT ( 'NONE',  ( 0.2764156081756483641, 0.1144950937579610056, -0.04013888888888804407 ) ) ;
#3541=DIRECTION ( 'NONE',  ( 0.5000000000000003331, -0.8660254037844383745, -9.106159978880865562E-16 ) ) ;
#3544=ORIENTED_EDGE ( 'NONE', *, *, #5352, .T. ) ;
#3552=CARTESIAN_POINT ( 'NONE',  ( -0.4687500000000004441, 0.2630309001378779987, 0.05971062996526180916 ) ) ;
#3556=ORIENTED_EDGE ( 'NONE', *, *, #7501, .T. ) ;
#3561=CARTESIAN_POINT ( 'NONE',  ( -0.3155070326520293400, 0.1306872919485614903, 0.003263888888889874412 ) ) ;
#3562=CARTESIAN_POINT ( 'NONE',  ( 0.000000000000000000, 0.000000000000000000, 1.326383476483184332 ) ) ;
#3569=ADVANCED_FACE ( 'NONE', ( #6176 ), #13871, .T. ) ;
#3573=CARTESIAN_POINT ( 'NONE',  ( -0.3853527072884239679, 0.3187823880793517195, 0.07808165802386347887 ) ) ;
#3591=ORIENTED_EDGE ( 'NONE', *, *, #11260, .F. ) ;
#3593=ORIENTED_EDGE ( 'NONE', *, *, #20932, .T. ) ;
#3595=CARTESIAN_POINT ( 'NONE',  ( 0.2764156081756483641, 0.1144950937579610056, 0.3418055555555594704 ) ) ;
#3598=CARTESIAN_POINT ( 'NONE',  ( 2.423612122230044959E-16, -0.5289902422706636020, 0.3941886329748525153 ) ) ;
#3609=CARTESIAN_POINT ( 'NONE',  ( 0.2230971623002954429, 0.2230971623002953319, 0.2671527777777812362 ) ) ;
#3613=CARTESIAN_POINT ( 'NONE',  ( 0.1904260988303481950, -0.4204977338396739817, 0.4343746145485237187 ) ) ;
#3614=ADVANCED_FACE ( 'NONE', ( #17518 ), #8240, .F. ) ;
#3618=CARTESIAN_POINT ( 'NONE',  ( 0.1954553509668046640, -0.1954553509668047195, 0.2827777777777811807 ) ) ;
#3620=CARTESIAN_POINT ( 'NONE',  ( -0.4800173708727313859, -0.1715353579592617805, 0.06110628606926749029 ) ) ;
#3631=CARTESIAN_POINT ( 'NONE',  ( 0.006583943204587710575, 0.5374646359837784715, 0.05971082423030439623 ) ) ;
#3632=ORIENTED_EDGE ( 'NONE', *, *, #17864, .T. ) ;
#3638=EDGE_CURVE ( 'NONE', #8540, #1241, #21598, .T. ) ;
#3641=CARTESIAN_POINT ( 'NONE',  ( 0.1144950937579609085, -0.2764156081756484751, 0.2723611111111144401 ) ) ;
#3643=EDGE_CURVE ( 'NONE', #8247, #20864, #10439, .T. ) ;
#3651=CARTESIAN_POINT ( 'NONE',  ( -0.2764156081756484196, -0.1144950937579609362, -0.01236111111111004406 ) ) ;
#3656=CARTESIAN_POINT ( 'NONE',  ( 0.4687499999999811262, 0.04487173304136180679, 0.4280330084738984131 ) ) ;
#3675=DIRECTION ( 'NONE',  ( 0.000000000000000000, 0.000000000000000000, 1.000000000000000000 ) ) ;
#3677=VECTOR ( 'NONE', #20766, 39.37007874015748143 ) ;
#3680=VERTEX_POINT ( 'NONE', #928 ) ;
#3685=CARTESIAN_POINT ( 'NONE',  ( 0.3155070326520292290, 0.1306872919485615736, -0.07312499999999962086 ) ) ;
#3686=CARTESIAN_POINT ( 'NONE',  ( -0.4570242136016808843, -0.2774028246161672762, 0.04874733047933989261 ) ) ;
#3692=CARTESIAN_POINT ( 'NONE',  ( 0.000000000000000000, 0.000000000000000000, -0.05999999999999999084 ) ) ;
#3706=AXIS2_PLACEMENT_3D ( 'NONE', #10467, #6795, #10225 ) ;
#3708=CARTESIAN_POINT ( 'NONE',  ( 0.000000000000000000, 0.000000000000000000, 1.326383476483184332 ) ) ;
#3716=LINE ( 'NONE', #13129, #15145 ) ;
#3722=ORIENTED_EDGE ( 'NONE', *, *, #467, .F. ) ;
#3724=CARTESIAN_POINT ( 'NONE',  ( 0.1144950937579609085, -0.2764156081756484751, 0.2723611111111144401 ) ) ;
#3737=DIRECTION ( 'NONE',  ( 0.8459207832372976910, 0.4883925919151544948, 0.2142211582677918946 ) ) ;
#3740=CARTESIAN_POINT ( 'NONE',  ( -0.2230971623002954152, -0.2230971623002953874, 0.2393750000000033074 ) ) ;
#3747=CARTESIAN_POINT ( 'NONE',  ( -0.2764156081756484196, 0.1144950937579609918, 0.1473611111111134686 ) ) ;
#3769=CARTESIAN_POINT ( 'NONE',  ( -3.385114897866767815E-17, -0.2764156081756484196, 0.2688888888888921747 ) ) ;
#3777=CARTESIAN_POINT ( 'NONE',  ( -0.3124999999999989453, -0.1294417382415932460, 0.06402777777777933499 ) ) ;
#3778=CARTESIAN_POINT ( 'NONE',  ( 0.1954553509668046640, -0.1954553509668047195, 0.005000000000001192726 ) ) ;
#3805=CARTESIAN_POINT ( 'NONE',  ( 0.6398935782932173577, 7.836436224517350621E-17, -0.1019043464467004889 ) ) ;
#3806=CARTESIAN_POINT ( 'NONE',  ( -0.1294417382415922746, -0.3125000000000000000, 0.1820833333333357340 ) ) ;
#3808=CARTESIAN_POINT ( 'NONE',  ( -0.3155070326520293400, -0.1306872919485614626, -0.1009027777777776053 ) ) ;
#3809=CARTESIAN_POINT ( 'NONE',  ( 0.4687500000000002776, -0.2386081413226768533, 0.3840704193421530244 ) ) ;
#3814=ADVANCED_FACE ( 'NONE', ( #4467, #18123 ), #7029, .T. ) ;
#3822=CARTESIAN_POINT ( 'NONE',  ( -0.4593750000000004219, 0.2760455974562898707, 0.06112444011295372487 ) ) ;
#3826=CARTESIAN_POINT ( 'NONE',  ( 0.004657599350281299740, -0.3068592482405122501, -0.09560169298593859666 ) ) ;
#3832=CARTESIAN_POINT ( 'NONE',  ( 0.1899274842524382167, -0.4207833852643003136, 0.4343212420608418833 ) ) ;
#3837=CARTESIAN_POINT ( 'NONE',  ( -0.3125000000000000555, 1.913510623667739771E-17, 0.1786111111111139127 ) ) ;
#3847=CARTESIAN_POINT ( 'NONE',  ( -0.2026594160797258459, 0.4367605021652133379, 0.07441357458167799366 ) ) ;
#3858=VERTEX_POINT ( 'NONE', #16174 ) ;
#3859=( BOUNDED_CURVE ( )  B_SPLINE_CURVE ( 2, ( #18526, #16937, #18407, #1816, #15001, #1585, #20597, #13184, #9260 ),
 .UNSPECIFIED., .F., .T. ) 
 B_SPLINE_CURVE_WITH_KNOTS ( ( 3, 2, 2, 2, 3 ),
 ( 0.4062499999999999445, 0.4166666666666667407, 0.4270833333333333703, 0.4375000000000001110, 0.4479166666666667407 ),
 .UNSPECIFIED. ) 
 CURVE ( )  GEOMETRIC_REPRESENTATION_ITEM ( )  RATIONAL_B_SPLINE_CURVE ( ( 1.000000000000000444, 0.9238795325112862944, 1.000000000000000000, 0.9238795325112867385, 1.000000000000000000, 0.9238795325112867385, 1.000000000000000000, 0.9238795325112862944, 1.000000000000000444 ) ) 
 REPRESENTATION_ITEM ( '' )  );
#3860=CARTESIAN_POINT ( 'NONE',  ( 0.4621664414996921044, 0.2744339579550159058, 0.05971062996526297489 ) ) ;
#3862=( BOUNDED_CURVE ( )  B_SPLINE_CURVE ( 2, ( #1242, #19650, #14168, #13814, #6604, #15997, #16118, #21367, #17704 ),
 .UNSPECIFIED., .F., .T. ) 
 B_SPLINE_CURVE_WITH_KNOTS ( ( 3, 2, 2, 2, 3 ),
 ( 0.07291666666666669905, 0.08333333333333332871, 0.09374999999999994449, 0.1041666666666666852, 0.1145833333333333148 ),
 .UNSPECIFIED. ) 
 CURVE ( )  GEOMETRIC_REPRESENTATION_ITEM ( )  RATIONAL_B_SPLINE_CURVE ( ( 1.000000000000000222, 0.9238795325112864054, 1.000000000000000000, 0.9238795325112867385, 1.000000000000000000, 0.9238795325112867385, 1.000000000000000000, 0.9238795325112871826, 0.9999999999999995559 ) ) 
 REPRESENTATION_ITEM ( '' )  );
#3867=CARTESIAN_POINT ( 'NONE',  ( -0.2764156081756484196, -0.1144950937579609362, 0.03625000000000147549 ) ) ;
#3869=CARTESIAN_POINT ( 'NONE',  ( -0.1144950937579609779, 0.2764156081756484196, 0.1959722222222249899 ) ) ;
#3876=CARTESIAN_POINT ( 'NONE',  ( 0.2800968539712072602, -5.145295735006237905E-17, 0.3917635206378741186 ) ) ;
#3882=VECTOR ( 'NONE', #7538, 39.37007874015748143 ) ;
#3885=CARTESIAN_POINT ( 'NONE',  ( -3.385114897866767815E-17, -0.2764156081756484196, 0.4355555555555601921 ) ) ;
#3889=CIRCLE ( 'NONE', #17144, 0.01875000000000003400 ) ;
#3894=CARTESIAN_POINT ( 'NONE',  ( 0.4620259694561523744, -0.2880908832651558615, 0.04413116910601658921 ) ) ;
#3896=CARTESIAN_POINT ( 'NONE',  ( 0.1395639791202929747, 0.4606885764509979220, 0.4108348780186336091 ) ) ;
#3897=CARTESIAN_POINT ( 'NONE',  ( 0.1954553509668047195, 0.1954553509668046085, 0.2966666666666701313 ) ) ;
#3900=CARTESIAN_POINT ( 'NONE',  ( 0.4687500000000003886, 0.1119035383512243936, 0.4216345187268149552 ) ) ;
#3907=CARTESIAN_POINT ( 'NONE',  ( 0.3125000000000000000, -5.740531871003217465E-17, 0.2063888888888918416 ) ) ;
#3916=CARTESIAN_POINT ( 'NONE',  ( 0.2969103404914450461, -0.03343391069991762110, -0.08748023474661176246 ) ) ;
#3920=CARTESIAN_POINT ( 'NONE',  ( -0.1144950937579609918, -0.2764156081756484196, -0.005416666666665556629 ) ) ;
#3927=CARTESIAN_POINT ( 'NONE',  ( -0.3155070326520293400, 0.1306872919485614903, -0.1078472222222221499 ) ) ;
#3929=CARTESIAN_POINT ( 'NONE',  ( -0.05483022876052533884, -0.5228926224321407412, 0.05347271648849222930 ) ) ;
#3940=CARTESIAN_POINT ( 'NONE',  ( -0.01172578639831971595, 0.5344959914317446437, 0.04874733047933995506 ) ) ;
#3944=EDGE_CURVE ( 'NONE', #23326, #19970, #10689, .T. ) ;
#3949=FACE_OUTER_BOUND ( 'NONE', #12550, .T. ) ;
#3958=VERTEX_POINT ( 'NONE', #424 ) ;
#3961=CARTESIAN_POINT ( 'NONE',  ( -0.2764156081756484196, -0.1144950937579609362, 0.4251388888888933959 ) ) ;
#3974=CARTESIAN_POINT ( 'NONE',  ( 0.1306872919485614071, -0.3155070326520293955, 0.4164583333333380377 ) ) ;
#3978=EDGE_CURVE ( 'NONE', #20894, #5886, #7739, .T. ) ;
#3979=CARTESIAN_POINT ( 'NONE',  ( 0.2021572709300329673, -0.4370510722512370161, 0.07439726544913842499 ) ) ;
#3980=CARTESIAN_POINT ( 'NONE',  ( -3.385114897866767815E-17, -0.2764156081756484196, 0.3244444444444482545 ) ) ;
#3982=CARTESIAN_POINT ( 'NONE',  ( -3.385114897866767815E-17, -0.2764156081756484196, -0.06444444444444379083 ) ) ;
#3984=CARTESIAN_POINT ( 'NONE',  ( -0.006583943204589224121, -0.5374646359837778054, 0.05971082423030150271 ) ) ;
#3996=CARTESIAN_POINT ( 'NONE',  ( 0.4500000000000003442, -0.2598076211353317899, 0.3779506566538943235 ) ) ;
#4003=CARTESIAN_POINT ( 'NONE',  ( 0.3155070326520292845, -5.795770164686806123E-17, -0.07312499999999920453 ) ) ;
#4005=EDGE_CURVE ( 'NONE', #11906, #20538, #6564, .T. ) ;
#4015=CARTESIAN_POINT ( 'NONE',  ( -0.1954553509668046640, 0.1954553509668046918, 0.1438888888888912032 ) ) ;
#4020=VECTOR ( 'NONE', #13628, 39.37007874015748854 ) ;
#4025=VERTEX_POINT ( 'NONE', #15073 ) ;
#4026=CARTESIAN_POINT ( 'NONE',  ( 0.3125000000000000555, -5.740531871003217465E-17, 0.1508333333333358728 ) ) ;
#4029=SHAPE_REPRESENTATION_RELATIONSHIP ( 'NONE' , 'NONE' ,  #12001, #14347 ) ;
#4030=CARTESIAN_POINT ( 'NONE',  ( -0.1954553509668046640, 0.1954553509668046918, -0.1408333333333332826 ) ) ;
#4033=DIRECTION ( 'NONE',  ( -0.000000000000000000, -0.000000000000000000, -1.000000000000000000 ) ) ;
#4034=LINE ( 'NONE', #19151, #11247 ) ;
#4038=CARTESIAN_POINT ( 'NONE',  ( 0.2800968539712072602, -5.145295735006237905E-17, 0.3917635206378741186 ) ) ;
#4041=CARTESIAN_POINT ( 'NONE',  ( 0.2230971623002954429, 0.2230971623002953319, 0.1525694444444466169 ) ) ;
#4042=CARTESIAN_POINT ( 'NONE',  ( -0.3886748462736269172, -0.3298755754955817743, 0.06108448616841026524 ) ) ;
#4050=EDGE_CURVE ( 'NONE', #5967, #4025, #15493, .T. ) ;
#4059=CARTESIAN_POINT ( 'NONE',  ( 0.1209188320989911664, 0.2598538660581671822, 0.3981211010572119902 ) ) ;
#4062=VERTEX_POINT ( 'NONE', #16774 ) ;
#4064=ORIENTED_EDGE ( 'NONE', *, *, #23173, .F. ) ;
#4068=AXIS2_PLACEMENT_3D ( 'NONE', #10430, #1627, #12622 ) ;
#4073=CARTESIAN_POINT ( 'NONE',  ( -2.187612651176460788E-16, 0.5196152422706634688, 0.3779506566538943790 ) ) ;
#4076=CARTESIAN_POINT ( 'NONE',  ( -0.3068695747081881531, -0.3531079105191464729, 0.4306248051561444301 ) ) ;
#4094=CARTESIAN_POINT ( 'NONE',  ( 0.1144950937579611444, 0.2764156081756483641, 0.3556944444444484210 ) ) ;
#4095=EDGE_CURVE ( 'NONE', #11153, #14969, #6920, .T. ) ;
#4098=CARTESIAN_POINT ( 'NONE',  ( -0.1144950937579609918, -0.2764156081756484196, 0.2098611111111139960 ) ) ;
#4100=CARTESIAN_POINT ( 'NONE',  ( 0.2764156081756484196, -5.077672346800151106E-17, -0.05055555555555477781 ) ) ;
#4105=CARTESIAN_POINT ( 'NONE',  ( -0.2229532752983975630, 0.1767350293216390922, -0.07304505964698700116 ) ) ;
#4108=CARTESIAN_POINT ( 'NONE',  ( 0.4687500000000014988, 0.2629282712287717150, 0.05975564523638850906 ) ) ;
#4114=DIRECTION ( 'NONE',  ( 1.000000000000000000, 0.000000000000000000, 0.000000000000000000 ) ) ;
#4121=AXIS2_PLACEMENT_3D ( 'NONE', #7019, #21884, #5175 ) ;
#4122=CARTESIAN_POINT ( 'NONE',  ( -0.2764156081756484196, 0.1144950937579609918, 0.4181944444444490872 ) ) ;
#4128=CARTESIAN_POINT ( 'NONE',  ( 0.2764156081756484196, -5.077672346800151106E-17, -0.09916666666666629215 ) ) ;
#4131=CARTESIAN_POINT ( 'NONE',  ( -0.1144950937579609918, -0.2764156081756484196, 0.2168055555555584712 ) ) ;
#4156=CARTESIAN_POINT ( 'NONE',  ( 0.1144950937579611444, 0.2764156081756483641, 0.07791666666666842433 ) ) ;
#4160=CARTESIAN_POINT ( 'NONE',  ( 0.000000000000000000, 0.000000000000000000, 0.4425000000000000044 ) ) ;
#4163=CARTESIAN_POINT ( 'NONE',  ( 0.2230971623002953874, -0.2230971623002954429, 0.08312500000000162814 ) ) ;
#4164=CARTESIAN_POINT ( 'NONE',  ( -0.2774186958558242933, -0.3935988683107538577, 0.07439726544913140283 ) ) ;
#4168=ORIENTED_EDGE ( 'NONE', *, *, #521, .F. ) ;
#4174=CARTESIAN_POINT ( 'NONE',  ( 0.2209708691207961651, 0.2209708691207959985, 0.09527777777777951540 ) ) ;
#4177=CARTESIAN_POINT ( 'NONE',  ( -0.1986479633930287036, -0.2391244849435051334, -0.09958585457510185646 ) ) ;
#4183=DIRECTION ( 'NONE',  ( -0.000000000000000000, -0.000000000000000000, -1.000000000000000000 ) ) ;
#4186=ORIENTED_EDGE ( 'NONE', *, *, #20332, .F. ) ;
#4190=CARTESIAN_POINT ( 'NONE',  ( -0.3125000000000000000, 1.913510623667739771E-17, 0.2341666666666698537 ) ) ;
#4191=CARTESIAN_POINT ( 'NONE',  ( 0.3112631253509388074, 0.3615580281551279418, 0.4252366019055049406 ) ) ;
#4197=CARTESIAN_POINT ( 'NONE',  ( 0.1144950937579609085, -0.2764156081756484751, 0.4390277777777825130 ) ) ;
#4199=EDGE_CURVE ( 'NONE', #1725, #17904, #5610, .T. ) ;
#4208=EDGE_LOOP ( 'NONE', ( #19682, #4186, #9707, #18248 ) ) ;
#4213=CARTESIAN_POINT ( 'NONE',  ( 0.3155070326520292290, 0.1306872919485615736, 0.4303472222222270438 ) ) ;
#4219=CARTESIAN_POINT ( 'NONE',  ( 0.1590601067977331917, -0.4494324818882468597, 0.07654795713851240968 ) ) ;
#4221=CARTESIAN_POINT ( 'NONE',  ( -0.1954553509668046640, 0.1954553509668046918, 0.1925000000000027245 ) ) ;
#4223=CARTESIAN_POINT ( 'NONE',  ( -0.2764156081756484196, 1.692557448933383907E-17, -0.1338888888888887796 ) ) ;
#4224=ORIENTED_EDGE ( 'NONE', *, *, #15315, .T. ) ;
#4238=VERTEX_POINT ( 'NONE', #11349 ) ;
#4240=CIRCLE ( 'NONE', #17874, 0.6211549996190571798 ) ;
#4243=CARTESIAN_POINT ( 'NONE',  ( 0.1144950937579611444, 0.2764156081756483641, 0.4598611111111159389 ) ) ;
#4252=CARTESIAN_POINT ( 'NONE',  ( 0.3125000000000004996, -0.1294417382415918583, 0.08486111111111281635 ) ) ;
#4253=CARTESIAN_POINT ( 'NONE',  ( -0.2764156081756484196, 1.692557448933383907E-17, 0.1508333333333356785 ) ) ;
#4260=CIRCLE ( 'NONE', #14776, 0.3125000000000000000 ) ;
#4267=CARTESIAN_POINT ( 'NONE',  ( 0.3124999999999993339, -0.1294417382415928852, 0.1473611111111136351 ) ) ;
#4270=CARTESIAN_POINT ( 'NONE',  ( 0.3854970698558352615, -0.3186990403121960913, 0.4003306813560889577 ) ) ;
#4271=DIRECTION ( 'NONE',  ( 0.000000000000000000, 0.000000000000000000, 1.000000000000000000 ) ) ;
#4282=CARTESIAN_POINT ( 'NONE',  ( 0.000000000000000000, 0.3155070326520292845, 0.2150694444444470887 ) ) ;
#4296=CARTESIAN_POINT ( 'NONE',  ( 0.1064715942167347440, -0.2552471790384449046, 0.3880822748423152224 ) ) ;
#4308=DIRECTION ( 'NONE',  ( -0.000000000000000000, -0.000000000000000000, -1.000000000000000000 ) ) ;
#4324=EDGE_LOOP ( 'NONE', ( #36, #1115, #5653, #21234 ) ) ;
#4331=CARTESIAN_POINT ( 'NONE',  ( -0.2230971623002954152, -0.2230971623002953874, 0.4060416666666712970 ) ) ;
#4336=CARTESIAN_POINT ( 'NONE',  ( 0.3853527072883956572, -0.3187823880793682063, 0.07808165802388239429 ) ) ;
#4337=CARTESIAN_POINT ( 'NONE',  ( 0.2764156081756484196, -5.077672346800151106E-17, 0.1716666666666692431 ) ) ;
#4339=CARTESIAN_POINT ( 'NONE',  ( -0.1144950937579609779, 0.2764156081756484196, -0.08874999999999953759 ) ) ;
#4342=CARTESIAN_POINT ( 'NONE',  ( -0.01172578639833055797, -0.5344959914317364280, 0.04874733047934380614 ) ) ;
#4360=CARTESIAN_POINT ( 'NONE',  ( 0.1954553509668047195, 0.1954553509668046085, 0.4563888888888936735 ) ) ;
#4362=ORIENTED_EDGE ( 'NONE', *, *, #20927, .T. ) ;
#4368=CARTESIAN_POINT ( 'NONE',  ( -0.2764156081756484196, 1.692557448933383907E-17, 0.2619444444444476994 ) ) ;
#4377=CARTESIAN_POINT ( 'NONE',  ( -0.1568395974156474859, 0.4507144935777588346, 0.4251457422752842330 ) ) ;
#4380=EDGE_CURVE ( 'NONE', #1752, #20538, #21338, .T. ) ;
#4383=CARTESIAN_POINT ( 'NONE',  ( -3.827021247335479543E-17, -0.3125000000000000000, 0.1369444444444468667 ) ) ;
#4385=FACE_OUTER_BOUND ( 'NONE', #9237, .T. ) ;
#4386=CARTESIAN_POINT ( 'NONE',  ( 0.1956796206285028594, -0.4282901957204846011, 0.4181140142936810578 ) ) ;
#4389=CARTESIAN_POINT ( 'NONE',  ( -0.4687500000000003331, 0.04364354118082217765, 0.07944686358224754830 ) ) ;
#4393=CARTESIAN_POINT ( 'NONE',  ( -0.2764156081756484196, 1.692557448933383907E-17, -0.01583333333333230425 ) ) ;
#4394=CARTESIAN_POINT ( 'NONE',  ( -0.2209708691207961373, -0.2209708691207961095, 0.3522222222222263222 ) ) ;
#4400=CARTESIAN_POINT ( 'NONE',  ( -0.2230971623002954152, -0.2230971623002953874, 0.2359027777777805979 ) ) ;
#4413=ORIENTED_EDGE ( 'NONE', *, *, #15590, .T. ) ;
#4414=CARTESIAN_POINT ( 'NONE',  ( 0.3124999999999993339, 0.1294417382415928297, 0.09180555555555727776 ) ) ;
#4420=ORIENTED_EDGE ( 'NONE', *, *, #14991, .F. ) ;
#4421=CARTESIAN_POINT ( 'NONE',  ( 0.2784250239278243666, 0.03789337644375263825, 0.3924996019884888221 ) ) ;
#4432=CARTESIAN_POINT ( 'NONE',  ( -0.3885631146789287338, -0.3299392016703766028, 0.06110928887248354840 ) ) ;
#4433=AXIS2_PLACEMENT_3D ( 'NONE', #20154, #6990, #21620 ) ;
#4445=B_SPLINE_CURVE_WITH_KNOTS ( 'NONE', 3,
 ( #21985, #21502, #5156, #12747, #4919, #6873, #20162, #3450, #21749, #10656 ),
 .UNSPECIFIED., .F., .F.,
 ( 4, 2, 2, 2, 4 ),
 ( 0.000000000000000000, 0.003321891969150509404, 0.006643783938301018807, 0.009965675907451529078, 0.01328756787660204108 ),
 .UNSPECIFIED. ) ;
#4449=ORIENTED_EDGE ( 'NONE', *, *, #23504, .T. ) ;
#4450=FACE_OUTER_BOUND ( 'NONE', #1373, .T. ) ;
#4454=CARTESIAN_POINT ( 'NONE',  ( -0.4687500000000003886, -0.02223792287132515463, 0.4181395016878637905 ) ) ;
#4455=CARTESIAN_POINT ( 'NONE',  ( 0.1294417382415924134, 0.3124999999999999445, 0.2723611111111146621 ) ) ;
#4456=CARTESIAN_POINT ( 'NONE',  ( 0.1650087075157316563, -0.4586159948670568420, 0.07156199457778184003 ) ) ;
#4457=CARTESIAN_POINT ( 'NONE',  ( -0.1954553509668046918, -0.1954553509668046640, 0.2063888888888917028 ) ) ;
#4459=CARTESIAN_POINT ( 'NONE',  ( -0.1954553509668046918, -0.1954553509668046640, 0.3800000000000041678 ) ) ;
#4460=VERTEX_POINT ( 'NONE', #20847 ) ;
#4466=CYLINDRICAL_SURFACE ( 'NONE', #15669, 0.3125000000000000000 ) ;
#4467=FACE_BOUND ( 'NONE', #22915, .T. ) ;
#4473=ORIENTED_EDGE ( 'NONE', *, *, #6647, .T. ) ;
#4479=CARTESIAN_POINT ( 'NONE',  ( -0.3155070326520293400, 0.1306872919485614903, 0.06229166666666853536 ) ) ;
#4480=AXIS2_PLACEMENT_3D ( 'NONE', #2188, #7664, #465 ) ;
#4482=ADVANCED_FACE ( 'NONE', ( #13310 ), #723, .F. ) ;
#4485=FACE_OUTER_BOUND ( 'NONE', #10551, .T. ) ;
#4487=DIRECTION ( 'NONE',  ( 0.8660254037844389297, -0.4999999999999995559, 0.000000000000000000 ) ) ;
#4500=CARTESIAN_POINT ( 'NONE',  ( -0.04612934949349477981, 0.5146330850176630278, 0.3902021065398098565 ) ) ;
#4514=CARTESIAN_POINT ( 'NONE',  ( -0.2764156081756484196, -0.1144950937579609362, 0.1543055555555579716 ) ) ;
#4517=VECTOR ( 'NONE', #21844, 39.37007874015748143 ) ;
#4519=CARTESIAN_POINT ( 'NONE',  ( 0.4796768774581259831, 0.08621990061574087705, 0.07157892306036504892 ) ) ;
#4522=CIRCLE ( 'NONE', #1787, 0.3125000000000000000 ) ;
#4524=CARTESIAN_POINT ( 'NONE',  ( 0.1306872919485616846, 0.3155070326520292290, 0.2671527777777808477 ) ) ;
#4536=VERTEX_POINT ( 'NONE', #19025 ) ;
#4539=CARTESIAN_POINT ( 'NONE',  ( 0.1961415469428243463, -0.1956144934195144791, 0.3880822748423151114 ) ) ;
#4540=VECTOR ( 'NONE', #12371, 39.37007874015748854 ) ;
#4543=CARTESIAN_POINT ( 'NONE',  ( 0.2107751267066954592, 0.1916353986792963815, 0.3959111835198027007 ) ) ;
#4559=EDGE_CURVE ( 'NONE', #13125, #17792, #2269, .T. ) ;
#4568=ADVANCED_FACE ( 'NONE', ( #955 ), #15723, .T. ) ;
#4571=AXIS2_PLACEMENT_3D ( 'NONE', #833, #6317, #2893 ) ;
#4574=ORIENTED_EDGE ( 'NONE', *, *, #20332, .T. ) ;
#4575=CARTESIAN_POINT ( 'NONE',  ( 0.4805070082343982918, 0.2560807851245620048, 0.04413116910602137705 ) ) ;
#4579=FACE_OUTER_BOUND ( 'NONE', #1706, .T. ) ;
#4580=CARTESIAN_POINT ( 'NONE',  ( -0.4687500000000003886, 0.1752294869986955883, 0.4001773373238182718 ) ) ;
#4581=CARTESIAN_POINT ( 'NONE',  ( 0.2209708691207961651, 0.2209708691207959985, 0.2688888888888923412 ) ) ;
#4584=CARTESIAN_POINT ( 'NONE',  ( -0.2764156081756484196, 0.1144950937579609918, 0.1404166666666689656 ) ) ;
#4591=DIRECTION ( 'NONE',  ( -1.000000000000000000, 0.000000000000000000, 0.000000000000000000 ) ) ;
#4592=CARTESIAN_POINT ( 'NONE',  ( 0.4875000000000002665, -0.2598076211353317899, 0.06112444011295373181 ) ) ;
#4598=CARTESIAN_POINT ( 'NONE',  ( 0.3101174172661914086, 0.3622195030262473359, 0.08858683671056809261 ) ) ;
#4600=CARTESIAN_POINT ( 'NONE',  ( 0.1294417382415921358, -0.3125000000000002220, 0.08486111111111313554 ) ) ;
#4601=DESIGN_CONTEXT ( 'detailed design', #12648, 'design' ) ;
#4602=FACE_OUTER_BOUND ( 'NONE', #7366, .T. ) ;
#4603=CARTESIAN_POINT ( 'NONE',  ( 0.1306872919485614071, -0.3155070326520293955, 0.08312500000000203060 ) ) ;
#4607=CARTESIAN_POINT ( 'NONE',  ( 0.2764156081756484196, -5.077672346800151106E-17, 0.1230555555555576941 ) ) ;
#4608=CARTESIAN_POINT ( 'NONE',  ( 0.2527126213444991776, -0.1892291168970930137, 0.4228708124548452574 ) ) ;
#4610=CARTESIAN_POINT ( 'NONE',  ( -0.1954553509668046918, -0.1954553509668046640, 0.3800000000000041678 ) ) ;
#4619=FACE_OUTER_BOUND ( 'NONE', #4208, .T. ) ;
#4622=ORIENTED_EDGE ( 'NONE', *, *, #16678, .F. ) ;
#4627=CARTESIAN_POINT ( 'NONE',  ( -0.4796773749965631550, -0.08638149583431357914, 0.07156438896664418792 ) ) ;
#4628=CARTESIAN_POINT ( 'NONE',  ( 0.1954553509668046640, -0.1954553509668047195, -0.001944444444443294917 ) ) ;
#4634=CARTESIAN_POINT ( 'NONE',  ( 0.000000000000000000, 0.2764156081756484196, 0.1925000000000026690 ) ) ;
#4635=( BOUNDED_SURFACE ( )  B_SPLINE_SURFACE ( 3, 2, ( 
 ( #19539, #2831, #1008 ),
 ( #16608, #8926, #3552 ),
 ( #14902, #11003, #11122 ),
 ( #18431, #5505, #5624 ),
 ( #14668, #21964, #18670 ),
 ( #13206, #1726, #16726 ) ),
 .UNSPECIFIED., .F., .F., .F. ) 
 B_SPLINE_SURFACE_WITH_KNOTS ( ( 4, 2, 4 ),
 ( 3, 3 ),
 ( 0.001022076388580720786, 0.001521441877679463508, 0.002020807366778206229 ),
 ( 0.000000000000000000, 1.000000000000000000 ),
 .UNSPECIFIED. ) 
 GEOMETRIC_REPRESENTATION_ITEM ( )  RATIONAL_B_SPLINE_SURFACE ( (
 ( 1.000000000000000000, 0.8285407536241355952, 1.000000000000000000),
 ( 1.000000000000000000, 0.8382697314793432497, 1.000000000000000000),
 ( 1.000000000000000000, 0.8433836253082970247, 1.000000000000000000),
 ( 1.000000000000000000, 0.8433992480895827759, 1.000000000000000000),
 ( 1.000000000000000000, 0.8382827608168984534, 1.000000000000000000),
 ( 1.000000000000000000, 0.8285407536241036208, 1.000000000000000000) ) ) 
 REPRESENTATION_ITEM ( '' )  SURFACE ( )  );
#4642=CARTESIAN_POINT ( 'NONE',  ( -0.2230971623002953874, 0.2230971623002954152, 0.3886805555555595815 ) ) ;
#4643=CARTESIAN_POINT ( 'NONE',  ( -0.3125000000000010547, 0.1294417382415911921, 0.05708333333333479032 ) ) ;
#4691=CARTESIAN_POINT ( 'NONE',  ( -0.3125000000000000000, 1.913510623667739771E-17, 0.2272222222222250176 ) ) ;
#4697=CARTESIAN_POINT ( 'NONE',  ( 0.1954553509668046640, -0.1954553509668047195, 0.3869444444444487541 ) ) ;
#4699=CARTESIAN_POINT ( 'NONE',  ( -0.2764156081756484196, 0.1144950937579609918, 0.02930555555555695163 ) ) ;
#4702=CARTESIAN_POINT ( 'NONE',  ( 0.2573004767273346927, 0.1442547113246375190, -0.08399358639954626615 ) ) ;
#4703=DIRECTION ( 'NONE',  ( 0.000000000000000000, 0.2773500981126160725, -0.9607689228305223983 ) ) ;
#4707=CIRCLE ( 'NONE', #17961, 0.01874999999999997502 ) ;
#4710=CARTESIAN_POINT ( 'NONE',  ( 0.4620259694561525410, 0.2880908832651559726, 0.04413116910601652676 ) ) ;
#4713=CARTESIAN_POINT ( 'NONE',  ( -0.6211549996190571798, 0.000000000000000000, -0.1199999999999999956 ) ) ;
#4714=CARTESIAN_POINT ( 'NONE',  ( 0.4692113125120487838, -0.2611562006105975775, 0.04763592618478877661 ) ) ;
#4715=CARTESIAN_POINT ( 'NONE',  ( 0.1306872919485614071, -0.3155070326520293955, 0.02756944444444603404 ) ) ;
#4716=CARTESIAN_POINT ( 'NONE',  ( 0.1961921601747127764, 0.4279942808755098915, 0.09139393128962811086 ) ) ;
#4720=CARTESIAN_POINT ( 'NONE',  ( -0.1954553509668046918, -0.1954553509668046640, -0.008888888888887799475 ) ) ;
#4722=CARTESIAN_POINT ( 'NONE',  ( 0.1294417382415921358, -0.3125000000000002220, 0.07791666666666827168 ) ) ;
#4723=CARTESIAN_POINT ( 'NONE',  ( -0.2764156081756484196, 1.692557448933383907E-17, 0.3730555555555596925 ) ) ;
#4732=DIRECTION ( 'NONE',  ( 1.000000000000000000, 0.000000000000000000, 0.000000000000000000 ) ) ;
#4734=ORIENTED_EDGE ( 'NONE', *, *, #11843, .F. ) ;
#4736=CARTESIAN_POINT ( 'NONE',  ( 0.1294417382415924134, 0.3124999999999999445, 0.1056944444444466308 ) ) ;
#4741=CARTESIAN_POINT ( 'NONE',  ( 0.03762146087705321024, 0.5076544266709851483, 0.4065068718547070747 ) ) ;
#4742=CARTESIAN_POINT ( 'NONE',  ( -0.2764156081756484196, 1.692557448933383907E-17, -0.07833333333333278303 ) ) ;
#4746=CARTESIAN_POINT ( 'NONE',  ( -0.3125000000000000000, 1.913510623667739771E-17, 0.2827777777777810142 ) ) ;
#4747=CARTESIAN_POINT ( 'NONE',  ( -0.1954553509668046640, 0.1954553509668046918, 0.1994444444444471720 ) ) ;
#4750=CARTESIAN_POINT ( 'NONE',  ( -0.2663714005177904576, 0.1275804160634904094, 0.4068622647240436319 ) ) ;
#4751=DIRECTION ( 'NONE',  ( -0.000000000000000000, -0.000000000000000000, 1.000000000000000000 ) ) ;
#4754=CARTESIAN_POINT ( 'NONE',  ( -0.1306872919485615459, -0.3155070326520293400, 0.2949305555555589153 ) ) ;
#4756=CARTESIAN_POINT ( 'NONE',  ( -0.3125000000000000000, 1.913510623667739771E-17, 0.3938888888888930628 ) ) ;
#4767=CARTESIAN_POINT ( 'NONE',  ( 0.6396424860381280109, 7.834898727884920884E-17, -0.01143517789850382292 ) ) ;
#4783=DIRECTION ( 'NONE',  ( -0.4999999999999990008, 0.8660254037844391517, -9.106159978880873451E-16 ) ) ;
#4786=LINE ( 'NONE', #5146, #10466 ) ;
#4787=CARTESIAN_POINT ( 'NONE',  ( 0.01848103877824613592, -0.5441716683897390716, 0.04413116910601658227 ) ) ;
#4792=CARTESIAN_POINT ( 'NONE',  ( 0.3125000000000000000, -5.740531871003217465E-17, 0.3730555555555599145 ) ) ;
#4793=B_SPLINE_CURVE_WITH_KNOTS ( 'NONE', 3,
 ( #8922, #20616, #3916, #7216, #14930, #517, #9802, #22711, #13233, #11510, #13115, #13468, #9675, #11753, #16752, #20885, #17112, #158, #11386, #3826, #18818, #21004, #22835, #2112, #5771, #9553, #7482, #22349, #4177, #7953, #7718, #20531, #15052, #18945 ),
 .UNSPECIFIED., .F., .F.,
 ( 4, 2, 2, 2, 2, 2, 2, 2, 2, 2, 2, 2, 2, 2, 2, 2, 4 ),
 ( 0.02754951627422265806, 0.02882399678900620515, 0.03009847730378974878, 0.03137295781857329935, 0.03264743833335684298, 0.03392191884814039354, 0.03519639936292394411, 0.03647087987770748774, 0.03774536039249104524, 0.03901984090727458887, 0.04029432142205813944, 0.04156880193684169000, 0.04284328245162523363, 0.04411776296640878420, 0.04539224348119233476, 0.04666672399597587839, 0.04794120451075942896 ),
 .UNSPECIFIED. ) ;
#4797=CIRCLE ( 'NONE', #18430, 0.01874999999999999237 ) ;
#4798=EDGE_CURVE ( 'NONE', #175, #16785, #21737, .T. ) ;
#4801=ORIENTED_EDGE ( 'NONE', *, *, #2887, .T. ) ;
#4804=ORIENTED_EDGE ( 'NONE', *, *, #20816, .T. ) ;
#4810=CARTESIAN_POINT ( 'NONE',  ( -0.4687500000000003886, -0.1119141212732240320, 0.4216323756266210920 ) ) ;
#4815=CARTESIAN_POINT ( 'NONE',  ( -0.1144950937579609779, 0.2764156081756484196, 0.1334722222222244348 ) ) ;
#4830=CARTESIAN_POINT ( 'NONE',  ( -0.1338087529395441955, -0.2734308413694009343, 0.4156188565751802733 ) ) ;
#4832=CARTESIAN_POINT ( 'NONE',  ( -0.3155070326520293400, -0.1306872919485614626, 0.01368055555555705224 ) ) ;
#4839=DIRECTION ( 'NONE',  ( 1.000000000000000000, 0.000000000000000000, 0.000000000000000000 ) ) ;
#4840=CARTESIAN_POINT ( 'NONE',  ( 0.2764156081756483641, -0.1144950937579611167, 0.06402777777777945989 ) ) ;
#4841=CARTESIAN_POINT ( 'NONE',  ( 0.4805070082343983473, -0.2560807851245830435, 0.04413116910601658921 ) ) ;
#4843=CARTESIAN_POINT ( 'NONE',  ( -0.2764156081756484196, 1.692557448933383907E-17, 0.3175000000000036682 ) ) ;
#4845=CARTESIAN_POINT ( 'NONE',  ( -0.3125000000000000000, 1.913510623667739771E-17, 0.005000000000001014917 ) ) ;
#4857=VERTEX_POINT ( 'NONE', #15340 ) ;
#4865=CARTESIAN_POINT ( 'NONE',  ( -0.1954553509668046918, -0.1954553509668046640, -0.01583333333333228690 ) ) ;
#4870=CARTESIAN_POINT ( 'NONE',  ( -0.2764156081756484196, 0.1144950937579609918, 0.2029166666666694097 ) ) ;
#4874=CARTESIAN_POINT ( 'NONE',  ( -0.2973707438694075944, 0.01885122216165719539, 0.4090374105360744528 ) ) ;
#4876=CARTESIAN_POINT ( 'NONE',  ( -0.2723623684625769426, 0.3840173906162817064, 0.09139303015897914939 ) ) ;
#4877=CARTESIAN_POINT ( 'NONE',  ( -3.385114897866767815E-17, -0.2764156081756484196, -0.06444444444444379083 ) ) ;
#4878=CARTESIAN_POINT ( 'NONE',  ( 0.2230971623002953874, -0.2230971623002954429, 0.3053472222222256005 ) ) ;
#4905=EDGE_LOOP ( 'NONE', ( #17407, #17243, #6803, #7105, #20292 ) ) ;
#4919=CARTESIAN_POINT ( 'NONE',  ( 0.4687500000000003886, -0.04388698013647539253, 0.09139229829490853885 ) ) ;
#4921=CARTESIAN_POINT ( 'NONE',  ( -0.4788479876972301374, -0.2689986204937560021, 0.04193567535760926723 ) ) ;
#4929=CARTESIAN_POINT ( 'NONE',  ( -0.4209440094115188824, -0.2863418823927886270, 0.4064695056028755915 ) ) ;
#4935=CARTESIAN_POINT ( 'NONE',  ( -0.4687500000000003886, -0.04441404256795419142, 0.4171848040509457123 ) ) ;
#4941=CARTESIAN_POINT ( 'NONE',  ( -0.2764156081756484196, 1.692557448933383907E-17, 0.08833333333333522053 ) ) ;
#4943=CARTESIAN_POINT ( 'NONE',  ( -0.2209708691207961373, -0.2209708691207961095, 0.4008333333333374826 ) ) ;
#4949=AXIS2_PLACEMENT_3D ( 'NONE', #10537, #23554, #21498 ) ;
#4954=CARTESIAN_POINT ( 'NONE',  ( 0.3155070326520292290, 0.1306872919485615736, -0.06965277777777696688 ) ) ;
#4955=DIRECTION ( 'NONE',  ( -0.4999999999999995559, 0.8660254037844389297, 0.000000000000000000 ) ) ;
#4957=ADVANCED_FACE ( 'NONE', ( #13400 ), #19407, .T. ) ;
#4960=CARTESIAN_POINT ( 'NONE',  ( 0.1144950937579611444, 0.2764156081756483641, -0.03319444444444354797 ) ) ;
#4963=CARTESIAN_POINT ( 'NONE',  ( -3.385114897866767815E-17, -0.2764156081756484196, 0.3313888888888926743 ) ) ;
#4971=CARTESIAN_POINT ( 'NONE',  ( 0.000000000000000000, 3.738758431839877614E-19, -0.1145082521472477743 ) ) ;
#4977=CARTESIAN_POINT ( 'NONE',  ( 0.4593750000000003664, -0.2760455974562899817, 0.06112444011295372487 ) ) ;
#4983=CARTESIAN_POINT ( 'NONE',  ( 0.1144950937579609085, -0.2764156081756484751, 0.1056944444444464504 ) ) ;
#4986=ADVANCED_FACE ( 'NONE', ( #11892 ), #9438, .T. ) ;
#4987=DIRECTION ( 'NONE',  ( -0.5000000000000012212, 0.8660254037844380415, 0.000000000000000000 ) ) ;
#4988=CARTESIAN_POINT ( 'NONE',  ( 0.1954553509668046640, -0.1954553509668047195, 0.2272222222222252119 ) ) ;
#4991=CARTESIAN_POINT ( 'NONE',  ( -0.09987075367823573802, 0.2738295200956166187, 0.4025228681615854454 ) ) ;
#4992=CARTESIAN_POINT ( 'NONE',  ( -0.4796770409652741929, 0.08628438008767304324, 0.07157438297392351712 ) ) ;
#4993=CARTESIAN_POINT ( 'NONE',  ( 0.000000000000000000, 3.738758431839877614E-19, 0.000000000000000000 ) ) ;
#4994=CARTESIAN_POINT ( 'NONE',  ( -0.2764156081756484196, 0.1144950937579609918, 0.08486111111111295513 ) ) ;
#4995=CARTESIAN_POINT ( 'NONE',  ( -0.2230971623002953874, 0.2230971623002954152, 0.3331250000000036127 ) ) ;
#5004=ORIENTED_EDGE ( 'NONE', *, *, #15741, .F. ) ;
#5038=DIRECTION ( 'NONE',  ( -1.224646799147353207E-16, 1.000000000000000000, 0.000000000000000000 ) ) ;
#5052=CARTESIAN_POINT ( 'NONE',  ( -0.4593750000000004219, -0.2760455974562901482, 0.4425000000000000044 ) ) ;
#5058=CARTESIAN_POINT ( 'NONE',  ( -3.385114897866767815E-17, -0.2764156081756484196, 0.1022222222222241989 ) ) ;
#5066=CONICAL_SURFACE ( 'NONE', #10161, 0.6391249999999999432, 1.134464013796309345 ) ;
#5071=CARTESIAN_POINT ( 'NONE',  ( 0.1306872919485616846, 0.3155070326520292290, 0.3261805555555595260 ) ) ;
#5072=DIRECTION ( 'NONE',  ( 0.8320502943378442762, 0.4803844614152616432, -0.2773500981126125198 ) ) ;
#5073=CARTESIAN_POINT ( 'NONE',  ( -0.4223136544080929311, -0.2974429753103077223, 0.07050986311825914454 ) ) ;
#5075=CIRCLE ( 'NONE', #8197, 0.01874999999999997502 ) ;
#5077=CIRCLE ( 'NONE', #1214, 0.4453125000000000000 ) ;
#5079=CARTESIAN_POINT ( 'NONE',  ( -0.1144950937579609918, -0.2764156081756484196, 0.1056944444444464504 ) ) ;
#5082=EDGE_LOOP ( 'NONE', ( #14987, #4449, #1532 ) ) ;
#5086=CARTESIAN_POINT ( 'NONE',  ( -0.4772460259542071759, 0.2717629240624621079, 0.04193793378272828859 ) ) ;
#5102=CARTESIAN_POINT ( 'NONE',  ( -0.1954553509668046918, -0.1954553509668046640, 0.2063888888888917028 ) ) ;
#5109=CARTESIAN_POINT ( 'NONE',  ( 0.4687500000000002220, 0.1725658479149915492, 0.06591615843556912491 ) ) ;
#5112=CARTESIAN_POINT ( 'NONE',  ( 0.1144950937579611444, 0.2764156081756483641, 0.07097222222222394905 ) ) ;
#5113=CARTESIAN_POINT ( 'NONE',  ( 0.2230971623002953874, -0.2230971623002954429, 0.3609027777777815693 ) ) ;
#5143=CYLINDRICAL_SURFACE ( 'NONE', #10018, 0.3125000000000000000 ) ;
#5146=CARTESIAN_POINT ( 'NONE',  ( -0.3125000000000000000, 0.000000000000000000, 1.326383476483184332 ) ) ;
#5148=CARTESIAN_POINT ( 'NONE',  ( 0.3124999999999996669, 0.04488961648801697429, 0.4228708124548387071 ) ) ;
#5150=CARTESIAN_POINT ( 'NONE',  ( -0.3125000000000000000, 0.000000000000000000, 1.326383476483184332 ) ) ;
#5156=CARTESIAN_POINT ( 'NONE',  ( 0.4687500000000003886, -0.1740109699597048587, 0.07813294176666470137 ) ) ;
#5159=ORIENTED_EDGE ( 'NONE', *, *, #13931, .F. ) ;
#5175=DIRECTION ( 'NONE',  ( -1.000000000000000000, 0.000000000000000000, 0.000000000000000000 ) ) ;
#5179=DIRECTION ( 'NONE',  ( 0.8320502943378449423, -0.4803844614152608106, -0.2773500981126125753 ) ) ;
#5180=CARTESIAN_POINT ( 'NONE',  ( 0.1954553509668046640, -0.1954553509668047195, 0.3869444444444487541 ) ) ;
#5183=CARTESIAN_POINT ( 'NONE',  ( 0.2464202454315519986, -0.1619151084083290393, 0.4060090615677847126 ) ) ;
#5193=CARTESIAN_POINT ( 'NONE',  ( -3.863846776457871776E-17, -0.3155070326520292845, 0.3574305555555597480 ) ) ;
#5195=CARTESIAN_POINT ( 'NONE',  ( 0.04345060704002973867, -0.5161796576941667380, 0.4013192973758499815 ) ) ;
#5198=CARTESIAN_POINT ( 'NONE',  ( 0.1144950937579609085, -0.2764156081756484751, 0.3348611111111148841 ) ) ;
#5219=EDGE_CURVE ( 'NONE', #4062, #9702, #1180, .T. ) ;
#5220=CARTESIAN_POINT ( 'NONE',  ( 0.2764156081756483641, 0.1144950937579610056, 0.2306944444444475328 ) ) ;
#5224=DIRECTION ( 'NONE',  ( 0.000000000000000000, 0.000000000000000000, -1.000000000000000000 ) ) ;
#5233=CARTESIAN_POINT ( 'NONE',  ( 0.2764156081756483641, 0.1144950937579610195, 0.06402777777777945989 ) ) ;
#5234=CARTESIAN_POINT ( 'NONE',  ( 0.2764156081756483641, -0.1144950937579611167, 0.06402777777777945989 ) ) ;
#5236=ORIENTED_EDGE ( 'NONE', *, *, #9382, .T. ) ;
#5246=CARTESIAN_POINT ( 'NONE',  ( 0.000000000000000000, 1.869379215919938807E-19, -0.01219352927422984872 ) ) ;
#5277=( BOUNDED_SURFACE ( )  B_SPLINE_SURFACE ( 3, 2, ( 
 ( #12665, #7404, #22389 ),
 ( #19964, #12910, #14732 ),
 ( #10946, #14603, #16669 ),
 ( #20085, #20325, #22149 ),
 ( #3375, #5691, #11188 ),
 ( #1669, #75, #14481 ),
 ( #7519, #22269, #23718 ),
 ( #3613, #10827, #18373 ),
 ( #24093, #23972, #14853 ),
 ( #5567, #9101, #18137 ),
 ( #3251, #5195, #9352 ),
 ( #13031, #20447, #18254 ) ),
 .UNSPECIFIED., .F., .F., .F. ) 
 B_SPLINE_SURFACE_WITH_KNOTS ( ( 4, 2, 2, 2, 2, 4 ),
 ( 3, 3 ),
 ( 0.001926919177646337121, 0.005264799389783187192, 0.006933739495851611902, 0.008602679601920036612, 0.01194055981405688603, 0.01527844002619373545 ),
 ( 0.000000000000000000, 1.000000000000000000 ),
 .UNSPECIFIED. ) 
 GEOMETRIC_REPRESENTATION_ITEM ( )  RATIONAL_B_SPLINE_SURFACE ( (
 ( 1.000000000000000000, 0.8464669816041905381, 1.000000000000000000),
 ( 1.000000000000000000, 0.8516517675253441055, 1.000000000000000000),
 ( 1.000000000000000000, 0.8565844288627803005, 1.000000000000000000),
 ( 1.000000000000000000, 0.8620057511681040729, 1.000000000000000000),
 ( 1.000000000000000000, 0.8634777350186887412, 1.000000000000000000),
 ( 1.000000000000000000, 0.8654907715253831180, 1.000000000000000000),
 ( 1.000000000000000000, 0.8660271740516733985, 1.000000000000000000),
 ( 1.000000000000000000, 0.8660218497377574209, 1.000000000000000000),
 ( 1.000000000000000000, 0.8638283365559311644, 1.000000000000000000),
 ( 1.000000000000000000, 0.8566178551151195641, 1.000000000000000000),
 ( 1.000000000000000000, 0.8516788886408952486, 1.000000000000000000),
 ( 1.000000000000000000, 0.8464669816041903161, 1.000000000000000000) ) ) 
 REPRESENTATION_ITEM ( '' )  SURFACE ( )  );
#5295=CARTESIAN_POINT ( 'NONE',  ( -0.004657599350067381447, -0.3068592482405227972, 0.4181016929859454612 ) ) ;
#5308=CARTESIAN_POINT ( 'NONE',  ( -0.1954553509668046640, 0.1954553509668046918, 0.1925000000000027245 ) ) ;
#5311=CARTESIAN_POINT ( 'NONE',  ( 0.1219426170921238256, -0.2560469716180380773, 0.3947246446402559727 ) ) ;
#5317=B_SPLINE_CURVE_WITH_KNOTS ( 'NONE', 3,
 ( #21217, #8043, #4270, #11845, #2451, #17204, #19262, #4386, #8161, #6336, #11972, #19386 ),
 .UNSPECIFIED., .F., .F.,
 ( 4, 2, 2, 2, 2, 4 ),
 ( 0.000000000000000000, 0.003345931539952394333, 0.005018897309928594536, 0.006691863079904794738, 0.01003779461985718734, 0.01338372615980958080 ),
 .UNSPECIFIED. ) ;
#5322=CARTESIAN_POINT ( 'NONE',  ( -0.2230971623002954152, -0.2230971623002953874, 0.3504861111111152727 ) ) ;
#5328=CARTESIAN_POINT ( 'NONE',  ( 0.2764156081756483641, -0.1144950937579611167, 0.3418055555555594704 ) ) ;
#5331=VERTEX_POINT ( 'NONE', #4691 ) ;
#5348=CARTESIAN_POINT ( 'NONE',  ( 0.1954553509668047195, 0.1954553509668046085, 0.2341666666666697150 ) ) ;
#5349=AXIS2_PLACEMENT_3D ( 'NONE', #2906, #19979, #4732 ) ;
#5352=EDGE_CURVE ( 'NONE', #11791, #9081, #322, .T. ) ;
#5353=CARTESIAN_POINT ( 'NONE',  ( -0.1144950937579609918, -0.2764156081756484196, 0.3279166666666704089 ) ) ;
#5358=DIRECTION ( 'NONE',  ( -0.000000000000000000, -0.000000000000000000, -1.000000000000000000 ) ) ;
#5359=CARTESIAN_POINT ( 'NONE',  ( 0.1144950937579609085, -0.2764156081756484751, -0.1095833333333330467 ) ) ;
#5361=EDGE_LOOP ( 'NONE', ( #11511, #11519, #5540, #2190, #15512, #9143, #10483 ) ) ;
#5363=B_SPLINE_CURVE_WITH_KNOTS ( 'NONE', 3,
 ( #3261, #1202, #6929, #23374, #1320, #12315 ),
 .UNSPECIFIED., .F., .F.,
 ( 4, 2, 4 ),
 ( 0.006804048971101872567, 0.01020032888717190694, 0.01359660880324194132 ),
 .UNSPECIFIED. ) ;
#5364=CARTESIAN_POINT ( 'NONE',  ( 0.4687500000000002776, 0.1753644386825057300, 0.4001479654036551592 ) ) ;
#5377=CARTESIAN_POINT ( 'NONE',  ( 0.4593750000000003664, 0.2760455974562901482, 0.4425000000000000044 ) ) ;
#5381=ORIENTED_EDGE ( 'NONE', *, *, #5497, .T. ) ;
#5392=CARTESIAN_POINT ( 'NONE',  ( -0.2230971623002953874, 0.2230971623002954152, -0.0002083333333323692741 ) ) ;
#5414=CARTESIAN_POINT ( 'NONE',  ( -0.2980062158858403643, -0.01674720435929506757, 0.4096728825525073336 ) ) ;
#5416=CARTESIAN_POINT ( 'NONE',  ( 0.4687500000000002776, 0.2598076211353318454, 0.3779506566538942125 ) ) ;
#5419=CARTESIAN_POINT ( 'NONE',  ( -0.3125000000000000000, 0.000000000000000000, 1.326383476483184332 ) ) ;
#5420=FACE_OUTER_BOUND ( 'NONE', #2943, .T. ) ;
#5423=( BOUNDED_CURVE ( )  B_SPLINE_CURVE ( 2, ( #152, #7833, #2237, #2357, #5996, #2477, #9797, #22941, #17344 ),
 .UNSPECIFIED., .F., .T. ) 
 B_SPLINE_CURVE_WITH_KNOTS ( ( 3, 2, 2, 2, 3 ),
 ( 0.1979166666666667129, 0.2083333333333333703, 0.2187500000000000000, 0.2291666666666667684, 0.2395833333333334259 ),
 .UNSPECIFIED. ) 
 CURVE ( )  GEOMETRIC_REPRESENTATION_ITEM ( )  RATIONAL_B_SPLINE_CURVE ( ( 1.000000000000000222, 0.9238795325112865164, 1.000000000000000000, 0.9238795325112867385, 1.000000000000000000, 0.9238795325112867385, 1.000000000000000000, 0.9238795325112862944, 1.000000000000000444 ) ) 
 REPRESENTATION_ITEM ( '' )  );
#5427=ORIENTED_EDGE ( 'NONE', *, *, #467, .T. ) ;
#5429=CARTESIAN_POINT ( 'NONE',  ( 0.2764156081756484196, -5.077672346800151106E-17, 0.2272222222222252119 ) ) ;
#5432=EDGE_CURVE ( 'NONE', #9081, #21037, #22514, .T. ) ;
#5444=CARTESIAN_POINT ( 'NONE',  ( -0.1306872919485615459, -0.3155070326520293400, 0.1872916666666696039 ) ) ;
#5446=FACE_OUTER_BOUND ( 'NONE', #10910, .T. ) ;
#5450=CARTESIAN_POINT ( 'NONE',  ( 0.1954553509668047195, 0.1954553509668046085, 0.1855555555555581937 ) ) ;
#5453=ORIENTED_EDGE ( 'NONE', *, *, #13328, .T. ) ;
#5458=FACE_OUTER_BOUND ( 'NONE', #8872, .T. ) ;
#5460=CARTESIAN_POINT ( 'NONE',  ( -0.4620259694561524855, 0.2880908832651556950, 0.04413116910601659615 ) ) ;
#5472=CARTESIAN_POINT ( 'NONE',  ( -0.05455304208351747369, -0.2715891510243036988, -0.06558227484231508864 ) ) ;
#5474=CARTESIAN_POINT ( 'NONE',  ( 0.2764156081756484196, -5.077672346800151106E-17, 0.3383333333333372051 ) ) ;
#5476=CARTESIAN_POINT ( 'NONE',  ( 0.000000000000000000, 3.738758431839877614E-19, -0.1016666666666665164 ) ) ;
#5484=CARTESIAN_POINT ( 'NONE',  ( -0.2764156081756484196, 0.1144950937579609918, -0.07486111111111054539 ) ) ;
#5492=DIRECTION ( 'NONE',  ( 0.7071067811865435759, 0.000000000000000000, 0.7071067811865514585 ) ) ;
#5494=VECTOR ( 'NONE', #9758, 39.37007874015748854 ) ;
#5495=ORIENTED_EDGE ( 'NONE', *, *, #14837, .T. ) ;
#5497=EDGE_CURVE ( 'NONE', #10448, #13469, #15350, .T. ) ;
#5505=CARTESIAN_POINT ( 'NONE',  ( -0.4641461581055078001, 0.2728099291808048221, 0.04698409998689238865 ) ) ;
#5508=ORIENTED_EDGE ( 'NONE', *, *, #23008, .T. ) ;
#5509=ORIENTED_EDGE ( 'NONE', *, *, #13293, .F. ) ;
#5511=LINE ( 'NONE', #11128, #7265 ) ;
#5514=CARTESIAN_POINT ( 'NONE',  ( -0.2230971623002954152, -0.2230971623002953874, 0.01368055555555662377 ) ) ;
#5515=CARTESIAN_POINT ( 'NONE',  ( -0.4206476797389064881, -0.2984048262340653901, 0.05816208736403803703 ) ) ;
#5536=PLANE ( 'NONE',  #6547 ) ;
#5540=ORIENTED_EDGE ( 'NONE', *, *, #15845, .T. ) ;
#5542=LINE ( 'NONE', #5052, #6255 ) ;
#5547=CARTESIAN_POINT ( 'NONE',  ( 0.000000000000000000, 0.2764156081756484196, 0.3522222222222262111 ) ) ;
#5555=VECTOR ( 'NONE', #19606, 39.37007874015748143 ) ;
#5559=CARTESIAN_POINT ( 'NONE',  ( -0.4687500000000004441, 0.2922835737772480069, 0.06112444011295372487 ) ) ;
#5562=( BOUNDED_CURVE ( )  B_SPLINE_CURVE ( 2, ( #5988, #16, #5636, #22581, #20514, #7464, #9418, #20629, #266 ),
 .UNSPECIFIED., .F., .T. ) 
 B_SPLINE_CURVE_WITH_KNOTS ( ( 3, 2, 2, 2, 3 ),
 ( 0.6145833333333333703, 0.6250000000000000000, 0.6354166666666667407, 0.6458333333333334814, 0.6562500000000001110 ),
 .UNSPECIFIED. ) 
 CURVE ( )  GEOMETRIC_REPRESENTATION_ITEM ( )  RATIONAL_B_SPLINE_CURVE ( ( 1.000000000000000000, 0.9238795325112867385, 1.000000000000000000, 0.9238795325112867385, 1.000000000000000000, 0.9238795325112867385, 1.000000000000000000, 0.9238795325112859613, 1.000000000000000888 ) ) 
 REPRESENTATION_ITEM ( '' )  );
#5563=CARTESIAN_POINT ( 'NONE',  ( 0.2230971623002954429, 0.2230971623002953319, 0.2115972222222252952 ) ) ;
#5567=CARTESIAN_POINT ( 'NONE',  ( 0.07520958173006334069, -0.4863159908245684449, 0.4165421425001717415 ) ) ;
#5570=CARTESIAN_POINT ( 'NONE',  ( -0.1954553509668046918, -0.1954553509668046640, 0.2688888888888921747 ) ) ;
#5580=CARTESIAN_POINT ( 'NONE',  ( 0.000000000000000000, 0.000000000000000000, 1.326383476483184332 ) ) ;
#5584=ORIENTED_EDGE ( 'NONE', *, *, #21938, .T. ) ;
#5587=CARTESIAN_POINT ( 'NONE',  ( 0.3853713378992902894, 0.3187716316911530789, 0.07807775719021836647 ) ) ;
#5589=ADVANCED_FACE ( 'NONE', ( #3949 ), #5536, .F. ) ;
#5590=CARTESIAN_POINT ( 'NONE',  ( 0.1144950937579609085, -0.2764156081756484751, 0.2168055555555584712 ) ) ;
#5599=CARTESIAN_POINT ( 'NONE',  ( 0.1144950937579611444, 0.2764156081756483641, -0.03319444444444354797 ) ) ;
#5604=CARTESIAN_POINT ( 'NONE',  ( 0.4687500000000003331, -0.2209812308046625595, 0.4011722195456132734 ) ) ;
#5610=LINE ( 'NONE', #20490, #10053 ) ;
#5620=DIRECTION ( 'NONE',  ( 0.8320502943378454974, -0.4803844614152598114, 0.2773500981126120757 ) ) ;
#5624=CARTESIAN_POINT ( 'NONE',  ( -0.4645997322663009688, 0.2720228281466814391, 0.05892894635879200593 ) ) ;
#5628=VERTEX_POINT ( 'NONE', #5416 ) ;
#5631=DIRECTION ( 'NONE',  ( 0.000000000000000000, 0.000000000000000000, -1.000000000000000000 ) ) ;
#5634=CARTESIAN_POINT ( 'NONE',  ( 0.2230971623002954429, 0.2230971623002953319, -0.01409722222222137972 ) ) ;
#5636=CARTESIAN_POINT ( 'NONE',  ( 0.2209708691207961095, -0.2209708691207961651, 0.03277777777777939050 ) ) ;
#5646=CARTESIAN_POINT ( 'NONE',  ( -0.3146277125502374705, 0.3722332453489713422, 0.07156651416104445329 ) ) ;
#5653=ORIENTED_EDGE ( 'NONE', *, *, #6637, .T. ) ;
#5673=CARTESIAN_POINT ( 'NONE',  ( 0.3006586688675964014, -0.04349558104366376549, 0.4153305990016259441 ) ) ;
#5690=AXIS2_PLACEMENT_3D ( 'NONE', #7691, #4271, #20736 ) ;
#5691=CARTESIAN_POINT ( 'NONE',  ( 0.3118573088780851599, -0.3612149761357442146, 0.4243809486557439392 ) ) ;
#5692=DIRECTION ( 'NONE',  ( -1.000000000000000000, 0.000000000000000000, 0.000000000000000000 ) ) ;
#5693=CARTESIAN_POINT ( 'NONE',  ( 0.1954553509668046640, -0.1954553509668047195, -0.001944444444443294917 ) ) ;
#5695=CARTESIAN_POINT ( 'NONE',  ( 0.1144950937579611444, 0.2764156081756483641, 0.3001388888888924522 ) ) ;
#5716=EDGE_CURVE ( 'NONE', #7699, #18597, #16875, .T. ) ;
#5718=CARTESIAN_POINT ( 'NONE',  ( -0.2764156081756484196, -0.1144950937579609362, 0.4251388888888933959 ) ) ;
#5721=ORIENTED_EDGE ( 'NONE', *, *, #20732, .F. ) ;
#5723=CIRCLE ( 'NONE', #1814, 0.4453125000000000000 ) ;
#5728=CARTESIAN_POINT ( 'NONE',  ( -0.1954553509668046918, -0.1954553509668046640, -0.06444444444444380471 ) ) ;
#5730=CARTESIAN_POINT ( 'NONE',  ( 0.4593405033095763201, 0.04515253527788225252, 0.4334345840242775361 ) ) ;
#5733=EDGE_LOOP ( 'NONE', ( #1881, #2952, #21768, #17828 ) ) ;
#5744=( CONVERSION_BASED_UNIT ( 'INCH', #7690 ) LENGTH_UNIT ( ) NAMED_UNIT ( #11808 ) );
#5749=CARTESIAN_POINT ( 'NONE',  ( -0.1144950937579609918, -0.2764156081756484196, 0.05013888888889046075 ) ) ;
#5754=DIRECTION ( 'NONE',  ( 1.000000000000000000, 0.000000000000000000, 0.000000000000000000 ) ) ;
#5755=CARTESIAN_POINT ( 'NONE',  ( 0.3125000000000000000, -5.740531871003217465E-17, 0.1994444444444470055 ) ) ;
#5757=CARTESIAN_POINT ( 'NONE',  ( 0.1306872919485616846, 0.3155070326520292290, -0.06618055555555513170 ) ) ;
#5758=CARTESIAN_POINT ( 'NONE',  ( -0.08494034609768597033, -0.4922255456807479446, 0.06591861138174437418 ) ) ;
#5759=CARTESIAN_POINT ( 'NONE',  ( -0.2800968539712042626, 1.715098578335394762E-17, -0.06926352063787094560 ) ) ;
#5771=CARTESIAN_POINT ( 'NONE',  ( -0.1111235690147887867, -0.2883545979861809605, -0.09773750720628669730 ) ) ;
#5787=CARTESIAN_POINT ( 'NONE',  ( 0.2764156081756483641, 0.1144950937579610056, 0.3973611111111154393 ) ) ;
#5800=ORIENTED_EDGE ( 'NONE', *, *, #8889, .F. ) ;
#5802=CARTESIAN_POINT ( 'NONE',  ( 0.4593750000000003664, 0.2760455974562900372, 0.06112444011295369711 ) ) ;
#5808=CARTESIAN_POINT ( 'NONE',  ( 0.000000000000000000, 0.2764156081756484196, 0.1855555555555581937 ) ) ;
#5810=CARTESIAN_POINT ( 'NONE',  ( -0.1144950937579609918, -0.2764156081756484196, 0.4390277777777824020 ) ) ;
#5815=CARTESIAN_POINT ( 'NONE',  ( 0.3125000000000000000, -5.740531871003217465E-17, 0.3661111111111149397 ) ) ;
#5824=TOROIDAL_SURFACE ( 'NONE', #23713, -0.5601250000000235207, 1.200750000000023521 ) ;
#5829=CARTESIAN_POINT ( 'NONE',  ( -0.2764156081756484196, -0.1144950937579609362, 0.3695833333333374826 ) ) ;
#5833=AXIS2_PLACEMENT_3D ( 'NONE', #7666, #17626, #20592 ) ;
#5838=CARTESIAN_POINT ( 'NONE',  ( 0.000000000000000000, 0.2764156081756484196, -0.1408333333333332826 ) ) ;
#5840=CARTESIAN_POINT ( 'NONE',  ( 0.1584465904743050102, 0.4497866957027559787, 0.4135550951626319471 ) ) ;
#5841=CARTESIAN_POINT ( 'NONE',  ( -0.1144950937579609779, 0.2764156081756484196, 0.1959722222222249899 ) ) ;
#5858=CARTESIAN_POINT ( 'NONE',  ( -0.1144950937579609779, 0.2764156081756484196, -0.1443055555555555203 ) ) ;
#5861=CARTESIAN_POINT ( 'NONE',  ( -0.1954553509668046640, 0.1954553509668046918, -0.02277777777777679341 ) ) ;
#5868=CARTESIAN_POINT ( 'NONE',  ( 0.3155070326520292290, 0.1306872919485615736, 0.09354166666666836882 ) ) ;
#5879=CARTESIAN_POINT ( 'NONE',  ( -0.2209708691207961095, 0.2209708691207961373, 0.1091666666666684937 ) ) ;
#5884=VECTOR ( 'NONE', #9444, 39.37007874015748143 ) ;
#5886=VERTEX_POINT ( 'NONE', #14424 ) ;
#5887=CARTESIAN_POINT ( 'NONE',  ( 0.2525416622817170942, 0.1285646679930055047, 0.3944156602770289566 ) ) ;
#5891=ORIENTED_EDGE ( 'NONE', *, *, #8761, .T. ) ;
#5896=CARTESIAN_POINT ( 'NONE',  ( 0.3253415854805812857, 4.021672897201586740E-17, -0.1145082521472477743 ) ) ;
#5897=CARTESIAN_POINT ( 'NONE',  ( 0.1504789989860620958, 0.4433647533406533392, 0.4295860435587880999 ) ) ;
#5898=DIRECTION ( 'NONE',  ( 1.000000000000000000, 0.000000000000000000, 0.000000000000000000 ) ) ;
#5905=CARTESIAN_POINT ( 'NONE',  ( 0.1144950937579611444, 0.2764156081756483641, 0.4598611111111159389 ) ) ;
#5916=VERTEX_POINT ( 'NONE', #1727 ) ;
#5917=VERTEX_POINT ( 'NONE', #12730 ) ;
#5924=CARTESIAN_POINT ( 'NONE',  ( 0.003269416932269875696, -0.5491886443627421732, 0.04193793378272824696 ) ) ;
#5926=CARTESIAN_POINT ( 'NONE',  ( 0.1954553509668046640, -0.1954553509668047195, 0.2202777777777807366 ) ) ;
#5928=CARTESIAN_POINT ( 'NONE',  ( -0.1144950937579609779, 0.2764156081756484196, 0.4737500000000048894 ) ) ;
#5949=CARTESIAN_POINT ( 'NONE',  ( 0.1306872919485614071, -0.3155070326520293955, -0.08354166666666594521 ) ) ;
#5951=EDGE_LOOP ( 'NONE', ( #18918, #18174, #5800, #8437 ) ) ;
#5956=CARTESIAN_POINT ( 'NONE',  ( -0.1144950937579609779, 0.2764156081756484196, 0.1404166666666689378 ) ) ;
#5957=B_SPLINE_CURVE_WITH_KNOTS ( 'NONE', 3,
 ( #12819, #11092, #12572, #5924, #18981, #22058, #1811, #20115 ),
 .UNSPECIFIED., .F., .F.,
 ( 4, 2, 2, 4 ),
 ( 0.000000000000000000, 0.0004997454757086389372, 0.0007496182135629584058, 0.0009994909514172778744 ),
 .UNSPECIFIED. ) ;
#5967=VERTEX_POINT ( 'NONE', #14669 ) ;
#5980=CARTESIAN_POINT ( 'NONE',  ( 0.2764156081756483641, 0.1144950937579610195, 0.01541666666666794208 ) ) ;
#5987=CARTESIAN_POINT ( 'NONE',  ( 0.000000000000000000, 0.3155070326520292845, 0.2706250000000031131 ) ) ;
#5988=CARTESIAN_POINT ( 'NONE',  ( 0.3125000000000000000, -5.740531871003217465E-17, 0.03972222222222387966 ) ) ;
#5996=CARTESIAN_POINT ( 'NONE',  ( -3.827021247335479543E-17, -0.3125000000000000000, 0.3036111111111148841 ) ) ;
#5997=ORIENTED_EDGE ( 'NONE', *, *, #8670, .F. ) ;
#5998=CARTESIAN_POINT ( 'NONE',  ( -0.009375000000000069042, 0.5358532185916218271, 0.06112444011295372487 ) ) ;
#6007=DIRECTION ( 'NONE',  ( -1.000000000000000000, 0.000000000000000000, 0.000000000000000000 ) ) ;
#6009=VERTEX_POINT ( 'NONE', #20385 ) ;
#6013=CARTESIAN_POINT ( 'NONE',  ( 0.1557525356064934918, 0.4513421090059003271, 0.4242370903632993739 ) ) ;
#6033=ORIENTED_EDGE ( 'NONE', *, *, #1536, .F. ) ;
#6034=CONICAL_SURFACE ( 'NONE', #3706, 0.6391249999999999432, 1.134464013796309345 ) ;
#6039=CARTESIAN_POINT ( 'NONE',  ( -0.2230971623002953874, 0.2230971623002954152, 0.3921527777777822354 ) ) ;
#6045=CARTESIAN_POINT ( 'NONE',  ( 0.4570242136016807177, -0.2774028246161671651, 0.04874733047933994118 ) ) ;
#6046=CARTESIAN_POINT ( 'NONE',  ( 0.2764156081756483641, -0.1144950937579611028, 0.2237500000000029743 ) ) ;
#6048=CARTESIAN_POINT ( 'NONE',  ( 0.1144950937579611444, 0.2764156081756483641, 0.4112500000000043898 ) ) ;
#6060=( BOUNDED_CURVE ( )  B_SPLINE_CURVE ( 2, ( #11736, #23045, #6351, #2697, #17573, #8294, #21351, #19276, #863 ),
 .UNSPECIFIED., .F., .F. ) 
 B_SPLINE_CURVE_WITH_KNOTS ( ( 3, 2, 2, 2, 3 ),
 ( 0.1458333333333333703, 0.1562500000000000278, 0.1666666666666666852, 0.1770833333333333703, 0.1875000000000000278 ),
 .UNSPECIFIED. ) 
 CURVE ( )  GEOMETRIC_REPRESENTATION_ITEM ( )  RATIONAL_B_SPLINE_CURVE ( ( 0.9999999999999997780, 0.9238795325112869605, 1.000000000000000000, 0.9238795325112867385, 1.000000000000000000, 0.9238795325112867385, 1.000000000000000000, 0.9238795325112865164, 1.000000000000000222 ) ) 
 REPRESENTATION_ITEM ( '' )  );
#6063=VERTEX_POINT ( 'NONE', #20505 ) ;
#6066=CARTESIAN_POINT ( 'NONE',  ( -3.827021247335479543E-17, -0.3125000000000000000, 0.08138888888889088402 ) ) ;
#6067=CIRCLE ( 'NONE', #5690, 0.6288319206375507786 ) ;
#6069=CARTESIAN_POINT ( 'NONE',  ( -0.3155070326520293400, -0.1306872919485614626, -0.1529861111111109617 ) ) ;
#6070=CARTESIAN_POINT ( 'NONE',  ( 0.4206476797388901123, 0.2984048262340602276, 0.05816208736408770563 ) ) ;
#6076=CARTESIAN_POINT ( 'NONE',  ( 0.1954553509668046640, -0.1954553509668047195, -0.1061111111111108091 ) ) ;
#6078=CARTESIAN_POINT ( 'NONE',  ( -0.3060165374364204882, -0.008786209580229879454, -0.09518320410308689361 ) ) ;
#6079=CARTESIAN_POINT ( 'NONE',  ( -0.1954553509668046640, 0.1954553509668046918, 0.08833333333333517889 ) ) ;
#6089=ORIENTED_EDGE ( 'NONE', *, *, #562, .T. ) ;
#6101=CARTESIAN_POINT ( 'NONE',  ( -0.1144950937579609779, 0.2764156081756484196, 0.08486111111111295513 ) ) ;
#6107=CARTESIAN_POINT ( 'NONE',  ( -0.3155070326520293400, -0.1306872919485614626, 0.06576388888889039830 ) ) ;
#6117=CARTESIAN_POINT ( 'NONE',  ( 0.4581189881604794123, 0.2644951211353319120, 0.3941886329748525153 ) ) ;
#6133=CARTESIAN_POINT ( 'NONE',  ( 0.1943163256447900666, 0.4290772944463143168, 0.4279515871991319553 ) ) ;
#6141=CARTESIAN_POINT ( 'NONE',  ( -0.1144950937579609918, -0.2764156081756484196, 0.4320833333333379822 ) ) ;
#6157=CARTESIAN_POINT ( 'NONE',  ( 0.000000000000000000, 0.3155070326520292845, 0.3852083333333378157 ) ) ;
#6161=CARTESIAN_POINT ( 'NONE',  ( -0.1294417382415922746, -0.3125000000000000000, -0.08874999999999934330 ) ) ;
#6164=EDGE_CURVE ( 'NONE', #20369, #11906, #4034, .T. ) ;
#6166=CARTESIAN_POINT ( 'NONE',  ( 0.2764156081756483641, 0.1144950937579610195, 0.2306944444444475328 ) ) ;
#6168=CARTESIAN_POINT ( 'NONE',  ( -0.1954553509668046640, 0.1954553509668046918, 0.3661111111111151617 ) ) ;
#6174=CARTESIAN_POINT ( 'NONE',  ( -0.2209708691207961373, -0.2209708691207961095, 0.3452777777777815138 ) ) ;
#6176=FACE_OUTER_BOUND ( 'NONE', #5082, .T. ) ;
#6178=B_SPLINE_CURVE_WITH_KNOTS ( 'NONE', 3,
 ( #5460, #18148, #23854, #5086, #21915, #10713, #14746, #1680 ),
 .UNSPECIFIED., .F., .F.,
 ( 4, 2, 2, 4 ),
 ( 0.000000000000000000, 0.0004997454757086407804, 0.0007496182135629599237, 0.0009994909514172789586 ),
 .UNSPECIFIED. ) ;
#6180=EDGE_CURVE ( 'NONE', #13004, #22501, #17390, .T. ) ;
#6188=CARTESIAN_POINT ( 'NONE',  ( -0.2230971623002954152, -0.2230971623002953874, -0.09395833333333269977 ) ) ;
#6194=CARTESIAN_POINT ( 'NONE',  ( -0.1954553509668046640, 0.1954553509668046918, -0.1338888888888887796 ) ) ;
#6197=CARTESIAN_POINT ( 'NONE',  ( 0.2764156081756483641, 0.1144950937579610056, 0.1820833333333359283 ) ) ;
#6209=CARTESIAN_POINT ( 'NONE',  ( -1.889944503261478141E-16, 0.5289902422706634910, 0.3941886329748526263 ) ) ;
#6212=CARTESIAN_POINT ( 'NONE',  ( -0.4788451055546355528, -0.2690082051306183497, 0.04193467568257207984 ) ) ;
#6214=CARTESIAN_POINT ( 'NONE',  ( 0.4254287158503464727, -0.3089275304546717504, 0.05347130368200839895 ) ) ;
#6222=CARTESIAN_POINT ( 'NONE',  ( -0.4593750000000003664, -6.734002413227273428E-17, 0.4343810118395207698 ) ) ;
#6224=CARTESIAN_POINT ( 'NONE',  ( 0.4500000000000003442, 0.2598076211353319009, 0.3779506566538943235 ) ) ;
#6229=CARTESIAN_POINT ( 'NONE',  ( -0.3155070326520293400, -0.1306872919485614626, 0.1213194444444463810 ) ) ;
#6236=EDGE_CURVE ( 'NONE', #18304, #2863, #5957, .T. ) ;
#6238=AXIS2_PLACEMENT_3D ( 'NONE', #17538, #21789, #4839 ) ;
#6240=VECTOR ( 'NONE', #19156, 39.37007874015748143 ) ;
#6245=( BOUNDED_CURVE ( )  B_SPLINE_CURVE ( 2, ( #8013, #21187, #9984, #4600, #6066, #10221, #13405, #12059, #2655 ),
 .UNSPECIFIED., .F., .T. ) 
 B_SPLINE_CURVE_WITH_KNOTS ( ( 3, 2, 2, 2, 3 ),
 ( 0.5312500000000001110, 0.5416666666666668517, 0.5520833333333334814, 0.5625000000000000000, 0.5729166666666667407 ),
 .UNSPECIFIED. ) 
 CURVE ( )  GEOMETRIC_REPRESENTATION_ITEM ( )  RATIONAL_B_SPLINE_CURVE ( ( 0.9999999999999992228, 0.9238795325112875156, 1.000000000000000000, 0.9238795325112867385, 1.000000000000000000, 0.9238795325112867385, 1.000000000000000000, 0.9238795325112867385, 1.000000000000000000 ) ) 
 REPRESENTATION_ITEM ( '' )  );
#6251=CIRCLE ( 'NONE', #9376, 0.6211549996190571798 ) ;
#6255=VECTOR ( 'NONE', #7018, 39.37007874015748143 ) ;
#6257=CARTESIAN_POINT ( 'NONE',  ( 0.3832388449590170554, 0.3084783300535419159, 0.4166279060364238562 ) ) ;
#6267=CARTESIAN_POINT ( 'NONE',  ( -0.4208772603875798324, -0.2863811090246152768, 0.4064915563616229299 ) ) ;
#6271=VERTEX_POINT ( 'NONE', #1697 ) ;
#6282=CARTESIAN_POINT ( 'NONE',  ( -0.1294417382415922191, 0.3125000000000000000, 0.2723611111111142735 ) ) ;
#6286=CARTESIAN_POINT ( 'NONE',  ( -0.4687500000000004996, 0.08992298774708656905, 0.4251082876142271982 ) ) ;
#6290=CARTESIAN_POINT ( 'NONE',  ( -0.1144950937579609918, -0.2764156081756484196, 0.3209722222222259891 ) ) ;
#6292=CARTESIAN_POINT ( 'NONE',  ( 0.000000000000000000, 0.2764156081756484196, 0.3591666666666706309 ) ) ;
#6295=CARTESIAN_POINT ( 'NONE',  ( 0.4581189881604794123, -0.2644951211353317455, 0.3941886329748525153 ) ) ;
#6297=CARTESIAN_POINT ( 'NONE',  ( 0.4588877537281843555, -0.1552297620431791481, 0.4201833234654208660 ) ) ;
#6299=CARTESIAN_POINT ( 'NONE',  ( 0.000000000000000000, 0.000000000000000000, 1.326383476483184332 ) ) ;
#6300=CARTESIAN_POINT ( 'NONE',  ( -0.4620775622572422248, 0.2744852724095708241, 0.05975564523638852987 ) ) ;
#6305=CARTESIAN_POINT ( 'NONE',  ( 0.1963876315374232240, 0.4278814254316301580, 0.09139303015897916327 ) ) ;
#6311=CARTESIAN_POINT ( 'NONE',  ( -0.3155070326520292845, 1.931923388228935888E-17, 0.1213194444444467696 ) ) ;
#6317=DIRECTION ( 'NONE',  ( -0.000000000000000000, -0.000000000000000000, -1.000000000000000000 ) ) ;
#6318=CARTESIAN_POINT ( 'NONE',  ( -0.009375000000000190473, 0.5358532185916217161, 0.06112444011295373181 ) ) ;
#6319=CARTESIAN_POINT ( 'NONE',  ( 0.1144950937579609085, -0.2764156081756484751, 0.2237500000000028910 ) ) ;
#6322=CARTESIAN_POINT ( 'NONE',  ( -0.006528205157002933690, 0.5487477722931475288, 0.04212966708837333901 ) ) ;
#6327=DIRECTION ( 'NONE',  ( -0.000000000000000000, 0.000000000000000000, -1.000000000000000000 ) ) ;
#6328=CARTESIAN_POINT ( 'NONE',  ( -0.03741580292205138464, 0.5077710590217058284, 0.4064395341356222269 ) ) ;
#6329=CARTESIAN_POINT ( 'NONE',  ( 0.3065849364905491314, 4.945545817829770315E-15, 0.4182516031572158233 ) ) ;
#6334=CARTESIAN_POINT ( 'NONE',  ( 0.08339729271156200163, 0.4931164279685679719, 0.07808165802387295740 ) ) ;
#6336=CARTESIAN_POINT ( 'NONE',  ( 0.08311813270112124175, -0.4932776010757431440, 0.4002893343786021463 ) ) ;
#6342=EDGE_CURVE ( 'NONE', #22119, #10448, #20669, .T. ) ;
#6344=( BOUNDED_CURVE ( )  B_SPLINE_CURVE ( 2, ( #19106, #2411, #6174, #19221, #9973, #17400, #22994, #21176, #5815 ),
 .UNSPECIFIED., .F., .F. ) 
 B_SPLINE_CURVE_WITH_KNOTS ( ( 3, 2, 2, 2, 3 ),
 ( 0.6875000000000001110, 0.6979166666666667407, 0.7083333333333334814, 0.7187500000000000000, 0.7291666666666666297 ),
 .UNSPECIFIED. ) 
 CURVE ( )  GEOMETRIC_REPRESENTATION_ITEM ( )  RATIONAL_B_SPLINE_CURVE ( ( 0.9999999999999992228, 0.9238795325112875156, 1.000000000000000000, 0.9238795325112867385, 1.000000000000000000, 0.9238795325112867385, 1.000000000000000000, 0.9238795325112867385, 1.000000000000000000 ) ) 
 REPRESENTATION_ITEM ( '' )  );
#6345=CARTESIAN_POINT ( 'NONE',  ( -0.1144950937579609779, 0.2764156081756484196, 0.2515277777777809587 ) ) ;
#6351=CARTESIAN_POINT ( 'NONE',  ( 0.2209708691207961651, 0.2209708691207959985, -0.01583333333333248119 ) ) ;
#6352=CARTESIAN_POINT ( 'NONE',  ( 0.3155070326520292290, -0.1306872919485616569, 0.1421527777777798485 ) ) ;
#6365=ORIENTED_EDGE ( 'NONE', *, *, #3978, .F. ) ;
#6366=CARTESIAN_POINT ( 'NONE',  ( -0.3125000000000000000, 0.1294417382415922468, 0.1126388888888907869 ) ) ;
#6368=CARTESIAN_POINT ( 'NONE',  ( 0.05455304208337304755, -0.2715891510243326756, 0.3880822748423150559 ) ) ;
#6373=EDGE_CURVE ( 'NONE', #16983, #9622, #11487, .T. ) ;
#6374=CARTESIAN_POINT ( 'NONE',  ( 0.3125000000000000000, 3.827021247335477694E-17, 1.326383476483184332 ) ) ;
#6380=CARTESIAN_POINT ( 'NONE',  ( 0.1380212367034616694, 0.4615792792006457312, 0.4105854900893666781 ) ) ;
#6381=FACE_OUTER_BOUND ( 'NONE', #11749, .T. ) ;
#6395=ORIENTED_EDGE ( 'NONE', *, *, #21398, .F. ) ;
#6401=EDGE_CURVE ( 'NONE', #12731, #18304, #13211, .T. ) ;
#6402=CARTESIAN_POINT ( 'NONE',  ( 0.3125000000000000000, -5.740531871003217465E-17, 0.03972222222222387966 ) ) ;
#6403=CARTESIAN_POINT ( 'NONE',  ( -0.3125000000000000000, 1.913510623667739771E-17, 0.2827777777777810142 ) ) ;
#6404=CARTESIAN_POINT ( 'NONE',  ( 0.4593750000000002554, -1.978974282089605735E-13, 0.4343810118395207698 ) ) ;
#6406=CARTESIAN_POINT ( 'NONE',  ( -0.4593748724839620823, -0.02270121287663673382, 0.4343774780089812437 ) ) ;
#6407=CARTESIAN_POINT ( 'NONE',  ( -0.4687500000000002776, -0.04411484026395268848, 0.4171991399623933838 ) ) ;
#6411=CARTESIAN_POINT ( 'NONE',  ( 0.2764156081756483641, -0.1144950937579611167, 0.001527777777778965927 ) ) ;
#6414=CARTESIAN_POINT ( 'NONE',  ( -0.2800968539712042626, 1.715098578335394762E-17, -0.06926352063787094560 ) ) ;
#6419=CARTESIAN_POINT ( 'NONE',  ( 0.000000000000000000, 0.3125000000000000000, 0.1577777777777800150 ) ) ;
#6420=AXIS2_PLACEMENT_3D ( 'NONE', #7755, #18977, #11666 ) ;
#6424=DIRECTION ( 'NONE',  ( -0.000000000000000000, -0.000000000000000000, -1.000000000000000000 ) ) ;
#6425=ORIENTED_EDGE ( 'NONE', *, *, #17974, .T. ) ;
#6429=CARTESIAN_POINT ( 'NONE',  ( 0.3155070326520292845, -5.795770164686806123E-17, 0.1490972222222247956 ) ) ;
#6430=AXIS2_PLACEMENT_3D ( 'NONE', #1877, #4183, #6007 ) ;
#6435=CARTESIAN_POINT ( 'NONE',  ( -0.1144950937579609779, 0.2764156081756484196, 0.02930555555555695163 ) ) ;
#6449=CARTESIAN_POINT ( 'NONE',  ( -0.4500000000000003997, 0.2598076211353315124, 0.3779506566538943790 ) ) ;
#6452=ORIENTED_EDGE ( 'NONE', *, *, #2001, .F. ) ;
#6453=CARTESIAN_POINT ( 'NONE',  ( -0.3124999999999989453, 0.1294417382415933293, 0.1195833333333356230 ) ) ;
#6455=EDGE_CURVE ( 'NONE', #22264, #175, #1419, .T. ) ;
#6459=CARTESIAN_POINT ( 'NONE',  ( -0.1144950937579609918, -0.2764156081756484196, -0.06791666666666602847 ) ) ;
#6464=CARTESIAN_POINT ( 'NONE',  ( -0.2764156081756484196, -0.1144950937579609362, 0.09875000000000193345 ) ) ;
#6470=CARTESIAN_POINT ( 'NONE',  ( 0.3155070326520292290, -0.1306872919485616569, 0.4754861111111158278 ) ) ;
#6489=CARTESIAN_POINT ( 'NONE',  ( 0.009375000000000065573, -0.5358532185916218271, 0.3779506566538943235 ) ) ;
#6491=( BOUNDED_SURFACE ( )  B_SPLINE_SURFACE ( 3, 2, ( 
 ( #3598, #18240, #1772 ),
 ( #7028, #20431, #1894 ),
 ( #1539, #8971, #23828 ),
 ( #14590, #9337, #16773 ),
 ( #57, #15185, #2262 ),
 ( #9696, #19077, #19320 ),
 ( #7741, #2385, #13491 ),
 ( #7621, #11901, #181 ),
 ( #4076, #11407, #22854 ),
 ( #18965, #301, #9821 ),
 ( #6267, #2619, #15306 ),
 ( #11772, #13253, #8089 ) ),
 .UNSPECIFIED., .F., .F., .T. ) 
 B_SPLINE_SURFACE_WITH_KNOTS ( ( 4, 2, 2, 2, 2, 4 ),
 ( 3, 3 ),
 ( 0.03744456216066675835, 0.04077857935059427813, 0.04244558794555804149, 0.04411259654052179791, 0.04744661373044932462, 0.05078063092037684439 ),
 ( 0.000000000000000000, 1.000000000000000000 ),
 .UNSPECIFIED. ) 
 GEOMETRIC_REPRESENTATION_ITEM ( )  RATIONAL_B_SPLINE_SURFACE ( (
 ( 1.000000000000000000, 0.8464669816041904271, 1.000000000000000000),
 ( 1.000000000000000000, 0.8515868425021679844, 1.000000000000000000),
 ( 1.000000000000000000, 0.8564835659291879510, 1.000000000000000000),
 ( 1.000000000000000000, 0.8619139284918067023, 1.000000000000000000),
 ( 1.000000000000000000, 0.8633991495534405480, 1.000000000000000000),
 ( 1.000000000000000000, 0.8654490525000912982, 1.000000000000000000),
 ( 1.000000000000000000, 0.8660089163969103554, 1.000000000000000000),
 ( 1.000000000000000000, 0.8660572738274423532, 1.000000000000000000),
 ( 1.000000000000000000, 0.8638780250325636123, 1.000000000000000000),
 ( 1.000000000000000000, 0.8566598902920686820, 1.000000000000000000),
 ( 1.000000000000000000, 0.8517009389554219823, 1.000000000000000000),
 ( 1.000000000000000000, 0.8464669816041900940, 1.000000000000000000) ) ) 
 REPRESENTATION_ITEM ( '' )  SURFACE ( )  );
#6492=( BOUNDED_SURFACE ( )  B_SPLINE_SURFACE ( 3, 2, ( 
 ( #14563, #9189, #3822 ),
 ( #1511, #20288, #14925 ),
 ( #22344, #16394, #3573 ),
 ( #5646, #11026, #13111 ),
 ( #20525, #11265, #1992 ),
 ( #7123, #12751, #20166 ),
 ( #3453, #16511, #23925 ),
 ( #2359, #15641, #2596 ),
 ( #15280, #2239, #9799 ),
 ( #18811, #3940, #5998 ) ),
 .UNSPECIFIED., .F., .F., .F. ) 
 B_SPLINE_SURFACE_WITH_KNOTS ( ( 4, 2, 2, 2, 4 ),
 ( 3, 3 ),
 ( 0.04463809143445898048, 0.04796255359614957914, 0.05128701575784017086, 0.05461147791953076258, 0.05793594008122135430 ),
 ( 0.000000000000000000, 1.000000000000000000 ),
 .UNSPECIFIED. ) 
 GEOMETRIC_REPRESENTATION_ITEM ( )  RATIONAL_B_SPLINE_SURFACE ( (
 ( 1.000000000000000000, 0.8285407536241361504, 1.000000000000000000),
 ( 1.000000000000000000, 0.8326168960428312893, 1.000000000000000000),
 ( 1.000000000000000000, 0.8363786027323962813, 1.000000000000000000),
 ( 1.000000000000000000, 0.8417912930207285260, 1.000000000000000000),
 ( 1.000000000000000000, 0.8433923807916883231, 1.000000000000000000),
 ( 1.000000000000000000, 0.8433905099817204931, 1.000000000000000000),
 ( 1.000000000000000000, 0.8417888685870387189, 1.000000000000000000),
 ( 1.000000000000000000, 0.8363766775001262310, 1.000000000000000000),
 ( 1.000000000000000000, 0.8326159398061623307, 1.000000000000000000),
 ( 1.000000000000000000, 0.8285407536241354842, 1.000000000000000000) ) ) 
 REPRESENTATION_ITEM ( '' )  SURFACE ( )  );
#6495=FACE_OUTER_BOUND ( 'NONE', #2880, .T. ) ;
#6509=B_SPLINE_CURVE_WITH_KNOTS ( 'NONE', 3,
 ( #6414, #13868, #12048, #2171, #2290, #9604, #17035, #15212, #22647, #20815, #4105, #11564, #9725, #17161, #451, #7882, #22762, #3121, #10330, #10453, #6775, #23586, #2871, #12170, #6903, #21893, #14219, #19461, #12407, #21656, #18121, #17880, #14101, #10572, #16051, #10687, #4702, #16293, #2759, #1418, #8720, #10210, #14341, #18003 ),
 .UNSPECIFIED., .F., .F.,
 ( 4, 2, 1, 2, 2, 2, 2, 2, 2, 1, 2, 2, 2, 2, 2, 2, 2, 2, 2, 2, 2, 2, 4 ),
 ( 0.004595939250185037024, 0.005313238532186213142, 0.006030537814187388393, 0.006747837096188564511, 0.007465136378189738894, 0.008899734942192091131, 0.01033433350619443990, 0.01176893207019679040, 0.01248623135219796565, 0.01320353063419914263, 0.01392082991620031962, 0.01463812919820149661, 0.01607272776220385058, 0.01750732632620620455, 0.01894192489020856199, 0.01965922417220973550, 0.02037652345421091249, 0.02181112201821325952, 0.02324572058221561002, 0.02396301986421678354, 0.02468031914621796052, 0.02611491771022031103, 0.02754951627422265806 ),
 .UNSPECIFIED. ) ;
#6518=ORIENTED_EDGE ( 'NONE', *, *, #10812, .T. ) ;
#6523=CARTESIAN_POINT ( 'NONE',  ( 0.4593750000000006994, 0.04451021669580589035, 0.4343810118395315389 ) ) ;
#6526=CARTESIAN_POINT ( 'NONE',  ( -0.4593400809164812082, -0.04533910969798598395, 0.4334227803821231184 ) ) ;
#6528=CARTESIAN_POINT ( 'NONE',  ( 0.2084225359521126864, -0.1824881659814967805, 0.3875005808676508789 ) ) ;
#6530=CARTESIAN_POINT ( 'NONE',  ( 0.1144950937579611444, 0.2764156081756483641, -0.04013888888888803713 ) ) ;
#6542=CYLINDRICAL_SURFACE ( 'NONE', #12886, 0.3125000000000000000 ) ;
#6545=CARTESIAN_POINT ( 'NONE',  ( 0.4805070082343984583, -0.2560807851245830435, 0.04413116910601660309 ) ) ;
#6546=CARTESIAN_POINT ( 'NONE',  ( 0.3155070326520292845, -5.795770164686806123E-17, -0.01756944444444321490 ) ) ;
#6547=AXIS2_PLACEMENT_3D ( 'NONE', #164, #16642, #7255 ) ;
#6549=VERTEX_POINT ( 'NONE', #6768 ) ;
#6552=CARTESIAN_POINT ( 'NONE',  ( -0.1144950937579609779, 0.2764156081756484196, -0.08180555555555503455 ) ) ;
#6553=CARTESIAN_POINT ( 'NONE',  ( 0.2209708691207961095, -0.2209708691207961651, 0.4216666666666714081 ) ) ;
#6555=CARTESIAN_POINT ( 'NONE',  ( 0.2764156081756483641, -0.1144950937579611167, 0.4529166666666714636 ) ) ;
#6564=B_SPLINE_CURVE_WITH_KNOTS ( 'NONE', 3,
 ( #2707, #875, #11292, #16889, #9697, #182, #18720, #10158, #20671, #11533 ),
 .UNSPECIFIED., .F., .F.,
 ( 4, 2, 2, 2, 4 ),
 ( 0.000000000000000000, 0.003321633220911225561, 0.006643266441822451122, 0.009964899662733674515, 0.01328653288364489704 ),
 .UNSPECIFIED. ) ;
#6567=CARTESIAN_POINT ( 'NONE',  ( -0.3107848814623954126, 0.3618341423928944645, 0.4134938258000330769 ) ) ;
#6571=AXIS2_PLACEMENT_3D ( 'NONE', #1645, #14709, #16529 ) ;
#6572=CARTESIAN_POINT ( 'NONE',  ( -0.3125000000000000000, 1.913510623667739771E-17, -0.04361111111111011518 ) ) ;
#6578=CARTESIAN_POINT ( 'NONE',  ( 0.2764156081756483641, -0.1144950937579611167, -0.05402777777777704321 ) ) ;
#6584=CARTESIAN_POINT ( 'NONE',  ( -0.1954553509668046918, -0.1954553509668046640, 0.1577777777777801815 ) ) ;
#6587=CARTESIAN_POINT ( 'NONE',  ( -0.2523926463571780632, 0.1523216146538590721, 0.4063109944092492820 ) ) ;
#6591=CARTESIAN_POINT ( 'NONE',  ( 0.3155070326520292845, -5.795770164686806123E-17, 0.4789583333333381487 ) ) ;
#6599=B_SPLINE_CURVE_WITH_KNOTS ( 'NONE', 3,
 ( #22255, #7386, #14952, #11050, #5673, #20314, #9088, #10932, #20551, #5183, #12898, #22372, #11291, #7504, #2018, #23956, #16656, #5311, #12654, #18360, #12775, #18479 ),
 .UNSPECIFIED., .F., .F.,
 ( 4, 2, 2, 2, 2, 2, 2, 2, 2, 2, 4 ),
 ( 0.002245614500282211434, 0.002912534838767885485, 0.003579455177253559536, 0.004913295854224907638, 0.006247136531196254873, 0.007580977208167602975, 0.008914817885138950210, 0.009581738223624625128, 0.01024865856211029831, 0.01158249923908164641, 0.01291633991605299452 ),
 .UNSPECIFIED. ) ;
#6604=CARTESIAN_POINT ( 'NONE',  ( 0.000000000000000000, 0.3125000000000000000, 0.3869444444444488651 ) ) ;
#6606=LINE ( 'NONE', #15522, #18470 ) ;
#6621=AXIS2_PLACEMENT_3D ( 'NONE', #19870, #3162, #4987 ) ;
#6631=ORIENTED_EDGE ( 'NONE', *, *, #9929, .T. ) ;
#6637=EDGE_CURVE ( 'NONE', #18060, #3289, #3716, .T. ) ;
#6638=AXIS2_PLACEMENT_3D ( 'NONE', #22724, #2124, #20897 ) ;
#6641=CARTESIAN_POINT ( 'NONE',  ( 0.4687500000000003886, 0.2598076211353211318, 0.06112444011295851964 ) ) ;
#6647=EDGE_CURVE ( 'NONE', #11791, #8318, #15525, .T. ) ;
#6650=CARTESIAN_POINT ( 'NONE',  ( -0.1144950937579609779, 0.2764156081756484196, 0.3556944444444484765 ) ) ;
#6652=CARTESIAN_POINT ( 'NONE',  ( 0.1144950937579611444, 0.2764156081756483641, 0.1265277777777799595 ) ) ;
#6656=CARTESIAN_POINT ( 'NONE',  ( 0.000000000000000000, 0.000000000000000000, -0.01143517789850382292 ) ) ;
#6657=DIRECTION ( 'NONE',  ( 2.169098857401406875E-15, 0.9767851838303063250, 0.2142211582677929216 ) ) ;
#6659=CONICAL_SURFACE ( 'NONE', #1602, 0.3308333333333332571, 0.7853981633974427279 ) ;
#6664=CARTESIAN_POINT ( 'NONE',  ( 0.4223136544080928201, 0.2974429753103076668, 0.07050986311825918618 ) ) ;
#6665=ORIENTED_EDGE ( 'NONE', *, *, #15590, .F. ) ;
#6668=CARTESIAN_POINT ( 'NONE',  ( 0.3155070326520292290, 0.1306872919485615736, 0.09701388888889106443 ) ) ;
#6675=CARTESIAN_POINT ( 'NONE',  ( 0.000000000000000000, 0.2764156081756484196, 0.02583333333333468970 ) ) ;
#6676=CARTESIAN_POINT ( 'NONE',  ( 0.1294417382415921358, -0.3125000000000002220, 0.4181944444444491982 ) ) ;
#6678=CARTESIAN_POINT ( 'NONE',  ( 0.2764156081756483641, 0.1144950937579610056, 0.3487500000000040012 ) ) ;
#6688=CARTESIAN_POINT ( 'NONE',  ( -0.1904260988303179414, 0.4204977338396926889, 0.4343746145485231080 ) ) ;
#6692=CARTESIAN_POINT ( 'NONE',  ( 0.000000000000000000, 0.000000000000000000, 1.326383476483184332 ) ) ;
#6695=CARTESIAN_POINT ( 'NONE',  ( -0.4687500000000003331, -0.08694130287036218319, 0.07655038602225107403 ) ) ;
#6696=CARTESIAN_POINT ( 'NONE',  ( 0.1954553509668047195, 0.1954553509668046085, 0.06750000000000172529 ) ) ;
#6701=CARTESIAN_POINT ( 'NONE',  ( -3.827021247335479543E-17, -0.3125000000000000000, 0.2966666666666700203 ) ) ;
#6702=CARTESIAN_POINT ( 'NONE',  ( -3.385114897866767815E-17, -0.2764156081756484196, 0.1647222222222247123 ) ) ;
#6706=CARTESIAN_POINT ( 'NONE',  ( -0.2872991414527177878, 0.07488537861673925933, 0.4079643588709177537 ) ) ;
#6707=CARTESIAN_POINT ( 'NONE',  ( -0.4802535689586319156, 0.2139885278467183738, 0.05346681960559353242 ) ) ;
#6709=CARTESIAN_POINT ( 'NONE',  ( -0.1144950937579609918, -0.2764156081756484196, -0.01236111111111004406 ) ) ;
#6710=CARTESIAN_POINT ( 'NONE',  ( 0.2230971623002953874, -0.2230971623002954429, 0.4164583333333376491 ) ) ;
#6711=ORIENTED_EDGE ( 'NONE', *, *, #17864, .F. ) ;
#6714=CARTESIAN_POINT ( 'NONE',  ( -0.1294417382415922746, -0.3125000000000000000, 0.01541666666666776514 ) ) ;
#6724=ORIENTED_EDGE ( 'NONE', *, *, #21938, .F. ) ;
#6726=EDGE_CURVE ( 'NONE', #1635, #9081, #17091, .T. ) ;
#6736=ORIENTED_EDGE ( 'NONE', *, *, #4559, .T. ) ;
#6738=DIRECTION ( 'NONE',  ( -0.7071067811865484609, 0.000000000000000000, -0.7071067811865464625 ) ) ;
#6743=LINE ( 'NONE', #5150, #16263 ) ;
#6767=CARTESIAN_POINT ( 'NONE',  ( -0.4687499999999811817, -0.08977042653030931074, 0.4243505787549145536 ) ) ;
#6768=CARTESIAN_POINT ( 'NONE',  ( 0.4453125000000000000, 0.000000000000000000, 0.4425000000000000044 ) ) ;
#6771=CARTESIAN_POINT ( 'NONE',  ( -0.3125000000000000000, 1.913510623667739771E-17, 0.3452777777777818469 ) ) ;
#6773=CARTESIAN_POINT ( 'NONE',  ( -0.1144950937579609779, 0.2764156081756484196, 0.02236111111111246247 ) ) ;
#6775=CARTESIAN_POINT ( 'NONE',  ( -0.05866837512862337067, 0.2818896272181906082, -0.07694038459218610626 ) ) ;
#6778=CARTESIAN_POINT ( 'NONE',  ( 0.3125000000000002220, -0.1294417382415921358, -0.02624999999999922187 ) ) ;
#6783=CARTESIAN_POINT ( 'NONE',  ( -0.3125000000000004996, 0.1294417382415917195, 0.1681944444444467279 ) ) ;
#6785=ORIENTED_EDGE ( 'NONE', *, *, #9016, .T. ) ;
#6786=CARTESIAN_POINT ( 'NONE',  ( 0.000000000000000000, 3.738758431839877614E-19, -0.1012499999999999928 ) ) ;
#6791=CARTESIAN_POINT ( 'NONE',  ( 0.2209708691207961651, 0.2209708691207959985, 0.2133333333333364001 ) ) ;
#6792=CARTESIAN_POINT ( 'NONE',  ( -0.3155070326520292845, 1.931923388228935888E-17, 0.01020833333333479032 ) ) ;
#6795=DIRECTION ( 'NONE',  ( -0.000000000000000000, -0.000000000000000000, -1.000000000000000000 ) ) ;
#6799=CARTESIAN_POINT ( 'NONE',  ( 0.000000000000000000, 0.2764156081756484196, -0.08527777777777729995 ) ) ;
#6803=ORIENTED_EDGE ( 'NONE', *, *, #13522, .F. ) ;
#6817=CARTESIAN_POINT ( 'NONE',  ( 0.2351701443102654221, -0.2046330205462786322, 0.4229527702155532198 ) ) ;
#6818=CARTESIAN_POINT ( 'NONE',  ( 0.4645572405553155537, -0.2721000128023693954, 0.05892738626661211260 ) ) ;
#6821=CYLINDRICAL_SURFACE ( 'NONE', #22445, 0.01874999999999997155 ) ;
#6822=CARTESIAN_POINT ( 'NONE',  ( 0.000000000000000000, 0.2764156081756484196, 0.01888888888889020401 ) ) ;
#6825=CARTESIAN_POINT ( 'NONE',  ( 0.1294417382415921358, -0.3125000000000002220, 0.3001388888888922857 ) ) ;
#6826=CARTESIAN_POINT ( 'NONE',  ( 0.1954553509668046640, -0.1954553509668047195, 0.2827777777777811807 ) ) ;
#6830=CARTESIAN_POINT ( 'NONE',  ( -0.1294417382415922191, 0.3125000000000000000, -0.05402777777777686280 ) ) ;
#6832=FACE_BOUND ( 'NONE', #7981, .T. ) ;
#6834=CARTESIAN_POINT ( 'NONE',  ( 0.3155070326520292845, -5.795770164686806123E-17, 0.4234027777777820689 ) ) ;
#6835=ORIENTED_EDGE ( 'NONE', *, *, #14108, .F. ) ;
#6863=DIRECTION ( 'NONE',  ( -0.5000000000000012212, -0.8660254037844380415, 0.000000000000000000 ) ) ;
#6873=CARTESIAN_POINT ( 'NONE',  ( 0.4687500000000003886, 0.04389001238043919312, 0.09139217099949126233 ) ) ;
#6874=CARTESIAN_POINT ( 'NONE',  ( 0.3125000000000000000, -5.740531871003217465E-17, -0.07138888888888809958 ) ) ;
#6875=CARTESIAN_POINT ( 'NONE',  ( -0.4678785457174671758, -0.2663437566607215756, 0.05892894635879406678 ) ) ;
#6886=CARTESIAN_POINT ( 'NONE',  ( -0.1294417382415922746, -0.3125000000000000000, 0.2445833333333366777 ) ) ;
#6888=ORIENTED_EDGE ( 'NONE', *, *, #1111, .F. ) ;
#6890=CARTESIAN_POINT ( 'NONE',  ( 0.3146687483788559447, 0.3722097299877928367, 0.07156199457778794626 ) ) ;
#6894=CARTESIAN_POINT ( 'NONE',  ( 0.3125000000000000000, -5.740531871003217465E-17, -0.07833333333333296344 ) ) ;
#6896=B_SPLINE_CURVE_WITH_KNOTS ( 'NONE', 3,
 ( #15489, #22917, #6212, #13677, #123, #2078, #249, #7684 ),
 .UNSPECIFIED., .F., .F.,
 ( 4, 2, 2, 4 ),
 ( 0.000000000000000000, 0.0004997454757086376362, 0.0007496182135629577553, 0.0009994909514172778744 ),
 .UNSPECIFIED. ) ;
#6900=CARTESIAN_POINT ( 'NONE',  ( 0.1954553509668046640, -0.1954553509668047195, 0.1647222222222247123 ) ) ;
#6901=EDGE_CURVE ( 'NONE', #3858, #7205, #4786, .T. ) ;
#6903=CARTESIAN_POINT ( 'NONE',  ( 0.04489076912979098055, 0.2868701433674690215, -0.07891441836899415474 ) ) ;
#6909=CIRCLE ( 'NONE', #4949, 0.01875000000000000971 ) ;
#6910=CARTESIAN_POINT ( 'NONE',  ( -0.3125000000000000000, 1.913510623667739771E-17, -0.09916666666666609786 ) ) ;
#6911=ORIENTED_EDGE ( 'NONE', *, *, #9494, .F. ) ;
#6914=CARTESIAN_POINT ( 'NONE',  ( 0.3155070326520292290, -0.1306872919485616569, 0.3122916666666705754 ) ) ;
#6920=CIRCLE ( 'NONE', #21725, 0.3385998376278290256 ) ;
#6922=CARTESIAN_POINT ( 'NONE',  ( -3.385114897866767815E-17, -0.2764156081756484196, -0.001944444444443294917 ) ) ;
#6929=CARTESIAN_POINT ( 'NONE',  ( -0.4592340600545777307, -0.08946199657451012199, 0.4305916167228413527 ) ) ;
#6946=CARTESIAN_POINT ( 'NONE',  ( 0.2764156081756483641, 0.1144950937579610056, -0.04708333333333254017 ) ) ;
#6947=ADVANCED_FACE ( 'NONE', ( #20153 ), #8840, .F. ) ;
#6950=CARTESIAN_POINT ( 'NONE',  ( -0.2209708691207961373, -0.2209708691207961095, 0.2897222222222255450 ) ) ;
#6951=CARTESIAN_POINT ( 'NONE',  ( -0.1954553509668046918, -0.1954553509668046640, 0.3244444444444481435 ) ) ;
#6954=CARTESIAN_POINT ( 'NONE',  ( 0.03071979988720062796, 0.2873147545066538355, 0.3999952370221915854 ) ) ;
#6956=CARTESIAN_POINT ( 'NONE',  ( 0.2764156081756483641, -0.1144950937579611028, -0.05402777777777704321 ) ) ;
#6957=CARTESIAN_POINT ( 'NONE',  ( -0.1306872919485614903, 0.3155070326520293400, 0.3852083333333373161 ) ) ;
#6969=DIRECTION ( 'NONE',  ( 0.000000000000000000, 0.000000000000000000, 1.000000000000000000 ) ) ;
#6975=AXIS2_PLACEMENT_3D ( 'NONE', #1548, #5072, #4955 ) ;
#6990=DIRECTION ( 'NONE',  ( -1.224646799147353207E-16, 1.000000000000000000, 0.000000000000000000 ) ) ;
#6991=CARTESIAN_POINT ( 'NONE',  ( -0.3125000000000000000, 1.913510623667739771E-17, 0.06750000000000189182 ) ) ;
#6992=DIRECTION ( 'NONE',  ( 0.000000000000000000, 0.000000000000000000, -1.000000000000000000 ) ) ;
#6999=CARTESIAN_POINT ( 'NONE',  ( -0.4683334081279688643, -0.2655573993979173375, 0.04698409998688869021 ) ) ;
#7012=CARTESIAN_POINT ( 'NONE',  ( 0.1514837979169836590, -0.4428147562410877369, 0.4304954382810344260 ) ) ;
#7013=DIRECTION ( 'NONE',  ( 0.000000000000000000, -1.000000000000000000, 0.000000000000000000 ) ) ;
#7018=DIRECTION ( 'NONE',  ( 0.000000000000000000, 0.000000000000000000, -1.000000000000000000 ) ) ;
#7019=CARTESIAN_POINT ( 'NONE',  ( 0.000000000000000000, 3.738758431839877614E-19, -0.1199999999999999956 ) ) ;
#7024=CARTESIAN_POINT ( 'NONE',  ( -0.2764156081756484196, 0.1144950937579609918, 0.3626388888888929518 ) ) ;
#7028=CARTESIAN_POINT ( 'NONE',  ( -0.03677510111069775406, -0.5081344126854103749, 0.4062297518000713703 ) ) ;
#7029=PLANE ( 'NONE',  #12011 ) ;
#7034=AXIS2_PLACEMENT_3D ( 'NONE', #425, #21389, #9943 ) ;
#7040=CARTESIAN_POINT ( 'NONE',  ( -0.3155070326520293400, -0.1306872919485614626, 0.1803472222222250454 ) ) ;
#7042=ORIENTED_EDGE ( 'NONE', *, *, #13328, .F. ) ;
#7044=VECTOR ( 'NONE', #2367, 39.37007874015748143 ) ;
#7048=CARTESIAN_POINT ( 'NONE',  ( 0.000000000000000000, 0.2764156081756484196, 0.1925000000000026690 ) ) ;
#7060=CARTESIAN_POINT ( 'NONE',  ( 0.006464354918053449514, 0.5491938321437414006, 0.04193567535760748394 ) ) ;
#7062=CARTESIAN_POINT ( 'NONE',  ( -0.3125000000000000000, 1.913510623667739771E-17, 0.1161111111111130384 ) ) ;
#7069=CARTESIAN_POINT ( 'NONE',  ( -0.1688124736068475629, -0.2196335248263224516, -0.06558227484231513027 ) ) ;
#7070=CARTESIAN_POINT ( 'NONE',  ( -0.1954553509668046918, -0.1954553509668046640, 0.3175000000000037237 ) ) ;
#7072=CYLINDRICAL_SURFACE ( 'NONE', #10336, 0.3125000000000000000 ) ;
#7074=CARTESIAN_POINT ( 'NONE',  ( -0.2764156081756484196, 1.692557448933383907E-17, 0.3730555555555596925 ) ) ;
#7077=CARTESIAN_POINT ( 'NONE',  ( 0.4687500000000002776, 0.2172212470101570203, 0.07046416248101895763 ) ) ;
#7079=DIRECTION ( 'NONE',  ( 0.000000000000000000, -1.000000000000000000, 0.000000000000000000 ) ) ;
#7080=CARTESIAN_POINT ( 'NONE',  ( 0.000000000000000000, 0.2764156081756484196, -0.02972222222222129645 ) ) ;
#7084=CARTESIAN_POINT ( 'NONE',  ( -3.827021247335479543E-17, -0.3125000000000000000, 0.01888888888889002707 ) ) ;
#7089=CARTESIAN_POINT ( 'NONE',  ( 0.4687500000000003886, -0.2922835737772481735, 0.06112444011295372487 ) ) ;
#7092=EDGE_CURVE ( 'NONE', #10191, #18764, #8970, .T. ) ;
#7105=ORIENTED_EDGE ( 'NONE', *, *, #15845, .F. ) ;
#7111=CARTESIAN_POINT ( 'NONE',  ( -0.2230971623002954152, -0.2230971623002953874, -0.04187499999999937106 ) ) ;
#7114=ADVANCED_FACE ( 'NONE', ( #2168 ), #22232, .F. ) ;
#7123=CARTESIAN_POINT ( 'NONE',  ( -0.2021572709300195614, 0.4370510722512948587, 0.07439726544911813566 ) ) ;
#7129=ADVANCED_FACE ( 'NONE', ( #22760 ), #15096, .F. ) ;
#7131=ORIENTED_EDGE ( 'NONE', *, *, #14186, .T. ) ;
#7133=CARTESIAN_POINT ( 'NONE',  ( -0.03811151966973166244, -0.3039168590976487061, 0.4175033535898823311 ) ) ;
#7142=( BOUNDED_CURVE ( )  B_SPLINE_CURVE ( 2, ( #9898, #19394, #23041, #23155, #2575, #13919, #4394, #8053, #15502 ),
 .UNSPECIFIED., .F., .T. ) 
 B_SPLINE_CURVE_WITH_KNOTS ( ( 3, 2, 2, 2, 3 ),
 ( 0.1145833333333333148, 0.1249999999999999722, 0.1354166666666667407, 0.1458333333333333703, 0.1562500000000000278 ),
 .UNSPECIFIED. ) 
 CURVE ( )  GEOMETRIC_REPRESENTATION_ITEM ( )  RATIONAL_B_SPLINE_CURVE ( ( 1.000000000000000444, 0.9238795325112862944, 1.000000000000000000, 0.9238795325112867385, 1.000000000000000000, 0.9238795325112867385, 1.000000000000000000, 0.9238795325112865164, 1.000000000000000222 ) ) 
 REPRESENTATION_ITEM ( '' )  );
#7143=ORIENTED_EDGE ( 'NONE', *, *, #15315, .F. ) ;
#7145=DIRECTION ( 'NONE',  ( 7.284927983104698760E-15, -1.000000000000000000, -3.642463991552349380E-15 ) ) ;
#7146=CARTESIAN_POINT ( 'NONE',  ( 0.000000000000000000, 0.2764156081756484196, 0.2411111111111142458 ) ) ;
#7150=CARTESIAN_POINT ( 'NONE',  ( -0.4687500000000004441, 0.1740113748017589612, 0.07813285960791813145 ) ) ;
#7160=CARTESIAN_POINT ( 'NONE',  ( -0.3155070326520292845, 1.931923388228935888E-17, 0.2879861111111147731 ) ) ;
#7165=CARTESIAN_POINT ( 'NONE',  ( -0.2764156081756484196, -0.1144950937579609362, 0.1543055555555579716 ) ) ;
#7184=CARTESIAN_POINT ( 'NONE',  ( -0.003366903179265029553, -0.5383683782340863422, 0.05892738626661211260 ) ) ;
#7187=CARTESIAN_POINT ( 'NONE',  ( -0.2085087158398496454, -0.1823754829287230206, -0.06558227484231535231 ) ) ;
#7188=CARTESIAN_POINT ( 'NONE',  ( 0.000000000000000000, 0.2764156081756484196, 0.1300000000000022249 ) ) ;
#7191=CARTESIAN_POINT ( 'NONE',  ( -0.2764156081756484196, -0.1144950937579609362, 0.3765277777777819579 ) ) ;
#7198=CARTESIAN_POINT ( 'NONE',  ( 0.1954553509668047195, 0.1954553509668046085, 0.07444444444444621445 ) ) ;
#7201=CARTESIAN_POINT ( 'NONE',  ( 0.4593747947243453367, 0.02264684698529824056, 0.4343753230511080421 ) ) ;
#7205=VERTEX_POINT ( 'NONE', #22519 ) ;
#7212=AXIS2_PLACEMENT_3D ( 'NONE', #23748, #16695, #7432 ) ;
#7216=CARTESIAN_POINT ( 'NONE',  ( 0.2918969027557590246, -0.06668494381002647298, -0.08811163115763034903 ) ) ;
#7232=CARTESIAN_POINT ( 'NONE',  ( -0.2230971623002954152, -0.2230971623002953874, -0.09743055555555536762 ) ) ;
#7244=LINE ( 'NONE', #7359, #5494 ) ;
#7251=EDGE_LOOP ( 'NONE', ( #18276, #3353, #11940, #6835 ) ) ;
#7255=DIRECTION ( 'NONE',  ( 0.8660254037844383745, 0.5000000000000003331, 0.000000000000000000 ) ) ;
#7262=DIRECTION ( 'NONE',  ( -1.000000000000000000, 0.000000000000000000, 0.000000000000000000 ) ) ;
#7265=VECTOR ( 'NONE', #5631, 39.37007874015748143 ) ;
#7267=CARTESIAN_POINT ( 'NONE',  ( -0.1954553509668046640, 0.1954553509668046918, 0.3036111111111147176 ) ) ;
#7279=VERTEX_POINT ( 'NONE', #6295 ) ;
#7281=CARTESIAN_POINT ( 'NONE',  ( 0.3155070326520292845, -5.795770164686806123E-17, 0.2046527777777807644 ) ) ;
#7286=CARTESIAN_POINT ( 'NONE',  ( 0.1954553509668047195, 0.1954553509668046085, 0.2411111111111141903 ) ) ;
#7303=ORIENTED_EDGE ( 'NONE', *, *, #24055, .T. ) ;
#7304=CARTESIAN_POINT ( 'NONE',  ( -0.1294417382415922746, -0.3125000000000000000, 0.1265277777777797930 ) ) ;
#7307=CARTESIAN_POINT ( 'NONE',  ( -0.2764156081756484196, 1.692557448933383907E-17, 0.2550000000000032241 ) ) ;
#7309=CARTESIAN_POINT ( 'NONE',  ( -0.3125000000000000000, 1.913510623667739771E-17, 0.2897222222222258226 ) ) ;
#7310=CARTESIAN_POINT ( 'NONE',  ( 0.4673607484394255440, 0.2845795129072107299, 0.04287645741408792344 ) ) ;
#7318=CARTESIAN_POINT ( 'NONE',  ( -0.1144950937579609918, -0.2764156081756484196, -0.005416666666665557496 ) ) ;
#7322=CARTESIAN_POINT ( 'NONE',  ( 0.4687500000000003331, 0.02249286784990170429, 0.4289627432666881512 ) ) ;
#7347=CARTESIAN_POINT ( 'NONE',  ( 0.3155070326520292845, -5.795770164686806123E-17, -0.02104166666666586888 ) ) ;
#7348=CARTESIAN_POINT ( 'NONE',  ( -0.2721904660997562231, -0.3841166384917365506, 0.07944544255958575774 ) ) ;
#7359=CARTESIAN_POINT ( 'NONE',  ( 0.4453125000000000000, 0.000000000000000000, 0.4425000000000000044 ) ) ;
#7364=CIRCLE ( 'NONE', #6975, 0.01875000000000001318 ) ;
#7366=EDGE_LOOP ( 'NONE', ( #4734, #20179, #23700 ) ) ;
#7368=CARTESIAN_POINT ( 'NONE',  ( 0.06232504194019378163, -0.3017193634690418791, 0.4192984290766904043 ) ) ;
#7377=DIRECTION ( 'NONE',  ( 0.000000000000000000, 0.000000000000000000, -1.000000000000000000 ) ) ;
#7383=CARTESIAN_POINT ( 'NONE',  ( -0.1144950937579609918, -0.2764156081756484196, 0.2098611111111139960 ) ) ;
#7386=CARTESIAN_POINT ( 'NONE',  ( 0.3060165374364313129, -0.008786209580232379190, 0.4176832041030980047 ) ) ;
#7399=ORIENTED_EDGE ( 'NONE', *, *, #17718, .F. ) ;
#7401=CARTESIAN_POINT ( 'NONE',  ( 0.1306872919485614071, -0.3155070326520293955, 0.3053472222222260446 ) ) ;
#7404=CARTESIAN_POINT ( 'NONE',  ( 0.4622078388679876082, -0.2744100571732867588, 0.3892820121258429023 ) ) ;
#7407=CARTESIAN_POINT ( 'NONE',  ( 0.2764156081756483641, -0.1144950937579611167, 0.2306944444444474218 ) ) ;
#7425=CARTESIAN_POINT ( 'NONE',  ( -0.08325293014416509929, -0.4931997757357155510, 0.4003306813560889577 ) ) ;
#7430=CARTESIAN_POINT ( 'NONE',  ( 0.1144950937579611444, 0.2764156081756483641, 0.2376388888888919526 ) ) ;
#7431=AXIS2_PLACEMENT_3D ( 'NONE', #10231, #15476, #4487 ) ;
#7432=DIRECTION ( 'NONE',  ( 0.4999999999999992784, -0.8660254037844390407, 0.000000000000000000 ) ) ;
#7437=CARTESIAN_POINT ( 'NONE',  ( -3.385114897866767815E-17, -0.2764156081756484196, -0.001944444444443294917 ) ) ;
#7440=CARTESIAN_POINT ( 'NONE',  ( 0.4687500000000003886, -0.04437455914722442107, 0.4289794960421708381 ) ) ;
#7463=CARTESIAN_POINT ( 'NONE',  ( -0.1306872919485614903, 0.3155070326520293400, -0.05923611111111061478 ) ) ;
#7464=CARTESIAN_POINT ( 'NONE',  ( -0.1294417382415922746, -0.3125000000000000000, 0.02236111111111264288 ) ) ;
#7472=EDGE_CURVE ( 'NONE', #20446, #7699, #4260, .T. ) ;
#7482=CARTESIAN_POINT ( 'NONE',  ( -0.1567390680356932908, -0.2674066423995976605, -0.09867016728294440708 ) ) ;
#7483=ORIENTED_EDGE ( 'NONE', *, *, #23504, .F. ) ;
#7486=CARTESIAN_POINT ( 'NONE',  ( -0.2918969027557561380, -0.06668494381005772575, 0.4106116311576339384 ) ) ;
#7487=CARTESIAN_POINT ( 'NONE',  ( 0.2676934969451048585, -0.3758505236666522253, 0.4334994210334167652 ) ) ;
#7492=CARTESIAN_POINT ( 'NONE',  ( 0.3124999999999993339, -0.1294417382415928852, 0.2029166666666696039 ) ) ;
#7496=VERTEX_POINT ( 'NONE', #22025 ) ;
#7500=CARTESIAN_POINT ( 'NONE',  ( 0.000000000000000000, 0.2764156081756484196, 0.1855555555555581937 ) ) ;
#7501=EDGE_CURVE ( 'NONE', #19685, #21037, #4240, .T. ) ;
#7504=CARTESIAN_POINT ( 'NONE',  ( 0.1762772571227061713, -0.2274112121558803656, 0.3992673050735688900 ) ) ;
#7505=CARTESIAN_POINT ( 'NONE',  ( -0.4620259694561524855, 0.2880908832651556950, 0.04413116910601659615 ) ) ;
#7509=EDGE_CURVE ( 'NONE', #23140, #5916, #7364, .T. ) ;
#7519=CARTESIAN_POINT ( 'NONE',  ( 0.2491691211422967234, -0.3865828334249452047, 0.4343841983240312454 ) ) ;
#7520=CARTESIAN_POINT ( 'NONE',  ( 0.000000000000000000, 0.000000000000000000, 1.326383476483184332 ) ) ;
#7523=CARTESIAN_POINT ( 'NONE',  ( 0.2764156081756483641, 0.1144950937579610195, 0.1195833333333354703 ) ) ;
#7525=CARTESIAN_POINT ( 'NONE',  ( -0.1954553509668046640, 0.1954553509668046918, 0.3105555555555591929 ) ) ;
#7538=DIRECTION ( 'NONE',  ( -0.000000000000000000, -0.000000000000000000, 1.000000000000000000 ) ) ;
#7543=CARTESIAN_POINT ( 'NONE',  ( -0.1144950937579609779, 0.2764156081756484196, 0.3001388888888924522 ) ) ;
#7546=ORIENTED_EDGE ( 'NONE', *, *, #4095, .F. ) ;
#7552=CARTESIAN_POINT ( 'NONE',  ( -0.1954553509668046640, 0.1954553509668046918, 0.03277777777777921009 ) ) ;
#7585=CARTESIAN_POINT ( 'NONE',  ( -0.04811092099938358430, -0.5134890241753798934, 0.05816431335569525324 ) ) ;
#7591=CIRCLE ( 'NONE', #22379, 0.3308333333333332571 ) ;
#7600=CARTESIAN_POINT ( 'NONE',  ( 0.3125000000000000000, 3.827021247335477694E-17, 1.326383476483184332 ) ) ;
#7601=ORIENTED_EDGE ( 'NONE', *, *, #12651, .T. ) ;
#7604=CARTESIAN_POINT ( 'NONE',  ( -0.1898046044842733593, -0.2363956207630708017, 0.4143648991452117958 ) ) ;
#7618=DIRECTION ( 'NONE',  ( 1.000000000000000000, 0.000000000000000000, 0.000000000000000000 ) ) ;
#7621=CARTESIAN_POINT ( 'NONE',  ( -0.2681267372834953977, -0.3756399061183363086, 0.4344383781808794365 ) ) ;
#7631=ORIENTED_EDGE ( 'NONE', *, *, #21398, .T. ) ;
#7637=CARTESIAN_POINT ( 'NONE',  ( 0.4641327083039680779, 0.2728248698625151403, 0.04698599556840849650 ) ) ;
#7644=CARTESIAN_POINT ( 'NONE',  ( -0.1144950937579609918, -0.2764156081756484196, 0.2654166666666700203 ) ) ;
#7646=CARTESIAN_POINT ( 'NONE',  ( -0.1954553509668046918, -0.1954553509668046640, 0.4355555555555601921 ) ) ;
#7653=CARTESIAN_POINT ( 'NONE',  ( 0.4645343760433821023, 0.2721270390806222461, 0.05893285591566543163 ) ) ;
#7663=CARTESIAN_POINT ( 'NONE',  ( -3.863846776457871776E-17, -0.3155070326520292845, -0.08701388888888821060 ) ) ;
#7664=DIRECTION ( 'NONE',  ( 0.000000000000000000, 0.000000000000000000, -1.000000000000000000 ) ) ;
#7666=CARTESIAN_POINT ( 'NONE',  ( 0.000000000000000000, 0.000000000000000000, 1.326383476483184332 ) ) ;
#7671=CARTESIAN_POINT ( 'NONE',  ( 0.4687500000000002776, -0.2598076211353317344, 0.06112444011295377344 ) ) ;
#7673=CARTESIAN_POINT ( 'NONE',  ( 0.2730703793714973626, 0.3836086203274273188, 0.4181140142936810578 ) ) ;
#7674=CARTESIAN_POINT ( 'NONE',  ( -3.385114897866767815E-17, -0.2764156081756484196, 0.1647222222222247123 ) ) ;
#7676=CARTESIAN_POINT ( 'NONE',  ( 0.4592090122005416108, 0.09026097205167347981, 0.4297114009649623534 ) ) ;
#7683=EDGE_LOOP ( 'NONE', ( #17423, #21637, #14080, #16129 ) ) ;
#7684=CARTESIAN_POINT ( 'NONE',  ( -0.4620259694561524855, -0.2880908832651560281, 0.04413116910601651982 ) ) ;
#7690=LENGTH_MEASURE_WITH_UNIT ( LENGTH_MEASURE( 0.02539999999999999897 ), #11358 );
#7691=CARTESIAN_POINT ( 'NONE',  ( 0.000000000000000000, 3.738758431839877614E-19, 0.004799741732707325965 ) ) ;
#7693=B_SPLINE_CURVE_WITH_KNOTS ( 'NONE', 3,
 ( #22319, #2215, #2082, #17081, #11603, #490 ),
 .UNSPECIFIED., .F., .F.,
 ( 4, 2, 4 ),
 ( 0.006549771812455102565, 0.009815615986340283511, 0.01308146016022546446 ),
 .UNSPECIFIED. ) ;
#7697=CARTESIAN_POINT ( 'NONE',  ( -0.1954553509668046640, 0.1954553509668046918, 0.03277777777777921009 ) ) ;
#7699=VERTEX_POINT ( 'NONE', #9488 ) ;
#7702=CARTESIAN_POINT ( 'NONE',  ( -0.3125000000000000555, 1.913510623667739771E-17, 0.1716666666666689933 ) ) ;
#7704=CARTESIAN_POINT ( 'NONE',  ( -0.1306872919485615459, -0.3155070326520293400, 0.07270833333333487358 ) ) ;
#7705=CARTESIAN_POINT ( 'NONE',  ( -0.04626190099492148711, -0.5145565563726327563, 0.07046568677121804736 ) ) ;
#7718=CARTESIAN_POINT ( 'NONE',  ( -0.2351701443100413791, -0.2046330205465220486, -0.1004527702155444124 ) ) ;
#7724=CARTESIAN_POINT ( 'NONE',  ( 0.3257020783361852523, -0.3421021315173797817, 0.4271664148355318047 ) ) ;
#7730=CARTESIAN_POINT ( 'NONE',  ( 0.4593750000000004219, 0.2760455974562900927, 0.3779506566538943235 ) ) ;
#7738=DIRECTION ( 'NONE',  ( -1.000000000000000000, 0.000000000000000000, 0.000000000000000000 ) ) ;
#7739=B_SPLINE_CURVE_WITH_KNOTS ( 'NONE', 3,
 ( #7505, #17583, #58, #7858, #20552, #3847, #15307, #23171, #15186, #13017 ),
 .UNSPECIFIED., .F., .F.,
 ( 4, 2, 2, 2, 4 ),
 ( 0.000000000000000000, 0.003270554913819859362, 0.006541109827639718724, 0.009811664741459578953, 0.01308221965527943745 ),
 .UNSPECIFIED. ) ;
#7741=CARTESIAN_POINT ( 'NONE',  ( -0.2091198842963307158, -0.4097039017751712975, 0.4343513344076715410 ) ) ;
#7755=CARTESIAN_POINT ( 'NONE',  ( 0.4500000000000003442, -0.2598076211353317899, 0.3779506566538943235 ) ) ;
#7762=CARTESIAN_POINT ( 'NONE',  ( 0.1954553509668047195, 0.1954553509668046085, 0.3452777777777817358 ) ) ;
#7764=CARTESIAN_POINT ( 'NONE',  ( 0.2764156081756483641, -0.1144950937579611167, -0.05402777777777704321 ) ) ;
#7778=CIRCLE ( 'NONE', #373, 0.01874999999999997155 ) ;
#7780=FACE_OUTER_BOUND ( 'NONE', #2416, .T. ) ;
#7784=CARTESIAN_POINT ( 'NONE',  ( -0.1306872919485615459, -0.3155070326520293400, -0.09048611111111044825 ) ) ;
#7790=AXIS2_PLACEMENT_3D ( 'NONE', #6786, #6424, #17765 ) ;
#7794=CARTESIAN_POINT ( 'NONE',  ( 0.3108513798347909418, 0.3617957495396916245, 0.4142710792078267423 ) ) ;
#7795=CARTESIAN_POINT ( 'NONE',  ( -0.2764156081756484196, 1.692557448933383907E-17, 0.09527777777777970969 ) ) ;
#7803=CARTESIAN_POINT ( 'NONE',  ( -0.3830434977118161721, 0.3085929194348118187, 0.4166771511014252805 ) ) ;
#7811=CARTESIAN_POINT ( 'NONE',  ( 0.3125000000000000000, -5.740531871003217465E-17, -0.01583333333333210996 ) ) ;
#7818=CARTESIAN_POINT ( 'NONE',  ( -0.1954553509668046918, -0.1954553509668046640, -0.06444444444444380471 ) ) ;
#7821=LINE ( 'NONE', #381, #14050 ) ;
#7823=CARTESIAN_POINT ( 'NONE',  ( -3.863846776457871776E-17, -0.3155070326520292845, 0.2428472222222251287 ) ) ;
#7824=CARTESIAN_POINT ( 'NONE',  ( 0.4687500000000003886, 0.08771909047139087034, 0.4143497438722636428 ) ) ;
#7828=ADVANCED_FACE ( 'NONE', ( #2736 ), #16687, .F. ) ;
#7833=CARTESIAN_POINT ( 'NONE',  ( 0.3125000000000002220, -0.1294417382415921358, 0.3140277777777816803 ) ) ;
#7834=CARTESIAN_POINT ( 'NONE',  ( -0.1294417382415922746, -0.3125000000000000000, 0.2376388888888918416 ) ) ;
#7838=ORIENTED_EDGE ( 'NONE', *, *, #18127, .T. ) ;
#7840=CARTESIAN_POINT ( 'NONE',  ( 0.06796888784162435915, 0.2795977689546983447, 0.3992516814463595298 ) ) ;
#7858=CARTESIAN_POINT ( 'NONE',  ( -0.3147071693084031452, 0.3721877333702313662, 0.07155713030921627416 ) ) ;
#7869=CARTESIAN_POINT ( 'NONE',  ( 0.3155070326520292290, -0.1306872919485616569, 0.4234027777777825130 ) ) ;
#7874=CARTESIAN_POINT ( 'NONE',  ( 0.1965595339003342046, -0.4277821775561181927, 0.07944544255959536116 ) ) ;
#7875=CARTESIAN_POINT ( 'NONE',  ( -0.1144950937579609779, 0.2764156081756484196, 0.1890277777777804868 ) ) ;
#7877=CARTESIAN_POINT ( 'NONE',  ( 0.1144950937579609085, -0.2764156081756484751, 0.4459722222222269328 ) ) ;
#7878=ORIENTED_EDGE ( 'NONE', *, *, #16716, .T. ) ;
#7880=AXIS2_PLACEMENT_3D ( 'NONE', #19847, #10595, #18023 ) ;
#7882=CARTESIAN_POINT ( 'NONE',  ( -0.1376066337087289981, 0.2509841804965734502, -0.07524251643492650687 ) ) ;
#7891=DIRECTION ( 'NONE',  ( 1.000000000000000000, 0.000000000000000000, 0.000000000000000000 ) ) ;
#7892=ORIENTED_EDGE ( 'NONE', *, *, #11697, .T. ) ;
#7896=CARTESIAN_POINT ( 'NONE',  ( 0.2764156081756483641, 0.1144950937579610056, 0.4529166666666715191 ) ) ;
#7904=CARTESIAN_POINT ( 'NONE',  ( 0.1954553509668046640, -0.1954553509668047195, 0.2272222222222252119 ) ) ;
#7908=CARTESIAN_POINT ( 'NONE',  ( 0.1294417382415924134, 0.3124999999999999445, 0.3279166666666706864 ) ) ;
#7917=ORIENTED_EDGE ( 'NONE', *, *, #1423, .F. ) ;
#7921=B_SPLINE_CURVE_WITH_KNOTS ( 'NONE', 3,
 ( #20409, #1994, #9431, #11148, #16751, #759, #21002, #1123, #13590, #17833, #17467, #641 ),
 .UNSPECIFIED., .F., .F.,
 ( 4, 2, 2, 2, 2, 4 ),
 ( 0.000000000000000000, 0.003345931539952393900, 0.005018897309928590199, 0.006691863079904788666, 0.01003779461985718560, 0.01338372615980958080 ),
 .UNSPECIFIED. ) ;
#7923=FACE_OUTER_BOUND ( 'NONE', #21157, .T. ) ;
#7928=CARTESIAN_POINT ( 'NONE',  ( -3.385114897866767815E-17, -0.2764156081756484196, 0.05361111111111271227 ) ) ;
#7935=CARTESIAN_POINT ( 'NONE',  ( -0.2230971623002954152, -0.2230971623002953874, 0.1247916666666686186 ) ) ;
#7937=CARTESIAN_POINT ( 'NONE',  ( -0.2195630361087207438, -0.1679215936615484350, -0.06558227484231504700 ) ) ;
#7947=CARTESIAN_POINT ( 'NONE',  ( 0.000000000000000000, 0.3125000000000000000, 0.1022222222222240184 ) ) ;
#7953=CARTESIAN_POINT ( 'NONE',  ( -0.2236587330423011055, -0.2167494423014863503, -0.1001684177326861991 ) ) ;
#7958=CARTESIAN_POINT ( 'NONE',  ( 0.2800968539712072602, -5.145295735006237905E-17, 0.3917635206378741186 ) ) ;
#7964=CARTESIAN_POINT ( 'NONE',  ( 0.009374999999999843528, 0.5358532185916217161, 0.3779506566538944345 ) ) ;
#7969=EDGE_CURVE ( 'NONE', #14969, #13125, #7778, .T. ) ;
#7981=EDGE_LOOP ( 'NONE', ( #2283, #8338 ) ) ;
#7984=ORIENTED_EDGE ( 'NONE', *, *, #9464, .T. ) ;
#7988=CARTESIAN_POINT ( 'NONE',  ( 0.4620259694561523744, 0.2880908832651559726, 0.04413116910601654758 ) ) ;
#7994=B_SPLINE_CURVE_WITH_KNOTS ( 'NONE', 3,
 ( #7958, #20889, #17238, #4421, #2245, #10049, #765, #22603, #5887, #13822, #21256, #4543, #19420, #9679, #13348, #20770, #4059, #17118, #405, #7840, #17688, #6954, #18168, #16343, #981, #14515, #4991, #12455, #15977, #23514, #23398, #21936, #16100, #3052, #2930, #6587, #14150, #4750, #19514, #21579, #6706, #23637, #4874, #17929 ),
 .UNSPECIFIED., .F., .F.,
 ( 4, 2, 1, 2, 2, 2, 2, 2, 2, 1, 2, 2, 2, 2, 2, 2, 2, 2, 2, 2, 2, 2, 4 ),
 ( 0.004595939250188698158, 0.005313238532189881215, 0.006030537814191064272, 0.006747837096192247329, 0.007465136378193430386, 0.008899734942195796500, 0.01033433350619816435, 0.01176893207020052873, 0.01248623135220171265, 0.01320353063420289484, 0.01392082991620407877, 0.01463812919820526096, 0.01607272776220762533, 0.01750732632620999318, 0.01894192489021236103, 0.01965922417221354149, 0.02037652345421472194, 0.02181112201821708979, 0.02324572058221945764, 0.02396301986422064156, 0.02468031914622182549, 0.02611491771022419334, 0.02754951627422656119 ),
 .UNSPECIFIED. ) ;
#7996=CARTESIAN_POINT ( 'NONE',  ( -0.2764156081756484196, 0.1144950937579609918, 0.1959722222222249899 ) ) ;
#7998=CARTESIAN_POINT ( 'NONE',  ( 0.2764156081756483641, 0.1144950937579610056, 0.4598611111111158833 ) ) ;
#8001=CARTESIAN_POINT ( 'NONE',  ( 0.004206913933137047291, -0.5383631510497720596, 0.04698599556840569319 ) ) ;
#8010=ORIENTED_EDGE ( 'NONE', *, *, #2129, .T. ) ;
#8013=CARTESIAN_POINT ( 'NONE',  ( 0.3125000000000000000, -5.740531871003217465E-17, 0.09527777777777987622 ) ) ;
#8016=CARTESIAN_POINT ( 'NONE',  ( -0.3155070326520293400, 0.1306872919485614903, -0.1043749999999994543 ) ) ;
#8025=CARTESIAN_POINT ( 'NONE',  ( -0.1054825322677925281, -0.2618223909956075013, -0.07090283079844149350 ) ) ;
#8026=CARTESIAN_POINT ( 'NONE',  ( -0.2764156081756484196, 0.1144950937579609918, 0.2584722222222254340 ) ) ;
#8043=CARTESIAN_POINT ( 'NONE',  ( 0.4225900379021583775, -0.2972834052256092541, 0.3902123106865083013 ) ) ;
#8044=CARTESIAN_POINT ( 'NONE',  ( -0.4687500000000003886, -0.2150850509746254080, 0.05816300916149743511 ) ) ;
#8049=DIRECTION ( 'NONE',  ( 1.000000000000000000, 0.000000000000000000, 0.000000000000000000 ) ) ;
#8051=CARTESIAN_POINT ( 'NONE',  ( 0.1144950937579609085, -0.2764156081756484751, -0.05402777777777704321 ) ) ;
#8053=CARTESIAN_POINT ( 'NONE',  ( -0.3125000000000002776, -0.1294417382415919415, 0.3487500000000041678 ) ) ;
#8059=CARTESIAN_POINT ( 'NONE',  ( 0.2230971623002954429, 0.2230971623002953319, 0.2081250000000026412 ) ) ;
#8061=CARTESIAN_POINT ( 'NONE',  ( -0.2688584691416579520, -0.07459580784763643335, -0.06776396657361484499 ) ) ;
#8070=CARTESIAN_POINT ( 'NONE',  ( 0.2085087158397508078, -0.1823754829288359303, 0.3880822748423157220 ) ) ;
#8076=ORIENTED_EDGE ( 'NONE', *, *, #20394, .T. ) ;
#8081=CARTESIAN_POINT ( 'NONE',  ( 0.2142276530138180479, 0.4175814842298848917, 0.4181133580835095231 ) ) ;
#8089=CARTESIAN_POINT ( 'NONE',  ( -0.4593750000000003664, -0.2760455974562901482, 0.3779506566538943235 ) ) ;
#8098=ADVANCED_FACE ( 'NONE', ( #22471 ), #5824, .T. ) ;
#8102=CARTESIAN_POINT ( 'NONE',  ( 0.4683334081279746930, 0.2655573993979199465, 0.04698409998688510975 ) ) ;
#8103=CARTESIAN_POINT ( 'NONE',  ( 0.3125000000000000000, -5.740531871003217465E-17, 0.2550000000000030020 ) ) ;
#8106=CARTESIAN_POINT ( 'NONE',  ( -0.4687500000000004441, -0.08803459774007682537, 0.4135153894406012887 ) ) ;
#8107=CARTESIAN_POINT ( 'NONE',  ( 0.4620259694561524855, -0.2880908832651559170, 0.04413116910601655452 ) ) ;
#8109=CARTESIAN_POINT ( 'NONE',  ( -0.2764156081756484196, 0.1144950937579609918, 0.2515277777777809587 ) ) ;
#8111=CARTESIAN_POINT ( 'NONE',  ( -0.2764156081756484196, 1.692557448933383907E-17, 0.4286111111111156613 ) ) ;
#8112=ORIENTED_EDGE ( 'NONE', *, *, #6373, .T. ) ;
#8125=CARTESIAN_POINT ( 'NONE',  ( -0.3125000000000000000, 1.913510623667739771E-17, 0.1716666666666689933 ) ) ;
#8130=ADVANCED_FACE ( 'NONE', ( #9064 ), #6492, .F. ) ;
#8134=CARTESIAN_POINT ( 'NONE',  ( 0.1306872919485614071, -0.3155070326520293955, -0.1390972222222219556 ) ) ;
#8137=ORIENTED_EDGE ( 'NONE', *, *, #16678, .T. ) ;
#8143=CARTESIAN_POINT ( 'NONE',  ( 0.2764156081756483641, 0.1144950937579610056, 0.2931944444444479214 ) ) ;
#8146=FACE_OUTER_BOUND ( 'NONE', #9450, .T. ) ;
#8154=DIRECTION ( 'NONE',  ( -1.000000000000000000, 0.000000000000000000, 0.000000000000000000 ) ) ;
#8157=EDGE_CURVE ( 'NONE', #5331, #4062, #8986, .T. ) ;
#8159=EDGE_CURVE ( 'NONE', #23837, #3289, #3216, .T. ) ;
#8160=CARTESIAN_POINT ( 'NONE',  ( 0.09145417301143894673, -0.5014751291207466544, 0.06110928887248360392 ) ) ;
#8161=CARTESIAN_POINT ( 'NONE',  ( 0.1578986201652094745, -0.4501030665082204063, 0.4142710792078265758 ) ) ;
#8164=CARTESIAN_POINT ( 'NONE',  ( 0.4687500000000002776, -0.2598076211353317344, 0.4425000000000000044 ) ) ;
#8171=LINE ( 'NONE', #982, #23216 ) ;
#8174=CARTESIAN_POINT ( 'NONE',  ( 0.2230971623002953874, -0.2230971623002954429, 0.2497916666666696317 ) ) ;
#8182=CONICAL_SURFACE ( 'NONE', #12119, 0.3308333333333332571, 0.7853981633974427279 ) ;
#8187=CARTESIAN_POINT ( 'NONE',  ( -0.1294417382415922191, 0.3125000000000000000, 0.1056944444444462838 ) ) ;
#8189=CARTESIAN_POINT ( 'NONE',  ( 0.1229229017544715696, -0.2477443904640376227, 0.3880822748423153334 ) ) ;
#8192=ORIENTED_EDGE ( 'NONE', *, *, #10311, .T. ) ;
#8197=AXIS2_PLACEMENT_3D ( 'NONE', #15806, #10211, #4703 ) ;
#8201=AXIS2_PLACEMENT_3D ( 'NONE', #13319, #4033, #8049 ) ;
#8203=CARTESIAN_POINT ( 'NONE',  ( 0.04282247326130569909, 0.5165423109005278235, 0.4011144384304308752 ) ) ;
#8208=CARTESIAN_POINT ( 'NONE',  ( -0.09135502326330770251, -0.5015332108058754290, 0.06108558933789662304 ) ) ;
#8221=B_SPLINE_CURVE_WITH_KNOTS ( 'NONE', 3,
 ( #8556, #6368, #23179, #11880, #4296, #8189, #19294, #21252, #2598, #4539, #8070, #10408 ),
 .UNSPECIFIED., .F., .F.,
 ( 4, 2, 2, 2, 2, 4 ),
 ( 5.846333392818911776E-17, 0.001386135995484567536, 0.002079203993226821489, 0.002772271990969075225, 0.004158407986453582263, 0.005544543981938090602 ),
 .UNSPECIFIED. ) ;
#8223=CARTESIAN_POINT ( 'NONE',  ( -0.2111984196243033851, -0.4085062965502692101, 0.4344098397133764333 ) ) ;
#8224=CARTESIAN_POINT ( 'NONE',  ( -0.2209708691207961095, 0.2209708691207961373, 0.2758333333333364834 ) ) ;
#8225=CARTESIAN_POINT ( 'NONE',  ( 0.4584515285649273242, 0.2213539724899254713, 0.4064761396644160363 ) ) ;
#8228=CARTESIAN_POINT ( 'NONE',  ( -0.3125000000000000000, 1.913510623667739771E-17, -0.09916666666666609786 ) ) ;
#8233=CARTESIAN_POINT ( 'NONE',  ( 0.2764156081756483641, -0.1144950937579611167, 0.1681944444444469777 ) ) ;
#8237=CARTESIAN_POINT ( 'NONE',  ( 0.4587493717650694691, -0.1772960527124521901, 0.4158887382153850787 ) ) ;
#8238=DIRECTION ( 'NONE',  ( 0.9063077870366478273, 1.109906930436751740E-16, -0.4226182617407038267 ) ) ;
#8240=PLANE ( 'NONE',  #17802 ) ;
#8247=VERTEX_POINT ( 'NONE', #15162 ) ;
#8253=CARTESIAN_POINT ( 'NONE',  ( 0.1306872919485614071, -0.3155070326520293955, 0.1386805555555580272 ) ) ;
#8257=CARTESIAN_POINT ( 'NONE',  ( -0.1586475693114280106, -0.4496706605170417981, 0.08858850926231189027 ) ) ;
#8263=CARTESIAN_POINT ( 'NONE',  ( -0.2764156081756484196, 0.1144950937579609918, 0.3140277777777814583 ) ) ;
#8273=DIRECTION ( 'NONE',  ( -0.000000000000000000, -0.9607689228305225093, 0.2773500981126159615 ) ) ;
#8283=CARTESIAN_POINT ( 'NONE',  ( -0.1144950937579609918, -0.2764156081756484196, 0.09875000000000196121 ) ) ;
#8287=CARTESIAN_POINT ( 'NONE',  ( 0.3830434977118160611, -0.3085929194348117632, 0.4166771511014250029 ) ) ;
#8288=CARTESIAN_POINT ( 'NONE',  ( 0.3125000000000000000, -5.740531871003217465E-17, 0.3105555555555590819 ) ) ;
#8289=CARTESIAN_POINT ( 'NONE',  ( -0.1954553509668046640, 0.1954553509668046918, 0.3105555555555591929 ) ) ;
#8294=CARTESIAN_POINT ( 'NONE',  ( -0.1294417382415922191, 0.3125000000000000000, -0.005416666666665734438 ) ) ;
#8295=CARTESIAN_POINT ( 'NONE',  ( -0.3155070326520292845, 1.931923388228935888E-17, 0.2845138888888921191 ) ) ;
#8307=ORIENTED_EDGE ( 'NONE', *, *, #2102, .T. ) ;
#8318=VERTEX_POINT ( 'NONE', #4767 ) ;
#8332=DIRECTION ( 'NONE',  ( 1.000000000000000000, 0.000000000000000000, 0.000000000000000000 ) ) ;
#8338=ORIENTED_EDGE ( 'NONE', *, *, #23147, .T. ) ;
#8344=CARTESIAN_POINT ( 'NONE',  ( 0.2726274893998235638, 0.3838643229717945138, 0.09139053646024344890 ) ) ;
#8347=CARTESIAN_POINT ( 'NONE',  ( -0.3125000000000000000, -0.1294417382415921913, -0.09569444444444386022 ) ) ;
#8351=CARTESIAN_POINT ( 'NONE',  ( 0.1954553509668046640, -0.1954553509668047195, 0.05361111111111271227 ) ) ;
#8356=CARTESIAN_POINT ( 'NONE',  ( 0.6391249999999999432, 7.864411439368920513E-17, 0.000000000000000000 ) ) ;
#8360=CARTESIAN_POINT ( 'NONE',  ( 0.1294417382415924134, 0.3124999999999999445, 0.1543055555555577496 ) ) ;
#8366=CARTESIAN_POINT ( 'NONE',  ( 0.3125000000000000000, 3.827021247335477694E-17, 1.326383476483184332 ) ) ;
#8367=CARTESIAN_POINT ( 'NONE',  ( 0.000000000000000000, 0.3155070326520292845, 0.05187500000000178774 ) ) ;
#8369=CARTESIAN_POINT ( 'NONE',  ( 0.009374999999999746383, 0.5358532185916217161, 0.4425000000000000044 ) ) ;
#8370=ORIENTED_EDGE ( 'NONE', *, *, #8853, .F. ) ;
#8373=CARTESIAN_POINT ( 'NONE',  ( -0.2764156081756484196, -0.1144950937579609362, -0.06791666666666604235 ) ) ;
#8374=CARTESIAN_POINT ( 'NONE',  ( -0.3124999999999996114, -0.1294417382415925799, 0.4043055555555600811 ) ) ;
#8375=CARTESIAN_POINT ( 'NONE',  ( -0.1459302940035950014, -0.2450006702335510156, -0.07419985852680419103 ) ) ;
#8376=CARTESIAN_POINT ( 'NONE',  ( -0.1144950937579609779, 0.2764156081756484196, 0.3626388888888929518 ) ) ;
#8381=FACE_OUTER_BOUND ( 'NONE', #10462, .T. ) ;
#8389=ORIENTED_EDGE ( 'NONE', *, *, #16716, .F. ) ;
#8399=CARTESIAN_POINT ( 'NONE',  ( -0.4687500000000003886, 0.2598076211353315124, 0.06112444011295379426 ) ) ;
#8400=CARTESIAN_POINT ( 'NONE',  ( 0.1954553509668047195, 0.1954553509668046085, 0.1230555555555576941 ) ) ;
#8404=CARTESIAN_POINT ( 'NONE',  ( 0.3124999999999999445, -0.1294417382415923856, 0.3070833333333367055 ) ) ;
#8405=CARTESIAN_POINT ( 'NONE',  ( -0.2764156081756484196, 1.692557448933383907E-17, 0.1508333333333356785 ) ) ;
#8410=CARTESIAN_POINT ( 'NONE',  ( -0.3125000000000000000, 0.1294417382415922468, -0.04708333333333236670 ) ) ;
#8414=CARTESIAN_POINT ( 'NONE',  ( 0.2230971623002953874, -0.2230971623002954429, 0.4720138888888936179 ) ) ;
#8415=CARTESIAN_POINT ( 'NONE',  ( -0.2209708691207961095, 0.2209708691207961373, 0.05361111111111253186 ) ) ;
#8421=ORIENTED_EDGE ( 'NONE', *, *, #24038, .F. ) ;
#8425=EDGE_CURVE ( 'NONE', #3858, #16949, #3862, .T. ) ;
#8437=ORIENTED_EDGE ( 'NONE', *, *, #6164, .F. ) ;
#8442=VERTEX_POINT ( 'NONE', #21599 ) ;
#8449=LINE ( 'NONE', #13955, #15851 ) ;
#8454=CARTESIAN_POINT ( 'NONE',  ( -0.4641327083039736845, -0.2728248698625184154, 0.04698599556840495767 ) ) ;
#8463=VERTEX_POINT ( 'NONE', #21839 ) ;
#8466=CARTESIAN_POINT ( 'NONE',  ( -0.2209708691207961095, 0.2209708691207961373, 0.06055555555555736796 ) ) ;
#8471=CARTESIAN_POINT ( 'NONE',  ( -0.4687500000000002220, -0.2630787017013382356, 0.3892820121258429023 ) ) ;
#8473=ORIENTED_EDGE ( 'NONE', *, *, #17600, .F. ) ;
#8474=CARTESIAN_POINT ( 'NONE',  ( 0.2195630361086305937, -0.1679215936616662852, 0.3880822748423153334 ) ) ;
#8475=CARTESIAN_POINT ( 'NONE',  ( 0.1144950937579611444, 0.2764156081756483641, 0.07097222222222394905 ) ) ;
#8481=CARTESIAN_POINT ( 'NONE',  ( -0.4679361169221507022, 0.2662350510444109197, 0.05893285591566550796 ) ) ;
#8486=CARTESIAN_POINT ( 'NONE',  ( 0.4593750000000004774, 0.2760455974562900372, 0.06112444011295366936 ) ) ;
#8491=CARTESIAN_POINT ( 'NONE',  ( 0.1306872919485614071, -0.3155070326520293955, -0.02798611111110996946 ) ) ;
#8500=CARTESIAN_POINT ( 'NONE',  ( 0.000000000000000000, 0.2764156081756484196, -0.02972222222222129645 ) ) ;
#8503=CARTESIAN_POINT ( 'NONE',  ( -0.1144950937579609918, -0.2764156081756484196, 0.3279166666666703533 ) ) ;
#8505=DIRECTION ( 'NONE',  ( 1.224646799147353207E-16, 1.000000000000000000, -0.000000000000000000 ) ) ;
#8517=ORIENTED_EDGE ( 'NONE', *, *, #21130, .T. ) ;
#8525=CARTESIAN_POINT ( 'NONE',  ( 0.1954553509668046640, -0.1954553509668047195, -0.05749999999999928085 ) ) ;
#8530=CARTESIAN_POINT ( 'NONE',  ( -0.1954553509668046918, -0.1954553509668046640, 0.1022222222222241989 ) ) ;
#8534=CARTESIAN_POINT ( 'NONE',  ( 0.4800180224839157850, -0.1716599939501584626, 0.06108543995043075325 ) ) ;
#8535=CARTESIAN_POINT ( 'NONE',  ( 0.4795759075923620163, -5.969813580926603513E-13, 0.07439896364136204532 ) ) ;
#8539=CARTESIAN_POINT ( 'NONE',  ( -3.863846776457871776E-17, -0.3155070326520292845, 0.2984027777777810697 ) ) ;
#8540=VERTEX_POINT ( 'NONE', #10755 ) ;
#8543=FACE_OUTER_BOUND ( 'NONE', #1675, .T. ) ;
#8553=ORIENTED_EDGE ( 'NONE', *, *, #16516, .F. ) ;
#8556=CARTESIAN_POINT ( 'NONE',  ( 0.03651601414450977162, -0.2739930093161348501, 0.3880822748423153890 ) ) ;
#8564=EDGE_CURVE ( 'NONE', #14213, #17904, #16232, .T. ) ;
#8586=CARTESIAN_POINT ( 'NONE',  ( -0.4692112248683376619, -0.2611554184491534092, 0.04763613967037600566 ) ) ;
#8592=VERTEX_POINT ( 'NONE', #19259 ) ;
#8594=VECTOR ( 'NONE', #15779, 39.37007874015748143 ) ;
#8595=EDGE_CURVE ( 'NONE', #22303, #18060, #19095, .T. ) ;
#8599=CARTESIAN_POINT ( 'NONE',  ( -0.1294417382415922191, 0.3125000000000000000, 0.05708333333333515114 ) ) ;
#8608=CARTESIAN_POINT ( 'NONE',  ( -0.1144950937579609918, -0.2764156081756484196, 0.1543055555555579716 ) ) ;
#8610=CARTESIAN_POINT ( 'NONE',  ( -0.3125000000000000000, -0.1294417382415921913, 0.3973611111111152727 ) ) ;
#8612=CARTESIAN_POINT ( 'NONE',  ( 0.2209708691207961095, -0.2209708691207961651, -0.02972222222222147686 ) ) ;
#8613=CARTESIAN_POINT ( 'NONE',  ( -0.4687500000000004441, 0.2629256801278679334, 0.05975678175779900597 ) ) ;
#8620=CARTESIAN_POINT ( 'NONE',  ( -0.3125000000000004996, 0.1294417382415917195, 0.2306944444444476439 ) ) ;
#8621=CARTESIAN_POINT ( 'NONE',  ( -0.1306872919485614903, 0.3155070326520293400, 0.1109027777777800150 ) ) ;
#8626=CARTESIAN_POINT ( 'NONE',  ( -3.385114897866767815E-17, -0.2764156081756484196, 0.05361111111111271227 ) ) ;
#8629=CARTESIAN_POINT ( 'NONE',  ( -3.385114897866767815E-17, -0.2764156081756484196, 0.3869444444444486431 ) ) ;
#8639=CARTESIAN_POINT ( 'NONE',  ( -0.4254812175018319320, 0.2956141819054338149, 0.4012599972956991667 ) ) ;
#8644=CARTESIAN_POINT ( 'NONE',  ( -0.4645343760433822689, -0.2721270390806222461, 0.05893285591566541776 ) ) ;
#8645=CARTESIAN_POINT ( 'NONE',  ( -0.1954553509668046918, -0.1954553509668046640, 0.09527777777777970969 ) ) ;
#8648=CARTESIAN_POINT ( 'NONE',  ( -3.385114897866767815E-17, -0.2764156081756484196, 0.2758333333333366499 ) ) ;
#8652=CARTESIAN_POINT ( 'NONE',  ( -0.4795759075923621273, -5.504308098328212156E-13, 0.07439896364136201756 ) ) ;
#8654=CARTESIAN_POINT ( 'NONE',  ( -0.1954553509668046640, 0.1954553509668046918, 0.08138888888889070361 ) ) ;
#8655=CARTESIAN_POINT ( 'NONE',  ( -3.863846776457871776E-17, -0.3155070326520292845, 0.3539583333333371495 ) ) ;
#8665=DIRECTION ( 'NONE',  ( 0.000000000000000000, 0.000000000000000000, 1.000000000000000000 ) ) ;
#8670=EDGE_CURVE ( 'NONE', #10191, #4025, #6896, .T. ) ;
#8677=EDGE_CURVE ( 'NONE', #16468, #2585, #17255, .T. ) ;
#8682=VERTEX_POINT ( 'NONE', #15959 ) ;
#8688=CARTESIAN_POINT ( 'NONE',  ( -0.4795759075923621273, -5.504308098328212156E-13, 0.07439896364136201756 ) ) ;
#8689=DIRECTION ( 'NONE',  ( 0.000000000000000000, 0.000000000000000000, -1.000000000000000000 ) ) ;
#8695=CARTESIAN_POINT ( 'NONE',  ( -0.4570242136016807732, -0.2774028246161672762, 0.04874733047933989954 ) ) ;
#8698=VECTOR ( 'NONE', #20610, 39.37007874015748143 ) ;
#8707=CARTESIAN_POINT ( 'NONE',  ( 0.2209708691207961095, -0.2209708691207961651, 0.2550000000000033906 ) ) ;
#8712=AXIS2_PLACEMENT_3D ( 'NONE', #9054, #10535, #14679 ) ;
#8713=CARTESIAN_POINT ( 'NONE',  ( -0.4687500000000003886, -0.1103614930154983020, 0.4107126734332217644 ) ) ;
#8718=CARTESIAN_POINT ( 'NONE',  ( 0.2764156081756484196, -5.077672346800151106E-17, 0.005000000000001210074 ) ) ;
#8720=CARTESIAN_POINT ( 'NONE',  ( 0.2872991414527151233, 0.07488537861673724705, -0.08546435887091462236 ) ) ;
#8732=CARTESIAN_POINT ( 'NONE',  ( -0.3155070326520292845, 1.931923388228935888E-17, 0.2324305555555587766 ) ) ;
#8738=CARTESIAN_POINT ( 'NONE',  ( 0.1144950937579611444, 0.2764156081756483641, 0.02236111111111246247 ) ) ;
#8740=CARTESIAN_POINT ( 'NONE',  ( -0.1144950937579609918, -0.2764156081756484196, 0.4390277777777824020 ) ) ;
#8742=ORIENTED_EDGE ( 'NONE', *, *, #16450, .F. ) ;
#8758=B_SPLINE_CURVE_WITH_KNOTS ( 'NONE', 3,
 ( #454, #14980, #17283, #20579, #15458, #22765, #22650, #3876 ),
 .UNSPECIFIED., .F., .F.,
 ( 4, 2, 2, 4 ),
 ( 1.149246120147598830E-16, 0.002297969625094406759, 0.003446954437641552675, 0.004595939250188698158 ),
 .UNSPECIFIED. ) ;
#8759=EDGE_CURVE ( 'NONE', #18060, #3460, #23930, .T. ) ;
#8761=EDGE_CURVE ( 'NONE', #15581, #23410, #18667, .T. ) ;
#8763=CARTESIAN_POINT ( 'NONE',  ( -0.1229229017546027425, -0.2477443904639724803, -0.06558227484231506088 ) ) ;
#8764=CARTESIAN_POINT ( 'NONE',  ( -0.1144950937579609779, 0.2764156081756484196, 0.02236111111111246247 ) ) ;
#8766=CARTESIAN_POINT ( 'NONE',  ( -0.3125000000000000000, 1.913510623667739771E-17, -0.05055555555555497210 ) ) ;
#8768=CARTESIAN_POINT ( 'NONE',  ( 0.2764156081756483641, 0.1144950937579610195, 0.2931944444444479214 ) ) ;
#8774=PLANE ( 'NONE',  #1577 ) ;
#8775=CARTESIAN_POINT ( 'NONE',  ( 0.000000000000000000, 0.2764156081756484196, 0.01888888888889020401 ) ) ;
#8776=CARTESIAN_POINT ( 'NONE',  ( 0.3155070326520292290, 0.1306872919485615736, 0.3713194444444484765 ) ) ;
#8779=CARTESIAN_POINT ( 'NONE',  ( 0.3885631146789285117, 0.3299392016703767139, 0.06110928887248361085 ) ) ;
#8797=VERTEX_POINT ( 'NONE', #10369 ) ;
#8829=CARTESIAN_POINT ( 'NONE',  ( 0.03750733961385147031, -0.5077191469176455252, 0.4064695056028757025 ) ) ;
#8830=CARTESIAN_POINT ( 'NONE',  ( -3.827021247335479543E-17, -0.3125000000000000000, 0.2480555555555588598 ) ) ;
#8838=( BOUNDED_CURVE ( )  B_SPLINE_CURVE ( 2, ( #1342, #8410, #15858, #6830, #1225, #10616, #21707, #1464, #18046 ),
 .UNSPECIFIED., .F., .T. ) 
 B_SPLINE_CURVE_WITH_KNOTS ( ( 3, 2, 2, 2, 3 ),
 ( 0.7395833333333333703, 0.7500000000000000000, 0.7604166666666667407, 0.7708333333333334814, 0.7812500000000001110 ),
 .UNSPECIFIED. ) 
 CURVE ( )  GEOMETRIC_REPRESENTATION_ITEM ( )  RATIONAL_B_SPLINE_CURVE ( ( 1.000000000000000000, 0.9238795325112867385, 1.000000000000000000, 0.9238795325112867385, 1.000000000000000000, 0.9238795325112867385, 1.000000000000000000, 0.9238795325112859613, 1.000000000000000888 ) ) 
 REPRESENTATION_ITEM ( '' )  );
#8840=( BOUNDED_SURFACE ( )  B_SPLINE_SURFACE ( 1, 2, ( 
 ( #20274, #24037, #9053, #3927, #10893, #3808, #7232, #16499, #11254, #2094, #18560, #23791, #16734, #3685, #22458, #5757, #16618, #7463, #11132, #13218, #23911, #20628, #7111, #11372, #13100, #12737, #1850, #3442, #7347, #14799, #5634, #14677, #22214, #22096, #5392, #3561, #14912, #20513, #5514, #9293, #18799, #9536, #21975, #12976, #15, #18678, #1979, #9417, #16854, #141, #264, #23046, #22933, #6107, #20749, #7704, #2464, #11862, #4163, #9658, #19277, #5868, #18929, #22696, #20986, #11613, #19045, #20869, #9903, #6229, #7935, #2347, #383, #17334, #628, #6352, #11987, #15389, #4041, #15151, #11494, #22817, #17452, #2583, #13802, #9785, #15507, #2227, #13576, #22580, #17217, #13327, #21111, #501, #8059, #2698, #4282, #11737, #10030, #17097, #19158, #13693, #4400, #16969, #7823, #746, #8174, #15269, #15628, #19400, #21233, #4524, #5987, #13451, #23402, #21470, #8295, #17574, #19635, #4754, #8539, #15980, #4878, #19761, #15862, #21583, #23518, #12225, #17935, #16104, #4995, #21711, #2811, #23277, #2934, #1346, #8655, #12345, #5113, #10266, #12580, #8776, #3171, #1105, #864, #6957, #4642, #10392, #21823, #12459, #13924, #3056, #1229, #985, #6710, #10503, #6834, #14154, #14275, #19877, #10621, #18050, #15749, #17814, #20001, #16229, #23640, #14399, #10150, #23160, #8414, #6470, #6591, #21352, #12108, #19518, #17692, #14040, #22065 ),
 ( #12825, #14643, #1703, #9141, #22184, #12949, #9025, #14768, #16704, #5359, #11098, #9264, #22302, #14884, #20122, #16465, #20244, #18650, #1819, #5484, #22426, #3413, #5728, #1942, #20482, #18410, #18172, #111, #21941, #3533, #15004, #5599, #7080, #20360, #18529, #18292, #16586, #3651, #24123, #7318, #7437, #13064, #3778, #24007, #1468, #10984, #13187, #11221, #9389, #16829, #7552, #3288, #1589, #10742, #23877, #14519, #8903, #16347, #23759, #5234, #12707, #10863, #7198, #9750, #238, #11341, #6079, #15477, #7795, #13304, #22903, #9506, #22550, #2197, #473, #15239, #22668, #354, #13545, #2432, #11588, #5956, #4015, #20960, #4253, #9997, #15595, #19017, #7674, #18770, #15124, #2313, #21078, #6197, #17422, #13416, #19128, #5841, #17187, #2066, #20839, #16940, #594, #4131, #11705, #6319, #7904, #15356, #13663, #20719, #22785, #9874, #17301, #20600, #11463, #8026, #4368, #18896, #11825, #23017, #2549, #9628, #19245, #17061, #715, #8143, #3897, #15713, #21438, #2667, #19485, #8263, #4843, #12309, #17659, #8503, #4963, #19842, #18018, #19369, #16196, #6678, #14123, #946, #1071, #8376, #23610, #17779, #4723, #1316, #4610, #2895, #8629, #10117, #12430, #14243, #12195, #17903, #10232, #19723, #23246, #17542, #19602, #15943, #21552, #3026, #3141, #8740, #12072, #15827, #10473, #6555, #2779, #10591, #10355, #1197, #835, #14005, #16074 ) ),
 .UNSPECIFIED., .F., .F., .F. ) 
 B_SPLINE_SURFACE_WITH_KNOTS ( ( 2, 2 ),
 ( 3, 2, 2, 2, 2, 2, 2, 2, 2, 2, 2, 2, 2, 2, 2, 2, 2, 2, 2, 2, 2, 2, 2, 2, 2, 2, 2, 2, 2, 2, 2, 2, 2, 2, 2, 2, 2, 2, 2, 2, 2, 2, 2, 2, 2, 2, 2, 2, 2, 2, 2, 2, 2, 2, 2, 2, 2, 2, 2, 2, 2, 2, 2, 2, 2, 2, 2, 2, 2, 2, 2, 2, 2, 2, 2, 2, 2, 2, 2, 2, 2, 2, 2, 2, 2, 2, 2, 2, 2, 3 ),
 ( 0.000000000000000000, 1.000000000000000000 ),
 ( 0.000000000000000000, 0.01041666666666666609, 0.02083333333333333218, 0.03125000000000000000, 0.04166666666666666435, 0.05208333333333333565, 0.06250000000000000000, 0.07291666666666667129, 0.08333333333333332871, 0.09375000000000000000, 0.1041666666666666713, 0.1145833333333333287, 0.1250000000000000000, 0.1354166666666666574, 0.1458333333333333426, 0.1562500000000000000, 0.1666666666666666574, 0.1770833333333333426, 0.1875000000000000000, 0.1979166666666666574, 0.2083333333333333426, 0.2187500000000000000, 0.2291666666666666574, 0.2395833333333333426, 0.2500000000000000000, 0.2604166666666666852, 0.2708333333333333148, 0.2812500000000000000, 0.2916666666666666852, 0.3020833333333333148, 0.3125000000000000000, 0.3229166666666666852, 0.3333333333333333148, 0.3437500000000000000, 0.3541666666666666852, 0.3645833333333333148, 0.3750000000000000000, 0.3854166666666666852, 0.3958333333333333148, 0.4062500000000000000, 0.4166666666666666852, 0.4270833333333333148, 0.4375000000000000000, 0.4479166666666666852, 0.4583333333333333148, 0.4687500000000000000, 0.4791666666666666852, 0.4895833333333333148, 0.5000000000000000000, 0.5104166666666666297, 0.5208333333333333703, 0.5312500000000000000, 0.5416666666666666297, 0.5520833333333333703, 0.5625000000000000000, 0.5729166666666666297, 0.5833333333333333703, 0.5937500000000000000, 0.6041666666666666297, 0.6145833333333333703, 0.6250000000000000000, 0.6354166666666666297, 0.6458333333333333703, 0.6562500000000000000, 0.6666666666666666297, 0.6770833333333333703, 0.6875000000000000000, 0.6979166666666666297, 0.7083333333333333703, 0.7187500000000000000, 0.7291666666666666297, 0.7395833333333333703, 0.7500000000000000000, 0.7604166666666666297, 0.7708333333333333703, 0.7812500000000000000, 0.7916666666666666297, 0.8020833333333333703, 0.8125000000000000000, 0.8229166666666666297, 0.8333333333333333703, 0.8437500000000000000, 0.8541666666666666297, 0.8645833333333333703, 0.8750000000000000000, 0.8854166666666666297, 0.8958333333333333703, 0.9062500000000000000, 0.9166666666666666297, 0.9270833333333333703 ),
 .UNSPECIFIED. ) 
 GEOMETRIC_REPRESENTATION_ITEM ( )  RATIONAL_B_SPLINE_SURFACE ( (
 ( 1.000000000000000000, 0.9238795325112867385, 1.000000000000000000, 0.9238795325112867385, 1.000000000000000000, 0.9238795325112867385, 1.000000000000000000, 0.9238795325112867385, 1.000000000000000000, 0.9238795325112867385, 1.000000000000000000, 0.9238795325112867385, 1.000000000000000000, 0.9238795325112867385, 1.000000000000000000, 0.9238795325112867385, 1.000000000000000000, 0.9238795325112867385, 1.000000000000000000, 0.9238795325112867385, 1.000000000000000000, 0.9238795325112867385, 1.000000000000000000, 0.9238795325112867385, 1.000000000000000000, 0.9238795325112867385, 1.000000000000000000, 0.9238795325112867385, 1.000000000000000000, 0.9238795325112867385, 1.000000000000000000, 0.9238795325112867385, 1.000000000000000000, 0.9238795325112867385, 1.000000000000000000, 0.9238795325112867385, 1.000000000000000000, 0.9238795325112867385, 1.000000000000000000, 0.9238795325112867385, 1.000000000000000000, 0.9238795325112867385, 1.000000000000000000, 0.9238795325112867385, 1.000000000000000000, 0.9238795325112867385, 1.000000000000000000, 0.9238795325112867385, 1.000000000000000000, 0.9238795325112867385, 1.000000000000000000, 0.9238795325112867385, 1.000000000000000000, 0.9238795325112867385, 1.000000000000000000, 0.9238795325112867385, 1.000000000000000000, 0.9238795325112867385, 1.000000000000000000, 0.9238795325112867385, 1.000000000000000000, 0.9238795325112867385, 1.000000000000000000, 0.9238795325112867385, 1.000000000000000000, 0.9238795325112867385, 1.000000000000000000, 0.9238795325112867385, 1.000000000000000000, 0.9238795325112867385, 1.000000000000000000, 0.9238795325112867385, 1.000000000000000000, 0.9238795325112867385, 1.000000000000000000, 0.9238795325112867385, 1.000000000000000000, 0.9238795325112867385, 1.000000000000000000, 0.9238795325112867385, 1.000000000000000000, 0.9238795325112867385, 1.000000000000000000, 0.9238795325112867385, 1.000000000000000000, 0.9238795325112867385, 1.000000000000000000, 0.9238795325112867385, 1.000000000000000000, 0.9238795325112867385, 1.000000000000000000, 0.9238795325112867385, 1.000000000000000000, 0.9238795325112867385, 1.000000000000000000, 0.9238795325112867385, 1.000000000000000000, 0.9238795325112867385, 1.000000000000000000, 0.9238795325112867385, 1.000000000000000000, 0.9238795325112867385, 1.000000000000000000, 0.9238795325112867385, 1.000000000000000000, 0.9238795325112867385, 1.000000000000000000, 0.9238795325112867385, 1.000000000000000000, 0.9238795325112867385, 1.000000000000000000, 0.9238795325112867385, 1.000000000000000000, 0.9238795325112867385, 1.000000000000000000, 0.9238795325112867385, 1.000000000000000000, 0.9238795325112867385, 1.000000000000000000, 0.9238795325112867385, 1.000000000000000000, 0.9238795325112867385, 1.000000000000000000, 0.9238795325112867385, 1.000000000000000000, 0.9238795325112867385, 1.000000000000000000, 0.9238795325112867385, 1.000000000000000000, 0.9238795325112867385, 1.000000000000000000, 0.9238795325112867385, 1.000000000000000000, 0.9238795325112867385, 1.000000000000000000, 0.9238795325112867385, 1.000000000000000000, 0.9238795325112867385, 1.000000000000000000, 0.9238795325112867385, 1.000000000000000000, 0.9238795325112867385, 1.000000000000000000, 0.9238795325112867385, 1.000000000000000000, 0.9238795325112867385, 1.000000000000000000, 0.9238795325112867385, 1.000000000000000000, 0.9238795325112867385, 1.000000000000000000, 0.9238795325112867385, 1.000000000000000000, 0.9238795325112867385, 1.000000000000000000, 0.9238795325112867385, 1.000000000000000000, 0.9238795325112867385, 1.000000000000000000, 0.9238795325112867385, 1.000000000000000000, 0.9238795325112867385, 1.000000000000000000, 0.9238795325112867385, 1.000000000000000000, 0.9238795325112867385, 1.000000000000000000, 0.9238795325112867385, 1.000000000000000000, 0.9238795325112867385, 1.000000000000000000, 0.9238795325112867385, 1.000000000000000000, 0.9238795325112867385, 1.000000000000000000, 0.9238795325112867385, 1.000000000000000000, 0.9238795325112867385, 1.000000000000000000),
 ( 1.000000000000000000, 0.9238795325112867385, 1.000000000000000000, 0.9238795325112867385, 1.000000000000000000, 0.9238795325112867385, 1.000000000000000000, 0.9238795325112867385, 1.000000000000000000, 0.9238795325112867385, 1.000000000000000000, 0.9238795325112867385, 1.000000000000000000, 0.9238795325112867385, 1.000000000000000000, 0.9238795325112867385, 1.000000000000000000, 0.9238795325112867385, 1.000000000000000000, 0.9238795325112867385, 1.000000000000000000, 0.9238795325112867385, 1.000000000000000000, 0.9238795325112867385, 1.000000000000000000, 0.9238795325112867385, 1.000000000000000000, 0.9238795325112867385, 1.000000000000000000, 0.9238795325112867385, 1.000000000000000000, 0.9238795325112867385, 1.000000000000000000, 0.9238795325112867385, 1.000000000000000000, 0.9238795325112867385, 1.000000000000000000, 0.9238795325112867385, 1.000000000000000000, 0.9238795325112867385, 1.000000000000000000, 0.9238795325112867385, 1.000000000000000000, 0.9238795325112867385, 1.000000000000000000, 0.9238795325112867385, 1.000000000000000000, 0.9238795325112867385, 1.000000000000000000, 0.9238795325112867385, 1.000000000000000000, 0.9238795325112867385, 1.000000000000000000, 0.9238795325112867385, 1.000000000000000000, 0.9238795325112867385, 1.000000000000000000, 0.9238795325112867385, 1.000000000000000000, 0.9238795325112867385, 1.000000000000000000, 0.9238795325112867385, 1.000000000000000000, 0.9238795325112867385, 1.000000000000000000, 0.9238795325112867385, 1.000000000000000000, 0.9238795325112867385, 1.000000000000000000, 0.9238795325112867385, 1.000000000000000000, 0.9238795325112867385, 1.000000000000000000, 0.9238795325112867385, 1.000000000000000000, 0.9238795325112867385, 1.000000000000000000, 0.9238795325112867385, 1.000000000000000000, 0.9238795325112867385, 1.000000000000000000, 0.9238795325112867385, 1.000000000000000000, 0.9238795325112867385, 1.000000000000000000, 0.9238795325112867385, 1.000000000000000000, 0.9238795325112867385, 1.000000000000000000, 0.9238795325112867385, 1.000000000000000000, 0.9238795325112867385, 1.000000000000000000, 0.9238795325112867385, 1.000000000000000000, 0.9238795325112867385, 1.000000000000000000, 0.9238795325112867385, 1.000000000000000000, 0.9238795325112867385, 1.000000000000000000, 0.9238795325112867385, 1.000000000000000000, 0.9238795325112867385, 1.000000000000000000, 0.9238795325112867385, 1.000000000000000000, 0.9238795325112867385, 1.000000000000000000, 0.9238795325112867385, 1.000000000000000000, 0.9238795325112867385, 1.000000000000000000, 0.9238795325112867385, 1.000000000000000000, 0.9238795325112867385, 1.000000000000000000, 0.9238795325112867385, 1.000000000000000000, 0.9238795325112867385, 1.000000000000000000, 0.9238795325112867385, 1.000000000000000000, 0.9238795325112867385, 1.000000000000000000, 0.9238795325112867385, 1.000000000000000000, 0.9238795325112867385, 1.000000000000000000, 0.9238795325112867385, 1.000000000000000000, 0.9238795325112867385, 1.000000000000000000, 0.9238795325112867385, 1.000000000000000000, 0.9238795325112867385, 1.000000000000000000, 0.9238795325112867385, 1.000000000000000000, 0.9238795325112867385, 1.000000000000000000, 0.9238795325112867385, 1.000000000000000000, 0.9238795325112867385, 1.000000000000000000, 0.9238795325112867385, 1.000000000000000000, 0.9238795325112867385, 1.000000000000000000, 0.9238795325112867385, 1.000000000000000000, 0.9238795325112867385, 1.000000000000000000, 0.9238795325112867385, 1.000000000000000000, 0.9238795325112867385, 1.000000000000000000, 0.9238795325112867385, 1.000000000000000000, 0.9238795325112867385, 1.000000000000000000, 0.9238795325112867385, 1.000000000000000000, 0.9238795325112867385, 1.000000000000000000, 0.9238795325112867385, 1.000000000000000000, 0.9238795325112867385, 1.000000000000000000, 0.9238795325112867385, 1.000000000000000000, 0.9238795325112867385, 1.000000000000000000, 0.9238795325112867385, 1.000000000000000000, 0.9238795325112867385, 1.000000000000000000, 0.9238795325112867385, 1.000000000000000000) ) ) 
 REPRESENTATION_ITEM ( '' )  SURFACE ( )  );
#8843=CARTESIAN_POINT ( 'NONE',  ( -3.385114897866767815E-17, -0.2764156081756484196, 0.2688888888888921747 ) ) ;
#8853=EDGE_CURVE ( 'NONE', #15906, #960, #23331, .T. ) ;
#8858=CARTESIAN_POINT ( 'NONE',  ( 0.3155070326520292290, -0.1306872919485616569, 0.2567361111111144956 ) ) ;
#8863=EDGE_CURVE ( 'NONE', #3289, #22427, #581, .T. ) ;
#8869=CARTESIAN_POINT ( 'NONE',  ( 0.2764156081756483641, 0.1144950937579610056, 0.2376388888888919526 ) ) ;
#8872=EDGE_LOOP ( 'NONE', ( #38, #4420, #12364, #15192 ) ) ;
#8876=CARTESIAN_POINT ( 'NONE',  ( 0.1294417382415924134, 0.3124999999999999445, 0.3209722222222258226 ) ) ;
#8889=EDGE_CURVE ( 'NONE', #11906, #12731, #22567, .T. ) ;
#8892=CARTESIAN_POINT ( 'NONE',  ( -0.2764156081756484196, 1.692557448933383907E-17, 0.3105555555555591929 ) ) ;
#8899=CARTESIAN_POINT ( 'NONE',  ( 0.4687500000000002220, 0.2150860547839004433, 0.05816278416816413055 ) ) ;
#8902=CARTESIAN_POINT ( 'NONE',  ( -0.1954553509668046918, -0.1954553509668046640, -0.01583333333333228690 ) ) ;
#8903=CARTESIAN_POINT ( 'NONE',  ( -3.385114897866767815E-17, -0.2764156081756484196, 0.05361111111111271227 ) ) ;
#8913=EDGE_LOOP ( 'NONE', ( #18714, #19832, #8137, #20681 ) ) ;
#8922=CARTESIAN_POINT ( 'NONE',  ( 0.2977072594216367274, -5.468793635004571549E-17, -0.08687392608830331320 ) ) ;
#8926=CARTESIAN_POINT ( 'NONE',  ( -0.4692113125120477846, 0.2611562006105974665, 0.04763592618481432561 ) ) ;
#8927=ORIENTED_EDGE ( 'NONE', *, *, #3638, .T. ) ;
#8931=DIRECTION ( 'NONE',  ( -1.000000000000000000, 0.000000000000000000, 0.000000000000000000 ) ) ;
#8967=CARTESIAN_POINT ( 'NONE',  ( 0.2764156081756483641, 0.1144950937579610056, 0.2862500000000035016 ) ) ;
#8970=B_SPLINE_CURVE_WITH_KNOTS ( 'NONE', 3,
 ( #16801, #8994, #3620, #3502, #22277, #14610 ),
 .UNSPECIFIED., .F., .F.,
 ( 4, 2, 4 ),
 ( 0.000000000000000000, 0.003274885914386082859, 0.006549771828772165717 ),
 .UNSPECIFIED. ) ;
#8971=CARTESIAN_POINT ( 'NONE',  ( -0.07990078027836888808, -0.4951351403630674386, 0.4110703004652378478 ) ) ;
#8984=CARTESIAN_POINT ( 'NONE',  ( 0.1306872919485616846, 0.3155070326520292290, 0.2706250000000035016 ) ) ;
#8986=( BOUNDED_CURVE ( )  B_SPLINE_CURVE ( 2, ( #10042, #17231, #13464, #7834, #17464, #2107, #513, #19291, #756 ),
 .UNSPECIFIED., .F., .F. ) 
 B_SPLINE_CURVE_WITH_KNOTS ( ( 3, 2, 2, 2, 3 ),
 ( 0.5208333333333334814, 0.5312500000000001110, 0.5416666666666667407, 0.5520833333333334814, 0.5625000000000001110 ),
 .UNSPECIFIED. ) 
 CURVE ( )  GEOMETRIC_REPRESENTATION_ITEM ( )  RATIONAL_B_SPLINE_CURVE ( ( 0.9999999999999992228, 0.9238795325112875156, 1.000000000000000000, 0.9238795325112867385, 1.000000000000000000, 0.9238795325112867385, 1.000000000000000000, 0.9238795325112859613, 1.000000000000000888 ) ) 
 REPRESENTATION_ITEM ( '' )  );
#8992=CARTESIAN_POINT ( 'NONE',  ( 0.1144950937579611444, 0.2764156081756483641, 0.3556944444444484210 ) ) ;
#8994=CARTESIAN_POINT ( 'NONE',  ( -0.4802530987341848134, -0.2139104309994724062, 0.05348414072159345806 ) ) ;
#9006=DIRECTION ( 'NONE',  ( -0.000000000000000000, -0.000000000000000000, -1.000000000000000000 ) ) ;
#9013=CARTESIAN_POINT ( 'NONE',  ( 0.1144950937579611444, 0.2764156081756483641, 0.3487500000000040012 ) ) ;
#9016=EDGE_CURVE ( 'NONE', #1241, #16785, #15464, .T. ) ;
#9021=CARTESIAN_POINT ( 'NONE',  ( 0.4805070082343983473, -0.2560807851245830435, 0.04413116910601663084 ) ) ;
#9024=CARTESIAN_POINT ( 'NONE',  ( -0.1954553509668046640, 0.1954553509668046918, 0.02583333333333472440 ) ) ;
#9025=CARTESIAN_POINT ( 'NONE',  ( -0.1954553509668046918, -0.1954553509668046640, -0.1199999999999998013 ) ) ;
#9026=ORIENTED_EDGE ( 'NONE', *, *, #17176, .F. ) ;
#9027=VERTEX_POINT ( 'NONE', #19001 ) ;
#9029=LINE ( 'NONE', #23882, #2969 ) ;
#9053=CARTESIAN_POINT ( 'NONE',  ( -0.2230971623002953874, 0.2230971623002954152, -0.1113194444444443598 ) ) ;
#9054=CARTESIAN_POINT ( 'NONE',  ( -0.4875000000000003220, -0.2598076211353319009, 0.06112444011295369711 ) ) ;
#9064=FACE_OUTER_BOUND ( 'NONE', #19278, .T. ) ;
#9068=ORIENTED_EDGE ( 'NONE', *, *, #17600, .T. ) ;
#9070=ADVANCED_FACE ( 'NONE', ( #7780 ), #1927, .T. ) ;
#9072=CARTESIAN_POINT ( 'NONE',  ( -0.2552321839961925742, -0.1601952157747160432, 0.4125377734234058624 ) ) ;
#9081=VERTEX_POINT ( 'NONE', #2052 ) ;
#9084=CARTESIAN_POINT ( 'NONE',  ( 0.1954553509668046640, -0.1954553509668047195, 0.3313888888888926743 ) ) ;
#9088=CARTESIAN_POINT ( 'NONE',  ( 0.2887653152721417760, -0.08545421435188853276, 0.4122949633718255291 ) ) ;
#9099=CARTESIAN_POINT ( 'NONE',  ( -0.1306872919485614903, 0.3155070326520293400, 0.1664583333333360671 ) ) ;
#9101=CARTESIAN_POINT ( 'NONE',  ( 0.08099032061186588194, -0.4945060939582642812, 0.4113389257669841648 ) ) ;
#9104=CARTESIAN_POINT ( 'NONE',  ( -3.385114897866767815E-17, -0.2764156081756484196, 0.2202777777777806811 ) ) ;
#9105=B_SPLINE_CURVE_WITH_KNOTS ( 'NONE', 3,
 ( #10390, #23275, #13922, #14152, #2580, #4876, #17812, #12223, #15747, #9901 ),
 .UNSPECIFIED., .F., .F.,
 ( 4, 2, 2, 2, 4 ),
 ( 1.355252715606880543E-19, 0.003321633220911224694, 0.006643266441822449388, 0.009964899662733674515, 0.01328653288364489878 ),
 .UNSPECIFIED. ) ;
#9115=B_SPLINE_CURVE_WITH_KNOTS ( 'NONE', 3,
 ( #8652, #10500, #4992, #19632, #6707, #17571 ),
 .UNSPECIFIED., .F., .F.,
 ( 4, 2, 4 ),
 ( 0.006549771828772165717, 0.009815671976345301253, 0.01308157212391843766 ),
 .UNSPECIFIED. ) ;
#9120=CARTESIAN_POINT ( 'NONE',  ( -0.01298396664829147909, 0.5473896884649155359, 0.04271845132552260643 ) ) ;
#9127=AXIS2_PLACEMENT_3D ( 'NONE', #15878, #23181, #23294 ) ;
#9130=CARTESIAN_POINT ( 'NONE',  ( -3.385114897866767815E-17, -0.2764156081756484196, 0.3244444444444482545 ) ) ;
#9137=CARTESIAN_POINT ( 'NONE',  ( 0.4687500000000003331, -0.2150879084408183761, 0.05816236869046900737 ) ) ;
#9141=CARTESIAN_POINT ( 'NONE',  ( -0.2764156081756484196, 0.1144950937579609918, -0.1304166666666665420 ) ) ;
#9143=ORIENTED_EDGE ( 'NONE', *, *, #19919, .T. ) ;
#9153=CARTESIAN_POINT ( 'NONE',  ( 0.3125000000000000000, -5.740531871003217465E-17, 0.3661111111111149397 ) ) ;
#9172=CIRCLE ( 'NONE', #22799, 0.01875000000000000625 ) ;
#9175=CARTESIAN_POINT ( 'NONE',  ( -0.3096898932023051110, -0.3624663341596540134, 0.07654795713852843853 ) ) ;
#9189=CARTESIAN_POINT ( 'NONE',  ( -0.4570242136016807177, 0.2774028246161669986, 0.04874733047933996893 ) ) ;
#9196=ORIENTED_EDGE ( 'NONE', *, *, #18763, .F. ) ;
#9198=CARTESIAN_POINT ( 'NONE',  ( -0.05458059743759432342, -0.3010824892324602819, 0.4171980187594044320 ) ) ;
#9204=CARTESIAN_POINT ( 'NONE',  ( -0.3124999999999993894, -0.1294417382415926909, 0.1820833333333360671 ) ) ;
#9212=ORIENTED_EDGE ( 'NONE', *, *, #6342, .F. ) ;
#9214=CARTESIAN_POINT ( 'NONE',  ( 0.1144950937579609085, -0.2764156081756484751, 0.3279166666666704089 ) ) ;
#9217=CARTESIAN_POINT ( 'NONE',  ( -0.4687500000000002776, 0.08745190237456286486, 0.08858760123954044496 ) ) ;
#9229=CARTESIAN_POINT ( 'NONE',  ( -0.1306872919485615459, -0.3155070326520293400, 0.2428472222222255728 ) ) ;
#9234=CARTESIAN_POINT ( 'NONE',  ( 0.1954553509668046640, -0.1954553509668047195, 0.2272222222222252119 ) ) ;
#9237=EDGE_LOOP ( 'NONE', ( #13429, #14363, #4168, #23596 ) ) ;
#9250=CARTESIAN_POINT ( 'NONE',  ( -0.006672437742759285313, -0.5374135436383427056, 0.05975564523638848130 ) ) ;
#9253=CARTESIAN_POINT ( 'NONE',  ( 0.2764156081756484196, -5.077672346800151106E-17, 0.2272222222222252119 ) ) ;
#9260=CARTESIAN_POINT ( 'NONE',  ( 0.3125000000000000000, -5.740531871003217465E-17, 0.1508333333333358728 ) ) ;
#9264=CARTESIAN_POINT ( 'NONE',  ( 0.2764156081756483641, -0.1144950937579611167, -0.1026388888888885437 ) ) ;
#9268=CARTESIAN_POINT ( 'NONE',  ( 0.4687500000000002776, -0.2178881689638759445, 0.3900517602158629638 ) ) ;
#9279=CARTESIAN_POINT ( 'NONE',  ( 0.2209708691207961651, 0.2209708691207959985, -0.008888888888887605186 ) ) ;
#9288=EDGE_LOOP ( 'NONE', ( #17733, #22023, #13389, #14532 ) ) ;
#9293=CARTESIAN_POINT ( 'NONE',  ( -0.1306872919485615459, -0.3155070326520293400, 0.01715277777777886661 ) ) ;
#9314=ADVANCED_FACE ( 'NONE', ( #16059 ), #23732, .T. ) ;
#9317=CARTESIAN_POINT ( 'NONE',  ( -0.2977072594216396695, 1.822931211668208286E-17, 0.4093739260883065278 ) ) ;
#9320=ORIENTED_EDGE ( 'NONE', *, *, #18851, .F. ) ;
#9332=CARTESIAN_POINT ( 'NONE',  ( 0.4687500000000002776, -0.2706329386826372141, 0.4425000000000000044 ) ) ;
#9333=CARTESIAN_POINT ( 'NONE',  ( -0.1144950937579609779, 0.2764156081756484196, 0.1890277777777805146 ) ) ;
#9337=CARTESIAN_POINT ( 'NONE',  ( -0.1366666852802201904, -0.4623613298295002894, 0.4215068951509234885 ) ) ;
#9344=( BOUNDED_CURVE ( )  B_SPLINE_CURVE ( 2, ( #13201, #22441, #11356, #16954, #18784, #11601, #9279, #19032, #7811 ),
 .UNSPECIFIED., .F., .F. ) 
 B_SPLINE_CURVE_WITH_KNOTS ( ( 3, 2, 2, 2, 3 ),
 ( 0.6562500000000001110, 0.6666666666666668517, 0.6770833333333334814, 0.6875000000000000000, 0.6979166666666667407 ),
 .UNSPECIFIED. ) 
 CURVE ( )  GEOMETRIC_REPRESENTATION_ITEM ( )  RATIONAL_B_SPLINE_CURVE ( ( 0.9999999999999992228, 0.9238795325112875156, 1.000000000000000000, 0.9238795325112867385, 1.000000000000000000, 0.9238795325112867385, 1.000000000000000000, 0.9238795325112867385, 1.000000000000000000 ) ) 
 REPRESENTATION_ITEM ( '' )  );
#9352=CARTESIAN_POINT ( 'NONE',  ( 0.04612934949352820446, -0.5146330850176437099, 0.3902021065396754085 ) ) ;
#9357=CARTESIAN_POINT ( 'NONE',  ( -0.2764156081756484196, -0.1144950937579609362, 0.2654166666666699093 ) ) ;
#9363=DIRECTION ( 'NONE',  ( -1.000000000000000000, 0.000000000000000000, 0.000000000000000000 ) ) ;
#9367=CONICAL_SURFACE ( 'NONE', #18708, 0.4453125000000000000, 1.047197551196600074 ) ;
#9373=ORIENTED_EDGE ( 'NONE', *, *, #21094, .F. ) ;
#9376=AXIS2_PLACEMENT_3D ( 'NONE', #9572, #22852, #7738 ) ;
#9377=CARTESIAN_POINT ( 'NONE',  ( 0.1954553509668047195, 0.1954553509668046085, 0.2897222222222257115 ) ) ;
#9381=CARTESIAN_POINT ( 'NONE',  ( 0.4739766090219372785, 0.2774257203002796213, 0.04193793378272820532 ) ) ;
#9382=EDGE_CURVE ( 'NONE', #18897, #8797, #10966, .T. ) ;
#9389=CARTESIAN_POINT ( 'NONE',  ( 0.000000000000000000, 0.2764156081756484196, 0.02583333333333468970 ) ) ;
#9391=CARTESIAN_POINT ( 'NONE',  ( 0.4687500000000002776, -0.08748112355138647211, 0.4143798302908627273 ) ) ;
#9398=ORIENTED_EDGE ( 'NONE', *, *, #23780, .F. ) ;
#9412=EDGE_LOOP ( 'NONE', ( #3110, #8076, #20645, #15644 ) ) ;
#9417=CARTESIAN_POINT ( 'NONE',  ( 0.1306872919485616846, 0.3155070326520292290, 0.04493055555555688918 ) ) ;
#9418=CARTESIAN_POINT ( 'NONE',  ( -0.2209708691207961373, -0.2209708691207961095, 0.01888888888889038095 ) ) ;
#9429=ADVANCED_FACE ( 'NONE', ( #23233 ), #6542, .F. ) ;
#9431=CARTESIAN_POINT ( 'NONE',  ( -0.3854970698558352060, 0.3186990403121960358, 0.4003306813560890132 ) ) ;
#9434=EDGE_LOOP ( 'NONE', ( #20916, #6631, #2576, #20601, #5508, #14178, #19603, #11664, #13002, #887, #12809, #15041, #19231, #16530, #22076, #7984, #23428, #12034, #22066, #17277, #9568, #24086, #14019, #11839, #19303, #7878 ) ) ;
#9435=EDGE_LOOP ( 'NONE', ( #22192, #3142, #21781, #16637, #8370, #9706, #18612 ) ) ;
#9437=CARTESIAN_POINT ( 'NONE',  ( -0.2144047338280713200, -0.2134821532158913959, 0.4137619532499328678 ) ) ;
#9438=( BOUNDED_SURFACE ( )  B_SPLINE_SURFACE ( 3, 2, ( 
 ( #20896, #19184, #7964 ),
 ( #20776, #8203, #11397 ),
 ( #653, #290, #15416 ),
 ( #10055, #19308, #6380 ),
 ( #5897, #6013, #23071 ),
 ( #15176, #6133, #2493 ),
 ( #2376, #22844, #8081 ),
 ( #15532, #13600, #22955 ),
 ( #9564, #4191, #18829 ),
 ( #6257, #21013, #2611 ),
 ( #9686, #13481, #2252 ),
 ( #17479, #13717, #7730 ) ),
 .UNSPECIFIED., .F., .F., .T. ) 
 B_SPLINE_SURFACE_WITH_KNOTS ( ( 4, 2, 2, 2, 2, 4 ),
 ( 3, 3 ),
 ( 0.03744456216066675835, 0.04077857935059428507, 0.04244558794555804149, 0.04411259654052180484, 0.04744661373044932462, 0.05078063092037685133 ),
 ( 0.000000000000000000, 1.000000000000000000 ),
 .UNSPECIFIED. ) 
 GEOMETRIC_REPRESENTATION_ITEM ( )  RATIONAL_B_SPLINE_SURFACE ( (
 ( 1.000000000000000000, 0.8464669816041904271, 1.000000000000000000),
 ( 1.000000000000000000, 0.8515868425024901711, 1.000000000000000000),
 ( 1.000000000000000000, 0.8564835659287574066, 1.000000000000000000),
 ( 1.000000000000000000, 0.8619139284920220856, 1.000000000000000000),
 ( 1.000000000000000000, 0.8633991495534084626, 1.000000000000000000),
 ( 1.000000000000000000, 0.8654490525001213852, 1.000000000000000000),
 ( 1.000000000000000000, 0.8660089163969105774, 1.000000000000000000),
 ( 1.000000000000000000, 0.8660572738274425753, 1.000000000000000000),
 ( 1.000000000000000000, 0.8638780250325636123, 1.000000000000000000),
 ( 1.000000000000000000, 0.8566598902920686820, 1.000000000000000000),
 ( 1.000000000000000000, 0.8517009389554212051, 1.000000000000000000),
 ( 1.000000000000000000, 0.8464669816041904271, 1.000000000000000000) ) ) 
 REPRESENTATION_ITEM ( '' )  SURFACE ( )  );
#9444=DIRECTION ( 'NONE',  ( 0.000000000000000000, 0.000000000000000000, -1.000000000000000000 ) ) ;
#9450=EDGE_LOOP ( 'NONE', ( #2998, #13811, #6724, #7399, #14255 ) ) ;
#9455=CARTESIAN_POINT ( 'NONE',  ( -0.4687500000000004441, -0.2922835737772483400, 0.06112444011295366242 ) ) ;
#9460=AXIS2_PLACEMENT_3D ( 'NONE', #6656, #16294, #4591 ) ;
#9464=EDGE_CURVE ( 'NONE', #11636, #5331, #21588, .T. ) ;
#9468=CARTESIAN_POINT ( 'NONE',  ( -0.3155070326520293400, 0.1306872919485614903, 0.3956250000000045564 ) ) ;
#9475=CARTESIAN_POINT ( 'NONE',  ( -0.2764156081756484196, -0.1144950937579609362, -0.01930555555555453148 ) ) ;
#9477=CARTESIAN_POINT ( 'NONE',  ( -0.2764156081756484196, 0.1144950937579609918, 0.4251388888888933959 ) ) ;
#9479=CARTESIAN_POINT ( 'NONE',  ( -0.009375000000009145115, -0.5358532185916164980, 0.06112444011295854046 ) ) ;
#9488=CARTESIAN_POINT ( 'NONE',  ( 0.3125000000000000000, 3.738758431839877614E-19, 0.4241666666666665253 ) ) ;
#9494=EDGE_CURVE ( 'NONE', #17972, #8797, #16365, .T. ) ;
#9497=CARTESIAN_POINT ( 'NONE',  ( -0.2764156081756484196, 0.1144950937579609918, 0.3626388888888929518 ) ) ;
#9504=CARTESIAN_POINT ( 'NONE',  ( 0.4675994362856802367, -0.2849176297964606253, 0.04270874187135767497 ) ) ;
#9505=CARTESIAN_POINT ( 'NONE',  ( 0.4593750000000003664, 0.2760455974562901482, 0.3779506566538943235 ) ) ;
#9506=CARTESIAN_POINT ( 'NONE',  ( -0.1144950937579609918, -0.2764156081756484196, 0.1056944444444464504 ) ) ;
#9515=EDGE_LOOP ( 'NONE', ( #15312, #9709, #16398, #17376, #21886 ) ) ;
#9523=DIRECTION ( 'NONE',  ( -0.4999999999999978906, -0.8660254037844398178, 0.000000000000000000 ) ) ;
#9525=ADVANCED_FACE ( 'NONE', ( #20077 ), #19958, .F. ) ;
#9534=CARTESIAN_POINT ( 'NONE',  ( -3.827021247335479543E-17, -0.3125000000000000000, 0.1855555555555580272 ) ) ;
#9536=CARTESIAN_POINT ( 'NONE',  ( 0.1306872919485614071, -0.3155070326520293955, 0.02409722222222336965 ) ) ;
#9537=CARTESIAN_POINT ( 'NONE',  ( -0.1591012008044459802, -0.4494087562524027857, 0.07655254331177707705 ) ) ;
#9538=CYLINDRICAL_SURFACE ( 'NONE', #21801, 0.01874999999999999931 ) ;
#9553=CARTESIAN_POINT ( 'NONE',  ( -0.1419551320363411084, -0.2751926619867112178, -0.09836143147318530955 ) ) ;
#9564=CARTESIAN_POINT ( 'NONE',  ( 0.3068695747082215153, 0.3531079105191415324, 0.4306248051561324952 ) ) ;
#9565=SPHERICAL_SURFACE ( 'NONE', #13644, 0.01874999999999999931 ) ;
#9568=ORIENTED_EDGE ( 'NONE', *, *, #14593, .T. ) ;
#9572=CARTESIAN_POINT ( 'NONE',  ( 0.000000000000000000, 0.000000000000000000, -0.1199999999999999956 ) ) ;
#9579=CONICAL_SURFACE ( 'NONE', #14233, 0.3125000000000000000, 0.7853981633974497223 ) ;
#9590=CYLINDRICAL_SURFACE ( 'NONE', #23920, 0.3125000000000000000 ) ;
#9595=CARTESIAN_POINT ( 'NONE',  ( 0.4254231800974607736, -0.3089306822179591072, 0.05347271648849192399 ) ) ;
#9597=CARTESIAN_POINT ( 'NONE',  ( 0.2764156081756484196, -5.077672346800151106E-17, 0.3383333333333372051 ) ) ;
#9599=CARTESIAN_POINT ( 'NONE',  ( -0.2764156081756484196, 0.1144950937579609918, 0.3695833333333374271 ) ) ;
#9601=CARTESIAN_POINT ( 'NONE',  ( 0.009375000000000032613, -0.5358532185916218271, 0.06112444011295373875 ) ) ;
#9604=CARTESIAN_POINT ( 'NONE',  ( -0.2716011131362577880, 0.07493431514972544172, -0.07075596294687129528 ) ) ;
#9617=CARTESIAN_POINT ( 'NONE',  ( -0.1584465904743051490, -0.4497866957027560897, 0.4135550951626319471 ) ) ;
#9618=CARTESIAN_POINT ( 'NONE',  ( -3.863846776457871776E-17, -0.3155070326520292845, -0.1425694444444441933 ) ) ;
#9622=VERTEX_POINT ( 'NONE', #6910 ) ;
#9625=CARTESIAN_POINT ( 'NONE',  ( -0.1954553509668046918, -0.1954553509668046640, -0.1199999999999998013 ) ) ;
#9628=CARTESIAN_POINT ( 'NONE',  ( 0.1144950937579609085, -0.2764156081756484751, 0.2793055555555589153 ) ) ;
#9638=CARTESIAN_POINT ( 'NONE',  ( 0.000000000000000000, 0.000000000000000000, 1.326383476483184332 ) ) ;
#9647=CARTESIAN_POINT ( 'NONE',  ( -0.2764156081756484196, -0.1144950937579609362, -0.1304166666666665420 ) ) ;
#9658=CARTESIAN_POINT ( 'NONE',  ( 0.3155070326520292290, -0.1306872919485616569, 0.08659722222222389354 ) ) ;
#9669=LINE ( 'NONE', #18689, #884 ) ;
#9675=CARTESIAN_POINT ( 'NONE',  ( 0.1764095973160011710, -0.2469329051807456488, -0.09217807008012661452 ) ) ;
#9679=CARTESIAN_POINT ( 'NONE',  ( 0.1695524133009104484, 0.2302630372892223998, 0.3969863378735464798 ) ) ;
#9686=CARTESIAN_POINT ( 'NONE',  ( 0.4208772603875943763, 0.2863811090245901303, 0.4064915563616229299 ) ) ;
#9693=CARTESIAN_POINT ( 'NONE',  ( -0.4500000000000003997, 0.2598076211353315124, 0.4425000000000000044 ) ) ;
#9696=CARTESIAN_POINT ( 'NONE',  ( -0.1893589898698174179, -0.4210708385985257873, 0.4333520680959401239 ) ) ;
#9697=CARTESIAN_POINT ( 'NONE',  ( 0.1963547988595201466, -0.4279003813870558282, 0.09139143879391149750 ) ) ;
#9702=VERTEX_POINT ( 'NONE', #20557 ) ;
#9706=ORIENTED_EDGE ( 'NONE', *, *, #1423, .T. ) ;
#9707=ORIENTED_EDGE ( 'NONE', *, *, #11413, .F. ) ;
#9709=ORIENTED_EDGE ( 'NONE', *, *, #15835, .T. ) ;
#9711=CARTESIAN_POINT ( 'NONE',  ( 0.2230971623002953874, -0.2230971623002954429, 0.4199305555555602476 ) ) ;
#9718=CARTESIAN_POINT ( 'NONE',  ( 0.1144950937579611444, 0.2764156081756483641, 0.1820833333333359838 ) ) ;
#9720=CARTESIAN_POINT ( 'NONE',  ( -0.2764156081756484196, 1.692557448933383907E-17, -0.07833333333333278303 ) ) ;
#9725=CARTESIAN_POINT ( 'NONE',  ( -0.1841151976024358594, 0.2183016720772819608, -0.07412050734230554716 ) ) ;
#9734=ORIENTED_EDGE ( 'NONE', *, *, #3221, .F. ) ;
#9739=ORIENTED_EDGE ( 'NONE', *, *, #18604, .F. ) ;
#9742=CARTESIAN_POINT ( 'NONE',  ( 0.2764156081756484196, -5.077672346800151106E-17, 0.3938888888888931739 ) ) ;
#9750=CARTESIAN_POINT ( 'NONE',  ( 0.1144950937579611444, 0.2764156081756483641, 0.07791666666666842433 ) ) ;
#9758=DIRECTION ( 'NONE',  ( 0.8660254037844397068, 0.000000000000000000, -0.4999999999999979461 ) ) ;
#9759=LINE ( 'NONE', #17197, #8698 ) ;
#9766=AXIS2_PLACEMENT_3D ( 'NONE', #10588, #18015, #19839 ) ;
#9772=CARTESIAN_POINT ( 'NONE',  ( -0.3062750282812776725, 0.05890668782146677579, -0.09963899732724015856 ) ) ;
#9776=( BOUNDED_CURVE ( )  B_SPLINE_CURVE ( 2, ( #21415, #17638, #18004 ),
 .UNSPECIFIED., .F., .T. ) 
 B_SPLINE_CURVE_WITH_KNOTS ( ( 3, 3 ),
 ( 0.8229166666666667407, 0.8267181212766938625 ),
 .UNSPECIFIED. ) 
 CURVE ( )  GEOMETRIC_REPRESENTATION_ITEM ( )  RATIONAL_B_SPLINE_CURVE ( ( 1.000000000000000000, 0.9722206238029704739, 0.9647168388458531307 ) ) 
 REPRESENTATION_ITEM ( '' )  );
#9777=CARTESIAN_POINT ( 'NONE',  ( 0.2764156081756483641, 0.1144950937579610195, 0.07097222222222394905 ) ) ;
#9782=DIRECTION ( 'NONE',  ( 0.000000000000000000, 0.000000000000000000, -1.000000000000000000 ) ) ;
#9785=CARTESIAN_POINT ( 'NONE',  ( -0.3155070326520293400, -0.1306872919485614626, 0.1768750000000023637 ) ) ;
#9789=B_SPLINE_CURVE_WITH_KNOTS ( 'NONE', 3,
 ( #19130, #718, #2200, #21201, #6322, #20962, #10001, #2315 ),
 .UNSPECIFIED., .F., .F.,
 ( 4, 2, 2, 4 ),
 ( 0.000000000000000000, 0.0004997454757086382867, 0.0007496182135629574301, 0.0009994909514172765734 ),
 .UNSPECIFIED. ) ;
#9797=CARTESIAN_POINT ( 'NONE',  ( -0.2209708691207961373, -0.2209708691207961095, 0.2966666666666704089 ) ) ;
#9799=CARTESIAN_POINT ( 'NONE',  ( -0.04625313968440265822, 0.5145616147176192978, 0.07046346805509136335 ) ) ;
#9802=CARTESIAN_POINT ( 'NONE',  ( 0.2709282478163133612, -0.1304588658952313962, -0.08939837573807506155 ) ) ;
#9821=CARTESIAN_POINT ( 'NONE',  ( -0.3852690508743131792, -0.3188306871325582437, 0.4003899297375634325 ) ) ;
#9822=CARTESIAN_POINT ( 'NONE',  ( 0.000000000000000000, 0.000000000000000000, 0.4425000000000000044 ) ) ;
#9823=APPLICATION_CONTEXT ( 'configuration controlled 3d designs of mechanical parts and assemblies' ) ;
#9826=ORIENTED_EDGE ( 'NONE', *, *, #15304, .F. ) ;
#9832=VERTEX_POINT ( 'NONE', #6991 ) ;
#9840=CARTESIAN_POINT ( 'NONE',  ( 0.3125000000000004996, 0.1294417382415917750, 0.2654166666666701313 ) ) ;
#9841=CARTESIAN_POINT ( 'NONE',  ( 0.3838096539023117537, -0.3196732703672033327, 0.06591861138176849377 ) ) ;
#9843=CARTESIAN_POINT ( 'NONE',  ( -0.1144950937579609779, 0.2764156081756484196, 0.1334722222222244348 ) ) ;
#9845=CARTESIAN_POINT ( 'NONE',  ( 0.1954553509668047195, 0.1954553509668046085, 0.4077777777777821799 ) ) ;
#9864=CARTESIAN_POINT ( 'NONE',  ( 0.4678838860311516079, -0.2663291305467024861, 0.05893128447555356919 ) ) ;
#9865=CARTESIAN_POINT ( 'NONE',  ( -0.1144950937579609918, -0.2764156081756484196, 0.3765277777777820134 ) ) ;
#9874=CARTESIAN_POINT ( 'NONE',  ( 0.1144950937579611444, 0.2764156081756483641, 0.2445833333333364279 ) ) ;
#9884=CARTESIAN_POINT ( 'NONE',  ( -0.4208308994021711102, 0.2864083541825031554, 0.4065068718547070747 ) ) ;
#9886=ORIENTED_EDGE ( 'NONE', *, *, #3485, .T. ) ;
#9898=CARTESIAN_POINT ( 'NONE',  ( 0.3125000000000000000, -5.740531871003217465E-17, 0.3730555555555599145 ) ) ;
#9901=CARTESIAN_POINT ( 'NONE',  ( -0.4593750000000004219, 0.2760455974562897596, 0.06112444011295372487 ) ) ;
#9903=CARTESIAN_POINT ( 'NONE',  ( -0.3155070326520292845, 1.931923388228935888E-17, 0.1178472222222241295 ) ) ;
#9919=ORIENTED_EDGE ( 'NONE', *, *, #4050, .F. ) ;
#9924=ADVANCED_FACE ( 'NONE', ( #18681 ), #23351, .T. ) ;
#9929=EDGE_CURVE ( 'NONE', #13004, #8463, #17043, .T. ) ;
#9933=VECTOR ( 'NONE', #2083, 39.37007874015748143 ) ;
#9943=DIRECTION ( 'NONE',  ( 0.5000000000000012212, -0.8660254037844380415, 0.000000000000000000 ) ) ;
#9946=ORIENTED_EDGE ( 'NONE', *, *, #19742, .F. ) ;
#9955=CYLINDRICAL_SURFACE ( 'NONE', #19652, 0.3125000000000000000 ) ;
#9960=CARTESIAN_POINT ( 'NONE',  ( -0.3124999999999993894, 0.1294417382415927742, 0.2862500000000035572 ) ) ;
#9962=CARTESIAN_POINT ( 'NONE',  ( -0.2764156081756484196, -0.1144950937579609362, 0.3140277777777815138 ) ) ;
#9964=CARTESIAN_POINT ( 'NONE',  ( 0.2764156081756484196, -5.077672346800151106E-17, 0.4008333333333376491 ) ) ;
#9973=CARTESIAN_POINT ( 'NONE',  ( -3.827021247335479543E-17, -0.3125000000000000000, 0.3522222222222260446 ) ) ;
#9975=CARTESIAN_POINT ( 'NONE',  ( -0.4687500000000003886, 0.2598076211353315124, 0.06112444011295379426 ) ) ;
#9982=CARTESIAN_POINT ( 'NONE',  ( 0.009374999999999774139, 0.5358532185916217161, 0.06112444011295372487 ) ) ;
#9984=CARTESIAN_POINT ( 'NONE',  ( 0.2209708691207961095, -0.2209708691207961651, 0.08833333333333540094 ) ) ;
#9989=CARTESIAN_POINT ( 'NONE',  ( -0.1144950937579609779, 0.2764156081756484196, 0.4668055555555604141 ) ) ;
#9996=CARTESIAN_POINT ( 'NONE',  ( 0.006672437742759138729, 0.5374135436383427056, 0.05975564523638855763 ) ) ;
#9997=CARTESIAN_POINT ( 'NONE',  ( -0.2764156081756484196, -0.1144950937579609362, 0.1543055555555579716 ) ) ;
#9999=ADVANCED_FACE ( 'NONE', ( #267 ), #18931, .F. ) ;
#10001=CARTESIAN_POINT ( 'NONE',  ( -0.01571427698143878018, 0.5457913482617613443, 0.04342012612512791830 ) ) ;
#10007=CARTESIAN_POINT ( 'NONE',  ( -0.4687500000000003886, 0.2706329386826371031, 0.4425000000000000044 ) ) ;
#10008=CARTESIAN_POINT ( 'NONE',  ( -0.1580560128843782330, 0.4500121957794397942, 0.4142946745564982658 ) ) ;
#10013=CARTESIAN_POINT ( 'NONE',  ( 0.09136153228682411531, 0.5015293579687603032, 0.06108838700204547584 ) ) ;
#10016=CARTESIAN_POINT ( 'NONE',  ( -0.4687500000000003886, 0.08695190463377312773, 0.07654938221781626417 ) ) ;
#10017=LINE ( 'NONE', #8164, #9933 ) ;
#10018=AXIS2_PLACEMENT_3D ( 'NONE', #12610, #1496, #8931 ) ;
#10022=ADVANCED_FACE ( 'NONE', ( #19161 ), #9538, .T. ) ;
#10024=CARTESIAN_POINT ( 'NONE',  ( -0.1144950937579609779, 0.2764156081756484196, 0.02930555555555695163 ) ) ;
#10030=CARTESIAN_POINT ( 'NONE',  ( -0.2230971623002953874, 0.2230971623002954152, 0.2220138888888916195 ) ) ;
#10042=CARTESIAN_POINT ( 'NONE',  ( -0.3125000000000000000, 1.913510623667739771E-17, 0.2272222222222250176 ) ) ;
#10049=CARTESIAN_POINT ( 'NONE',  ( 0.2716011131362610631, 0.07493431514972453966, 0.3932559629468742601 ) ) ;
#10053=VECTOR ( 'NONE', #5492, 39.37007874015748143 ) ;
#10055=CARTESIAN_POINT ( 'NONE',  ( 0.1312453311287957169, 0.4543582620183878595, 0.4268234664230710629 ) ) ;
#10074=VERTEX_POINT ( 'NONE', #21587 ) ;
#10077=EDGE_CURVE ( 'NONE', #17585, #7205, #24077, .T. ) ;
#10079=DIRECTION ( 'NONE',  ( -1.000000000000000000, 0.000000000000000000, 0.000000000000000000 ) ) ;
#10083=CARTESIAN_POINT ( 'NONE',  ( -0.4687500000000003331, 0.1777514598960921177, 0.4112133685574570485 ) ) ;
#10084=CARTESIAN_POINT ( 'NONE',  ( -0.2209708691207961095, 0.2209708691207961373, 0.2827777777777814028 ) ) ;
#10087=CARTESIAN_POINT ( 'NONE',  ( -0.1144950937579609779, 0.2764156081756484196, 0.2445833333333364834 ) ) ;
#10089=CARTESIAN_POINT ( 'NONE',  ( -0.2764156081756484196, -0.1144950937579609362, 0.1473611111111134686 ) ) ;
#10096=DIRECTION ( 'NONE',  ( 0.000000000000000000, 0.000000000000000000, -1.000000000000000000 ) ) ;
#10103=CARTESIAN_POINT ( 'NONE',  ( 0.000000000000000000, 0.000000000000000000, 1.326383476483184332 ) ) ;
#10106=DIRECTION ( 'NONE',  ( -2.489328460184014472E-15, -0.9607689228305229534, 0.2773500981126141296 ) ) ;
#10110=CARTESIAN_POINT ( 'NONE',  ( -0.2230971623002954152, -0.2230971623002953874, 0.1282638888888912865 ) ) ;
#10111=CARTESIAN_POINT ( 'NONE',  ( -0.3101174172661915196, -0.3622195030262472804, 0.08858683671056802322 ) ) ;
#10114=CARTESIAN_POINT ( 'NONE',  ( 0.2764156081756483641, -0.1144950937579611167, -0.1026388888888885437 ) ) ;
#10117=CARTESIAN_POINT ( 'NONE',  ( 0.1144950937579609085, -0.2764156081756484751, 0.3904166666666708529 ) ) ;
#10124=AXIS2_PLACEMENT_3D ( 'NONE', #21453, #23262, #19617 ) ;
#10133=CARTESIAN_POINT ( 'NONE',  ( 0.1653103785569666750, -0.4584405057248004955, 0.07159583130656670125 ) ) ;
#10137=FACE_OUTER_BOUND ( 'NONE', #10565, .T. ) ;
#10139=CARTESIAN_POINT ( 'NONE',  ( -0.1954553509668046918, -0.1954553509668046640, 0.03972222222222369925 ) ) ;
#10142=FACE_OUTER_BOUND ( 'NONE', #23662, .T. ) ;
#10144=CARTESIAN_POINT ( 'NONE',  ( 0.2764156081756483641, 0.1144950937579610195, 0.1265277777777799595 ) ) ;
#10150=CARTESIAN_POINT ( 'NONE',  ( -3.863846776457871776E-17, -0.3155070326520292845, 0.4650694444444490872 ) ) ;
#10151=CARTESIAN_POINT ( 'NONE',  ( -0.1294417382415922191, 0.3125000000000000000, 0.05013888888889027340 ) ) ;
#10158=CARTESIAN_POINT ( 'NONE',  ( 0.3850708708653794998, -0.3189451064140639280, 0.07813342133392808808 ) ) ;
#10161=AXIS2_PLACEMENT_3D ( 'NONE', #4993, #5358, #12457 ) ;
#10173=VERTEX_POINT ( 'NONE', #13926 ) ;
#10191=VERTEX_POINT ( 'NONE', #21113 ) ;
#10202=CARTESIAN_POINT ( 'NONE',  ( -0.4581189881604794678, 0.2644951211353315235, 0.3941886329748526263 ) ) ;
#10207=CARTESIAN_POINT ( 'NONE',  ( 0.1144950937579609085, -0.2764156081756484751, 0.1612500000000025024 ) ) ;
#10210=CARTESIAN_POINT ( 'NONE',  ( 0.2951834061891078775, 0.03795937687255809129, -0.08618158780276162501 ) ) ;
#10211=DIRECTION ( 'NONE',  ( 0.000000000000000000, -0.9607689228305228424, -0.2773500981126148512 ) ) ;
#10219=CARTESIAN_POINT ( 'NONE',  ( 0.1586475693114279273, 0.4496706605170417981, 0.08858850926231193190 ) ) ;
#10220=ORIENTED_EDGE ( 'NONE', *, *, #21071, .F. ) ;
#10221=CARTESIAN_POINT ( 'NONE',  ( -0.1294417382415922746, -0.3125000000000000000, 0.07791666666666866026 ) ) ;
#10223=CARTESIAN_POINT ( 'NONE',  ( -0.1306872919485615459, -0.3155070326520293400, -0.03493055555555446556 ) ) ;
#10225=DIRECTION ( 'NONE',  ( -1.000000000000000000, 0.000000000000000000, 0.000000000000000000 ) ) ;
#10229=CARTESIAN_POINT ( 'NONE',  ( -0.2764156081756484196, 0.1144950937579609918, -0.07486111111111054539 ) ) ;
#10231=CARTESIAN_POINT ( 'NONE',  ( 0.4687500000000002776, 0.2706329386826373806, 0.4425000000000000044 ) ) ;
#10232=CARTESIAN_POINT ( 'NONE',  ( 0.1954553509668047195, 0.1954553509668046085, 0.4077777777777821799 ) ) ;
#10247=CARTESIAN_POINT ( 'NONE',  ( 0.1294417382415921358, -0.3125000000000002220, -0.02624999999999886105 ) ) ;
#10250=FACE_OUTER_BOUND ( 'NONE', #16209, .T. ) ;
#10253=CARTESIAN_POINT ( 'NONE',  ( -0.4802534441549711763, -0.2139678024937353706, 0.05347141629229230919 ) ) ;
#10254=CARTESIAN_POINT ( 'NONE',  ( -0.1144950937579609779, 0.2764156081756484196, -0.08874999999999953759 ) ) ;
#10259=CARTESIAN_POINT ( 'NONE',  ( 0.1144950937579611444, 0.2764156081756483641, 0.1890277777777804313 ) ) ;
#10262=CARTESIAN_POINT ( 'NONE',  ( 0.4687500000000002776, -0.04414274412020515598, 0.09139217954989621584 ) ) ;
#10266=CARTESIAN_POINT ( 'NONE',  ( 0.3155070326520292290, -0.1306872919485616569, 0.3643750000000038902 ) ) ;
#10269=CARTESIAN_POINT ( 'NONE',  ( 0.4593750000000003664, 0.2760455974562901482, 0.06112444011295366936 ) ) ;
#10271=CARTESIAN_POINT ( 'NONE',  ( -0.3125000000000000000, 1.913510623667739771E-17, 0.005000000000001014917 ) ) ;
#10275=ADVANCED_FACE ( 'NONE', ( #22359 ), #3112, .F. ) ;
#10276=EDGE_LOOP ( 'NONE', ( #17889, #6665, #11698, #9734 ) ) ;
#10278=ADVANCED_FACE ( 'NONE', ( #654 ), #9565, .T. ) ;
#10281=ORIENTED_EDGE ( 'NONE', *, *, #8677, .F. ) ;
#10289=ORIENTED_EDGE ( 'NONE', *, *, #14848, .F. ) ;
#10296=CYLINDRICAL_SURFACE ( 'NONE', #16223, 0.3125000000000000000 ) ;
#10311=EDGE_CURVE ( 'NONE', #11169, #15529, #10937, .T. ) ;
#10317=DIRECTION ( 'NONE',  ( 0.000000000000000000, 0.000000000000000000, -1.000000000000000000 ) ) ;
#10323=CARTESIAN_POINT ( 'NONE',  ( -0.4687500000000003886, -0.1778076022956336377, 0.4111980179219333342 ) ) ;
#10327=CARTESIAN_POINT ( 'NONE',  ( 0.2764156081756484196, -5.077672346800151106E-17, 0.06055555555555720143 ) ) ;
#10330=CARTESIAN_POINT ( 'NONE',  ( -0.08610082984204266154, 0.2741627315343084792, -0.07637567569807812706 ) ) ;
#10336=AXIS2_PLACEMENT_3D ( 'NONE', #21929, #5224, #12695 ) ;
#10338=CARTESIAN_POINT ( 'NONE',  ( 0.2723952011404801032, 0.3839984346608560917, 0.09139143879391152525 ) ) ;
#10343=CARTESIAN_POINT ( 'NONE',  ( 0.4687500000000003886, -0.2570931668155774785, 0.04874733047934001057 ) ) ;
#10344=CARTESIAN_POINT ( 'NONE',  ( -0.3155070326520293400, -0.1306872919485614626, -0.04187499999999895473 ) ) ;
#10345=DIRECTION ( 'NONE',  ( 1.000000000000000000, 0.000000000000000000, 0.000000000000000000 ) ) ;
#10346=CIRCLE ( 'NONE', #16574, 0.01875000000000000278 ) ;
#10352=CARTESIAN_POINT ( 'NONE',  ( -0.1144950937579609918, -0.2764156081756484196, -0.005416666666665557496 ) ) ;
#10354=CARTESIAN_POINT ( 'NONE',  ( -0.3050515993604162590, -0.01759458571372108510, -0.09459994310003677631 ) ) ;
#10355=CARTESIAN_POINT ( 'NONE',  ( 0.1954553509668047195, 0.1954553509668046085, 0.4633333333333381487 ) ) ;
#10369=CARTESIAN_POINT ( 'NONE',  ( 0.009374999999999774139, 0.5358532185916217161, 0.06112444011295372487 ) ) ;
#10371=DIRECTION ( 'NONE',  ( 0.000000000000000000, 0.000000000000000000, -1.000000000000000000 ) ) ;
#10372=ADVANCED_FACE ( 'NONE', ( #6381 ), #2373, .T. ) ;
#10377=CARTESIAN_POINT ( 'NONE',  ( 0.3077469291169038779, 0.3525961953783998681, 0.4304954382810343705 ) ) ;
#10379=CARTESIAN_POINT ( 'NONE',  ( 0.1954553509668047195, 0.1954553509668046085, 0.01194444444444571485 ) ) ;
#10385=CARTESIAN_POINT ( 'NONE',  ( 0.2764156081756483641, -0.1144950937579611028, 0.2306944444444474218 ) ) ;
#10388=CARTESIAN_POINT ( 'NONE',  ( 0.4796774003163876143, -0.08638957141560613118, 0.07156364629625895646 ) ) ;
#10389=CARTESIAN_POINT ( 'NONE',  ( 0.4802530965259536599, 0.2139100642471496172, 0.05348422206366747894 ) ) ;
#10390=CARTESIAN_POINT ( 'NONE',  ( -0.009375000000000190473, 0.5358532185916217161, 0.06112444011295373181 ) ) ;
#10392=CARTESIAN_POINT ( 'NONE',  ( -0.3155070326520293400, 0.1306872919485614903, 0.3921527777777817914 ) ) ;
#10395=CARTESIAN_POINT ( 'NONE',  ( 0.3125000000000000000, -5.740531871003217465E-17, 0.3661111111111149397 ) ) ;
#10400=ORIENTED_EDGE ( 'NONE', *, *, #12276, .F. ) ;
#10408=CARTESIAN_POINT ( 'NONE',  ( 0.2195630361086305937, -0.1679215936616662852, 0.3880822748423153334 ) ) ;
#10420=LINE ( 'NONE', #14067, #23598 ) ;
#10427=DIRECTION ( 'NONE',  ( 0.000000000000000000, 0.000000000000000000, -1.000000000000000000 ) ) ;
#10430=CARTESIAN_POINT ( 'NONE',  ( 0.000000000000000000, 0.000000000000000000, -0.1012499999999999928 ) ) ;
#10439=CIRCLE ( 'NONE', #1856, 0.01874999999999998890 ) ;
#10442=DIRECTION ( 'NONE',  ( 0.000000000000000000, -1.000000000000000000, 0.000000000000000000 ) ) ;
#10448=VERTEX_POINT ( 'NONE', #23668 ) ;
#10449=CARTESIAN_POINT ( 'NONE',  ( -0.1144950937579609918, -0.2764156081756484196, 0.3765277777777819579 ) ) ;
#10451=CARTESIAN_POINT ( 'NONE',  ( 0.000000000000000000, 0.2764156081756484196, 0.1300000000000022249 ) ) ;
#10453=CARTESIAN_POINT ( 'NONE',  ( -0.06796888784162306851, 0.2795977689546957357, -0.07675168144635624579 ) ) ;
#10455=CARTESIAN_POINT ( 'NONE',  ( -3.827021247335479543E-17, -0.3125000000000000000, -0.03666666666666597990 ) ) ;
#10458=AXIS2_PLACEMENT_3D ( 'NONE', #12159, #7013, #16278 ) ;
#10462=EDGE_LOOP ( 'NONE', ( #2012, #11420, #19086, #1012 ) ) ;
#10463=CARTESIAN_POINT ( 'NONE',  ( -0.1294417382415922191, 0.3125000000000000000, 0.2237500000000031686 ) ) ;
#10464=CARTESIAN_POINT ( 'NONE',  ( 0.3155070326520292290, 0.1306872919485615736, 0.04145833333333503318 ) ) ;
#10466=VECTOR ( 'NONE', #12613, 39.37007874015748143 ) ;
#10467=CARTESIAN_POINT ( 'NONE',  ( 0.000000000000000000, 3.738758431839877614E-19, 0.000000000000000000 ) ) ;
#10470=CARTESIAN_POINT ( 'NONE',  ( 0.2764156081756483641, -0.1144950937579611167, -0.04708333333333256793 ) ) ;
#10473=CARTESIAN_POINT ( 'NONE',  ( 0.1954553509668046640, -0.1954553509668047195, 0.4494444444444491427 ) ) ;
#10477=LINE ( 'NONE', #21798, #5555 ) ;
#10483=ORIENTED_EDGE ( 'NONE', *, *, #11697, .F. ) ;
#10488=CARTESIAN_POINT ( 'NONE',  ( 0.1850421345843279164, -0.2494223792521799987, 0.4217812969067588624 ) ) ;
#10489=CARTESIAN_POINT ( 'NONE',  ( 0.4687500000000003886, -0.2629256801278681555, 0.05975678175779897128 ) ) ;
#10491=CARTESIAN_POINT ( 'NONE',  ( -0.4802534626491987146, 0.2139708740945671928, 0.05347073504130966243 ) ) ;
#10492=CARTESIAN_POINT ( 'NONE',  ( -0.2764156081756484196, 0.1144950937579609918, 0.02930555555555695163 ) ) ;
#10496=CARTESIAN_POINT ( 'NONE',  ( -0.1954553509668046918, -0.1954553509668046640, 0.2133333333333361503 ) ) ;
#10500=CARTESIAN_POINT ( 'NONE',  ( -0.4795759075923611281, 0.04315783544084986906, 0.07439896364138827434 ) ) ;
#10502=CARTESIAN_POINT ( 'NONE',  ( 0.1954553509668046640, -0.1954553509668047195, 0.05361111111111271227 ) ) ;
#10503=CARTESIAN_POINT ( 'NONE',  ( 0.3155070326520292290, -0.1306872919485616569, 0.4199305555555598590 ) ) ;
#10515=ORIENTED_EDGE ( 'NONE', *, *, #3643, .T. ) ;
#10519=DIRECTION ( 'NONE',  ( 0.000000000000000000, 0.000000000000000000, -1.000000000000000000 ) ) ;
#10535=DIRECTION ( 'NONE',  ( -0.000000000000000000, 0.9767851838303063250, 0.2142211582677935044 ) ) ;
#10536=EDGE_CURVE ( 'NONE', #10074, #10173, #11722, .T. ) ;
#10537=CARTESIAN_POINT ( 'NONE',  ( 6.402768735150616610E-17, -0.5196152422706635798, 0.3779506566538943235 ) ) ;
#10549=ORIENTED_EDGE ( 'NONE', *, *, #6164, .T. ) ;
#10551=EDGE_LOOP ( 'NONE', ( #19933, #6089, #2371, #11286 ) ) ;
#10559=ORIENTED_EDGE ( 'NONE', *, *, #13293, .T. ) ;
#10562=CARTESIAN_POINT ( 'NONE',  ( -0.4687500000000003886, 0.04410323065863043512, 0.4181500734908987771 ) ) ;
#10565=EDGE_LOOP ( 'NONE', ( #17314, #10709, #15233, #9196, #4622 ) ) ;
#10570=CARTESIAN_POINT ( 'NONE',  ( 0.2764156081756483641, 0.1144950937579610056, 0.1195833333333354703 ) ) ;
#10572=CARTESIAN_POINT ( 'NONE',  ( 0.2245903949464508609, 0.1902879574984975564, -0.08291343549538147950 ) ) ;
#10574=CARTESIAN_POINT ( 'NONE',  ( -0.2209708691207961373, -0.2209708691207961095, -0.04361111111111047600 ) ) ;
#10578=EDGE_CURVE ( 'NONE', #9622, #15906, #7821, .T. ) ;
#10580=EDGE_CURVE ( 'NONE', #17016, #11636, #21309, .T. ) ;
#10581=CARTESIAN_POINT ( 'NONE',  ( -0.3125000000000000000, 1.913510623667739771E-17, 0.2272222222222250176 ) ) ;
#10584=CARTESIAN_POINT ( 'NONE',  ( 0.2230971623002954429, 0.2230971623002953319, 0.04493055555555729857 ) ) ;
#10588=CARTESIAN_POINT ( 'NONE',  ( -1.949169748562458500E-16, 0.5196152422706634688, 0.3779506566538943790 ) ) ;
#10589=CARTESIAN_POINT ( 'NONE',  ( -0.2764156081756484196, 0.1144950937579609918, -0.01930555555555454883 ) ) ;
#10591=CARTESIAN_POINT ( 'NONE',  ( 0.2764156081756483641, 0.1144950937579610056, 0.4598611111111158833 ) ) ;
#10595=DIRECTION ( 'NONE',  ( 0.000000000000000000, 0.000000000000000000, -1.000000000000000000 ) ) ;
#10603=CARTESIAN_POINT ( 'NONE',  ( 0.009375000000000067307, -0.5358532185916218271, 0.06112444011295370405 ) ) ;
#10607=DIRECTION ( 'NONE',  ( -0.8459207832372978020, 0.4883925919151543282, 0.2142211582677917281 ) ) ;
#10609=CARTESIAN_POINT ( 'NONE',  ( 0.1954553509668046640, -0.1954553509668047195, 0.1091666666666687158 ) ) ;
#10611=CARTESIAN_POINT ( 'NONE',  ( -0.3125000000000002776, 0.1294417382415919970, -0.05402777777777723056 ) ) ;
#10613=CARTESIAN_POINT ( 'NONE',  ( -0.1144950937579609779, 0.2764156081756484196, 0.1959722222222249899 ) ) ;
#10616=CARTESIAN_POINT ( 'NONE',  ( 0.1294417382415924134, 0.3124999999999999445, -0.06097222222222135196 ) ) ;
#10620=CARTESIAN_POINT ( 'NONE',  ( 0.000000000000000000, 0.2764156081756484196, 0.1300000000000022249 ) ) ;
#10621=CARTESIAN_POINT ( 'NONE',  ( 0.000000000000000000, 0.3155070326520292845, 0.4372916666666711305 ) ) ;
#10622=ORIENTED_EDGE ( 'NONE', *, *, #23606, .T. ) ;
#10625=CARTESIAN_POINT ( 'NONE',  ( 0.4687500000000002776, 0.2178650770398900538, 0.3900584262746596420 ) ) ;
#10645=DIRECTION ( 'NONE',  ( -0.8459207832372988012, -0.4883925919151527184, -0.2142211582677917836 ) ) ;
#10656=CARTESIAN_POINT ( 'NONE',  ( 0.4687500000000002776, 0.2598076211353318454, 0.06112444011295372487 ) ) ;
#10672=CARTESIAN_POINT ( 'NONE',  ( 0.3125000000000000555, -5.740531871003217465E-17, 0.2619444444444478659 ) ) ;
#10684=CARTESIAN_POINT ( 'NONE',  ( -3.385114897866767815E-17, -0.2764156081756484196, 0.3800000000000042233 ) ) ;
#10687=CARTESIAN_POINT ( 'NONE',  ( 0.2523926463571754542, 0.1523216146538573512, -0.08381099440924590083 ) ) ;
#10689=LINE ( 'NONE', #20432, #18607 ) ;
#10697=CARTESIAN_POINT ( 'NONE',  ( -0.3155070326520293400, 0.1306872919485614903, 0.3400694444444484765 ) ) ;
#10702=DIRECTION ( 'NONE',  ( -1.224646799147353207E-16, 1.000000000000000000, 0.000000000000000000 ) ) ;
#10705=CARTESIAN_POINT ( 'NONE',  ( 0.2764156081756483641, -0.1144950937579611167, 0.008472222222223456389 ) ) ;
#10709=ORIENTED_EDGE ( 'NONE', *, *, #2102, .F. ) ;
#10712=CYLINDRICAL_SURFACE ( 'NONE', #7880, 0.3125000000000000000 ) ;
#10713=CARTESIAN_POINT ( 'NONE',  ( -0.4801334617939588822, 0.2624565244266455766, 0.04287645741408795813 ) ) ;
#10723=CARTESIAN_POINT ( 'NONE',  ( -3.827021247335479543E-17, -0.3125000000000000000, 0.1300000000000020028 ) ) ;
#10726=AXIS2_PLACEMENT_3D ( 'NONE', #5476, #24116, #1809 ) ;
#10728=DIRECTION ( 'NONE',  ( 1.000000000000000000, 1.821231995776178240E-15, 0.000000000000000000 ) ) ;
#10729=CARTESIAN_POINT ( 'NONE',  ( 0.1144950937579611444, 0.2764156081756483641, 0.2931944444444479769 ) ) ;
#10734=CARTESIAN_POINT ( 'NONE',  ( 0.2764156081756483641, 0.1144950937579610195, 0.3487500000000039457 ) ) ;
#10738=CARTESIAN_POINT ( 'NONE',  ( 0.4687500000000002776, 0.04363579668119251659, 0.07944722321499816942 ) ) ;
#10741=CARTESIAN_POINT ( 'NONE',  ( 0.2764156081756483641, -0.1144950937579611028, 0.1126388888888909395 ) ) ;
#10742=CARTESIAN_POINT ( 'NONE',  ( -0.2764156081756484196, -0.1144950937579609362, 0.04319444444444596465 ) ) ;
#10745=CARTESIAN_POINT ( 'NONE',  ( 0.09135502326330754985, 0.5015332108058753180, 0.06108558933789665774 ) ) ;
#10755=CARTESIAN_POINT ( 'NONE',  ( -0.4687500000000003886, 0.2598076211353315124, 0.06112444011295379426 ) ) ;
#10767=CIRCLE ( 'NONE', #20140, 0.01874999999999999584 ) ;
#10784=CARTESIAN_POINT ( 'NONE',  ( -0.6288319206375506676, 3.738758431839877614E-19, 0.004799741732707325965 ) ) ;
#10794=EDGE_CURVE ( 'NONE', #10448, #4062, #21581, .T. ) ;
#10798=CARTESIAN_POINT ( 'NONE',  ( -0.08700723303875142201, -0.2927098606306429707, 0.4165748844700365994 ) ) ;
#10804=DIRECTION ( 'NONE',  ( 0.000000000000000000, 0.000000000000000000, 1.000000000000000000 ) ) ;
#10809=CARTESIAN_POINT ( 'NONE',  ( -0.1144950937579609918, -0.2764156081756484196, 0.3209722222222259891 ) ) ;
#10812=EDGE_CURVE ( 'NONE', #280, #1241, #9105, .T. ) ;
#10820=CARTESIAN_POINT ( 'NONE',  ( -0.2209708691207961095, 0.2209708691207961373, 0.2202777777777805146 ) ) ;
#10824=CARTESIAN_POINT ( 'NONE',  ( 0.2230971623002954429, 0.2230971623002953319, 0.3227083333333373161 ) ) ;
#10826=ORIENTED_EDGE ( 'NONE', *, *, #12675, .F. ) ;
#10827=CARTESIAN_POINT ( 'NONE',  ( 0.1953806383669984825, -0.4284628132096562347, 0.4289620446068268533 ) ) ;
#10831=CARTESIAN_POINT ( 'NONE',  ( -0.1144950937579609918, -0.2764156081756484196, 0.1612500000000023914 ) ) ;
#10852=CARTESIAN_POINT ( 'NONE',  ( 0.1144950937579609085, -0.2764156081756484751, 0.1612500000000025024 ) ) ;
#10862=CARTESIAN_POINT ( 'NONE',  ( -0.1144950937579609779, 0.2764156081756484196, -0.03319444444444354797 ) ) ;
#10863=CARTESIAN_POINT ( 'NONE',  ( 0.2764156081756483641, 0.1144950937579610056, 0.07097222222222394905 ) ) ;
#10893=CARTESIAN_POINT ( 'NONE',  ( -0.3155070326520292845, 1.931923388228935888E-17, -0.1043749999999998707 ) ) ;
#10894=CARTESIAN_POINT ( 'NONE',  ( 0.3125000000000000000, -5.740531871003217465E-17, 0.4216666666666709085 ) ) ;
#10899=FACE_OUTER_BOUND ( 'NONE', #546, .T. ) ;
#10910=EDGE_LOOP ( 'NONE', ( #21994, #1129, #11264, #5721 ) ) ;
#10928=CARTESIAN_POINT ( 'NONE',  ( 0.2764156081756483641, -0.1144950937579611167, 0.2793055555555589153 ) ) ;
#10929=ADVANCED_FACE ( 'NONE', ( #22064 ), #5066, .T. ) ;
#10932=CARTESIAN_POINT ( 'NONE',  ( 0.2744310710835856093, -0.1177455570400168794, 0.4097706279014594610 ) ) ;
#10937=CIRCLE ( 'NONE', #6638, 0.6288319206375507786 ) ;
#10942=ORIENTED_EDGE ( 'NONE', *, *, #22479, .T. ) ;
#10943=CARTESIAN_POINT ( 'NONE',  ( 0.2230971623002953874, -0.2230971623002954429, 0.3643750000000042788 ) ) ;
#10946=CARTESIAN_POINT ( 'NONE',  ( 0.3838430204063560391, -0.3081239094298764414, 0.4164750180373182897 ) ) ;
#10950=CARTESIAN_POINT ( 'NONE',  ( -0.2764156081756484196, 0.1144950937579609918, 0.2029166666666694097 ) ) ;
#10954=EDGE_LOOP ( 'NONE', ( #17693, #7838, #21613 ) ) ;
#10965=CARTESIAN_POINT ( 'NONE',  ( 0.003278813451167444763, 0.5383665848074060678, 0.05892894635879485088 ) ) ;
#10966=B_SPLINE_CURVE_WITH_KNOTS ( 'NONE', 3,
 ( #21538, #6664, #17888, #4598, #10338, #6305, #10219, #2536, #17643, #9982 ),
 .UNSPECIFIED., .F., .F.,
 ( 4, 2, 2, 2, 4 ),
 ( 0.000000000000000000, 0.003321633220911225995, 0.006643266441822451990, 0.009964899662733677985, 0.01328653288364490398 ),
 .UNSPECIFIED. ) ;
#10969=ORIENTED_EDGE ( 'NONE', *, *, #23301, .T. ) ;
#10973=CARTESIAN_POINT ( 'NONE',  ( -0.1954553509668046918, -0.1954553509668046640, 0.1508333333333357063 ) ) ;
#10974=ADVANCED_FACE ( 'NONE', ( #6832, #21709 ), #8774, .T. ) ;
#10978=CARTESIAN_POINT ( 'NONE',  ( -0.1954553509668046640, 0.1954553509668046918, 0.3661111111111151617 ) ) ;
#10984=CARTESIAN_POINT ( 'NONE',  ( 0.2764156081756483641, 0.1144950937579610056, 0.01541666666666794208 ) ) ;
#10995=ORIENTED_EDGE ( 'NONE', *, *, #20666, .T. ) ;
#11003=CARTESIAN_POINT ( 'NONE',  ( -0.4683396222371151718, 0.2655382811872564197, 0.04698599556840152291 ) ) ;
#11026=CARTESIAN_POINT ( 'NONE',  ( -0.3096487991955141350, 0.3624900597954727188, 0.07655254331177274718 ) ) ;
#11038=LINE ( 'NONE', #5419, #19845 ) ;
#11040=CARTESIAN_POINT ( 'NONE',  ( -0.009375000000000190473, 0.5358532185916217161, 0.3779506566538943790 ) ) ;
#11041=DIRECTION ( 'NONE',  ( -0.000000000000000000, -0.000000000000000000, -1.000000000000000000 ) ) ;
#11046=CARTESIAN_POINT ( 'NONE',  ( 0.1144950937579611444, 0.2764156081756483641, 0.1820833333333359561 ) ) ;
#11047=AXIS2_PLACEMENT_3D ( 'NONE', #9638, #13195, #11472 ) ;
#11050=CARTESIAN_POINT ( 'NONE',  ( 0.3023734573831431405, -0.03492818159268935158, 0.4159249849313371161 ) ) ;
#11062=CARTESIAN_POINT ( 'NONE',  ( -0.1306872919485614903, 0.3155070326520293400, 0.2775694444444480324 ) ) ;
#11065=FACE_OUTER_BOUND ( 'NONE', #9288, .T. ) ;
#11068=CARTESIAN_POINT ( 'NONE',  ( 0.1144950937579609085, -0.2764156081756484751, 0.1681944444444469222 ) ) ;
#11071=ORIENTED_EDGE ( 'NONE', *, *, #5219, .F. ) ;
#11076=CARTESIAN_POINT ( 'NONE',  ( -0.3125000000000000000, 1.913510623667739771E-17, 0.3383333333333369830 ) ) ;
#11087=CARTESIAN_POINT ( 'NONE',  ( -0.4500000000000003997, -0.2598076211353319009, 0.3779506566538942125 ) ) ;
#11088=CARTESIAN_POINT ( 'NONE',  ( 0.1954553509668047195, 0.1954553509668046085, 0.1786111111111137462 ) ) ;
#11092=CARTESIAN_POINT ( 'NONE',  ( -0.01294618724694486522, -0.5474118055169125974, 0.04270874187135764027 ) ) ;
#11098=CARTESIAN_POINT ( 'NONE',  ( 0.1954553509668046640, -0.1954553509668047195, -0.1061111111111108091 ) ) ;
#11102=CARTESIAN_POINT ( 'NONE',  ( 0.4592349292584271825, -0.08929898372139863372, 0.4306178066313481878 ) ) ;
#11110=DIRECTION ( 'NONE',  ( 1.000000000000000000, 0.000000000000000000, 0.000000000000000000 ) ) ;
#11112=EDGE_CURVE ( 'NONE', #4857, #8682, #3234, .T. ) ;
#11122=CARTESIAN_POINT ( 'NONE',  ( -0.4678838860311506087, 0.2663291305467040404, 0.05893128447555430471 ) ) ;
#11128=CARTESIAN_POINT ( 'NONE',  ( 0.3125000000000000000, 3.827021247335477694E-17, 1.326383476483184332 ) ) ;
#11132=CARTESIAN_POINT ( 'NONE',  ( -0.2230971623002953874, 0.2230971623002954152, -0.05576388888888837714 ) ) ;
#11133=FACE_OUTER_BOUND ( 'NONE', #13877, .T. ) ;
#11144=CARTESIAN_POINT ( 'NONE',  ( -0.009374999999999951081, -0.5358532185916218271, 0.4425000000000000044 ) ) ;
#11148=CARTESIAN_POINT ( 'NONE',  ( -0.3291860208797072751, 0.3512102395969135538, 0.4108348780186336091 ) ) ;
#11153=VERTEX_POINT ( 'NONE', #24122 ) ;
#11155=CARTESIAN_POINT ( 'NONE',  ( 0.4570242136016680612, -0.2774028246161726607, 0.04874733047934382002 ) ) ;
#11168=CIRCLE ( 'NONE', #20883, 0.01874999999999999237 ) ;
#11169=VERTEX_POINT ( 'NONE', #13415 ) ;
#11171=CARTESIAN_POINT ( 'NONE',  ( -3.385114897866767815E-17, -0.2764156081756484196, 0.2133333333333362336 ) ) ;
#11184=ORIENTED_EDGE ( 'NONE', *, *, #4050, .T. ) ;
#11186=CARTESIAN_POINT ( 'NONE',  ( 0.3155070326520292845, -5.795770164686806123E-17, 0.3157638888888927853 ) ) ;
#11188=CARTESIAN_POINT ( 'NONE',  ( 0.3107848814624034617, -0.3618341423928899125, 0.4134938258000521172 ) ) ;
#11191=CARTESIAN_POINT ( 'NONE',  ( -0.1144950937579609779, 0.2764156081756484196, 0.3070833333333369275 ) ) ;
#11208=CARTESIAN_POINT ( 'NONE',  ( -0.04615996209784192089, -0.5146154108223025547, 0.3902123106865083013 ) ) ;
#11209=DIRECTION ( 'NONE',  ( 0.000000000000000000, 0.000000000000000000, -1.000000000000000000 ) ) ;
#11210=CARTESIAN_POINT ( 'NONE',  ( 0.1954553509668046640, -0.1954553509668047195, 0.2758333333333367055 ) ) ;
#11213=ORIENTED_EDGE ( 'NONE', *, *, #15292, .F. ) ;
#11214=EDGE_CURVE ( 'NONE', #15369, #23837, #23139, .T. ) ;
#11220=CARTESIAN_POINT ( 'NONE',  ( -0.2209708691207961373, -0.2209708691207961095, 0.06750000000000151712 ) ) ;
#11221=CARTESIAN_POINT ( 'NONE',  ( 0.1144950937579611444, 0.2764156081756483641, 0.02236111111111246247 ) ) ;
#11224=CARTESIAN_POINT ( 'NONE',  ( 0.4687500000000002776, 0.1103509067785291842, 0.4107148665556337175 ) ) ;
#11247=VECTOR ( 'NONE', #13687, 39.37007874015748143 ) ;
#11254=CARTESIAN_POINT ( 'NONE',  ( -3.863846776457871776E-17, -0.3155070326520292845, -0.09048611111111086458 ) ) ;
#11255=CARTESIAN_POINT ( 'NONE',  ( 0.4687500000000002776, -0.2598076211353317344, 0.3779506566538943235 ) ) ;
#11260=EDGE_CURVE ( 'NONE', #280, #8797, #2928, .T. ) ;
#11264=ORIENTED_EDGE ( 'NONE', *, *, #2968, .F. ) ;
#11265=CARTESIAN_POINT ( 'NONE',  ( -0.2721215285213482993, 0.3841564396211271104, 0.07944889038199838549 ) ) ;
#11277=ADVANCED_FACE ( 'NONE', ( #21437 ), #13770, .F. ) ;
#11278=EDGE_LOOP ( 'NONE', ( #10515, #4804, #1283, #17984 ) ) ;
#11286=ORIENTED_EDGE ( 'NONE', *, *, #20352, .T. ) ;
#11289=EDGE_CURVE ( 'NONE', #14698, #15146, #17193, .T. ) ;
#11291=CARTESIAN_POINT ( 'NONE',  ( 0.1975560007912697535, -0.2122688852239507096, 0.4011227751864958058 ) ) ;
#11292=CARTESIAN_POINT ( 'NONE',  ( 0.08367472778091819552, -0.4929562507565927731, 0.07813238993955244627 ) ) ;
#11303=CARTESIAN_POINT ( 'NONE',  ( 0.4723638629038580117, 0.2802187124228171511, 0.04193801346286276516 ) ) ;
#11308=CARTESIAN_POINT ( 'NONE',  ( 0.1144950937579611444, 0.2764156081756483641, -0.04013888888888803019 ) ) ;
#11310=CARTESIAN_POINT ( 'NONE',  ( 0.1954553509668046640, -0.1954553509668047195, 0.1716666666666691599 ) ) ;
#11313=CARTESIAN_POINT ( 'NONE',  ( -0.003278813451167537571, -0.5383665848074061788, 0.05892894635879412230 ) ) ;
#11319=CARTESIAN_POINT ( 'NONE',  ( 0.4620753182980354423, 0.2744865679600219099, 0.05975678175779888801 ) ) ;
#11330=CARTESIAN_POINT ( 'NONE',  ( -0.1306872919485614903, 0.3155070326520293400, -0.1113194444444439435 ) ) ;
#11340=CARTESIAN_POINT ( 'NONE',  ( 0.2156887100776809230, 0.4167379425407623517, 0.4181572966874575470 ) ) ;
#11341=CARTESIAN_POINT ( 'NONE',  ( -0.1144950937579609779, 0.2764156081756484196, 0.08486111111111295513 ) ) ;
#11345=CARTESIAN_POINT ( 'NONE',  ( 0.4687500000000002220, -0.2630787017013381246, 0.3892820121258429023 ) ) ;
#11349=CARTESIAN_POINT ( 'NONE',  ( 0.3125000000000000000, -5.740531871003217465E-17, 0.03972222222222387966 ) ) ;
#11356=CARTESIAN_POINT ( 'NONE',  ( -0.2209708691207961095, 0.2209708691207961373, 0.005000000000001404363 ) ) ;
#11358=( LENGTH_UNIT ( ) NAMED_UNIT ( * ) SI_UNIT ( $, .METRE. ) );
#11359=CARTESIAN_POINT ( 'NONE',  ( -0.009375000000000190473, 0.5358532185916217161, 0.06112444011295373181 ) ) ;
#11365=CARTESIAN_POINT ( 'NONE',  ( 0.1954553509668046640, -0.1954553509668047195, 0.005000000000001192726 ) ) ;
#11372=CARTESIAN_POINT ( 'NONE',  ( -0.1306872919485615459, -0.3155070326520293400, -0.03840277777777712648 ) ) ;
#11373=CARTESIAN_POINT ( 'NONE',  ( -0.1961921601747129984, -0.4279942808755098360, 0.09139393128960894563 ) ) ;
#11374=CARTESIAN_POINT ( 'NONE',  ( -0.4687500000000003886, -0.2706329386826373806, 0.4425000000000000044 ) ) ;
#11385=ADVANCED_FACE ( 'NONE', ( #17486 ), #9367, .T. ) ;
#11386=CARTESIAN_POINT ( 'NONE',  ( 0.03811151966992424450, -0.3039168590976173978, -0.09500335358987550827 ) ) ;
#11387=ORIENTED_EDGE ( 'NONE', *, *, #3258, .F. ) ;
#11397=CARTESIAN_POINT ( 'NONE',  ( 0.04549985820533886810, 0.5149965219823321450, 0.3899922761137797900 ) ) ;
#11407=CARTESIAN_POINT ( 'NONE',  ( -0.3112631253509005602, -0.3615580281551280528, 0.4252366019055051072 ) ) ;
#11413=EDGE_CURVE ( 'NONE', #22186, #16785, #14436, .T. ) ;
#11420=ORIENTED_EDGE ( 'NONE', *, *, #677, .T. ) ;
#11429=CARTESIAN_POINT ( 'NONE',  ( 0.3838280543219422247, 0.3196626468799559362, 0.06591465713332961274 ) ) ;
#11430=CARTESIAN_POINT ( 'NONE',  ( 0.1583113556674259903, -0.4498647735549116122, 0.08855526556984566477 ) ) ;
#11431=CARTESIAN_POINT ( 'NONE',  ( 0.1144950937579609085, -0.2764156081756484751, 0.3279166666666704644 ) ) ;
#11433=CARTESIAN_POINT ( 'NONE',  ( -0.1144950937579609779, 0.2764156081756484196, 0.4181944444444490316 ) ) ;
#11437=CARTESIAN_POINT ( 'NONE',  ( -0.4593750000000003664, -6.734002413227273428E-17, 0.4343810118395207698 ) ) ;
#11450=CARTESIAN_POINT ( 'NONE',  ( -0.2730703793714975292, -0.3836086203274272077, 0.4181140142936807802 ) ) ;
#11451=ADVANCED_FACE ( 'NONE', ( #21504 ), #20528, .F. ) ;
#11453=CARTESIAN_POINT ( 'NONE',  ( -0.3155070326520293400, 0.1306872919485614903, -0.1599305555555554370 ) ) ;
#11460=CARTESIAN_POINT ( 'NONE',  ( 0.1144950937579609085, -0.2764156081756484751, -0.1095833333333330467 ) ) ;
#11463=CARTESIAN_POINT ( 'NONE',  ( -0.1954553509668046640, 0.1954553509668046918, 0.2550000000000031686 ) ) ;
#11467=CARTESIAN_POINT ( 'NONE',  ( 0.2998642343065497373, 0.08796414601275419354, 0.4241666666666771834 ) ) ;
#11472=DIRECTION ( 'NONE',  ( -1.000000000000000000, 0.000000000000000000, 0.000000000000000000 ) ) ;
#11486=CARTESIAN_POINT ( 'NONE',  ( 0.1144950937579609085, -0.2764156081756484751, 0.001527777777778949230 ) ) ;
#11487=( BOUNDED_CURVE ( )  B_SPLINE_CURVE ( 2, ( #17505, #15680, #19454, #21288, #2401, #6161, #11786, #8347, #8228 ),
 .UNSPECIFIED., .F., .T. ) 
 B_SPLINE_CURVE_WITH_KNOTS ( ( 3, 2, 2, 2, 3 ),
 ( 0.7812500000000001110, 0.7916666666666668517, 0.8020833333333334814, 0.8125000000000000000, 0.8229166666666667407 ),
 .UNSPECIFIED. ) 
 CURVE ( )  GEOMETRIC_REPRESENTATION_ITEM ( )  RATIONAL_B_SPLINE_CURVE ( ( 0.9999999999999992228, 0.9238795325112875156, 1.000000000000000000, 0.9238795325112867385, 1.000000000000000000, 0.9238795325112867385, 1.000000000000000000, 0.9238795325112867385, 1.000000000000000000 ) ) 
 REPRESENTATION_ITEM ( '' )  );
#11492=CYLINDRICAL_SURFACE ( 'NONE', #16631, 0.3125000000000000000 ) ;
#11494=CARTESIAN_POINT ( 'NONE',  ( 0.000000000000000000, 0.3155070326520292845, 0.1595138888888911199 ) ) ;
#11495=CARTESIAN_POINT ( 'NONE',  ( -0.3838280543219043661, -0.3196626468799559362, 0.06591465713332006482 ) ) ;
#11510=CARTESIAN_POINT ( 'NONE',  ( 0.2256529556067323194, -0.2011140187169014881, -0.09097104604570598052 ) ) ;
#11511=ORIENTED_EDGE ( 'NONE', *, *, #12472, .F. ) ;
#11515=DIRECTION ( 'NONE',  ( 0.000000000000000000, 0.000000000000000000, -1.000000000000000000 ) ) ;
#11517=ORIENTED_EDGE ( 'NONE', *, *, #18095, .F. ) ;
#11519=ORIENTED_EDGE ( 'NONE', *, *, #18421, .T. ) ;
#11529=CARTESIAN_POINT ( 'NONE',  ( -0.1954553509668046640, 0.1954553509668046918, 0.4147222222222267107 ) ) ;
#11533=CARTESIAN_POINT ( 'NONE',  ( 0.4593750000000003664, -0.2760455974562899817, 0.06112444011295372487 ) ) ;
#11547=CARTESIAN_POINT ( 'NONE',  ( 0.000000000000000000, 0.000000000000000000, 1.326383476483184332 ) ) ;
#11552=CARTESIAN_POINT ( 'NONE',  ( 0.2764156081756483641, -0.1144950937579611028, 0.3418055555555594149 ) ) ;
#11557=CARTESIAN_POINT ( 'NONE',  ( -0.2764156081756484196, 1.692557448933383907E-17, 0.1438888888888912032 ) ) ;
#11559=CARTESIAN_POINT ( 'NONE',  ( 0.2764156081756483641, 0.1144950937579610056, 0.4043055555555599145 ) ) ;
#11564=CARTESIAN_POINT ( 'NONE',  ( -0.2107751267066935164, 0.1916353986792941333, -0.07341118351979945833 ) ) ;
#11568=CARTESIAN_POINT ( 'NONE',  ( 0.4687500000000002776, 0.2598076211353318454, 0.06112444011295372487 ) ) ;
#11579=CARTESIAN_POINT ( 'NONE',  ( 0.2764156081756483641, -0.1144950937579611167, 0.4459722222222269328 ) ) ;
#11588=CARTESIAN_POINT ( 'NONE',  ( 0.000000000000000000, 0.2764156081756484196, 0.1369444444444467002 ) ) ;
#11590=CARTESIAN_POINT ( 'NONE',  ( 0.3124999999999996669, 0.1294417382415925521, 0.3209722222222261001 ) ) ;
#11595=CARTESIAN_POINT ( 'NONE',  ( -0.3257020783361852523, 0.3421021315173792821, 0.4271664148355318602 ) ) ;
#11600=CARTESIAN_POINT ( 'NONE',  ( 0.3147071693084030897, -0.3721877333702315882, 0.07155713030921627416 ) ) ;
#11601=CARTESIAN_POINT ( 'NONE',  ( 0.1294417382415924134, 0.3124999999999999445, -0.005416666666665343258 ) ) ;
#11603=CARTESIAN_POINT ( 'NONE',  ( 0.4802535697964960826, -0.2139886670027110471, 0.05346678874215700372 ) ) ;
#11604=CARTESIAN_POINT ( 'NONE',  ( 0.000000000000000000, 0.2764156081756484196, -0.1477777777777777857 ) ) ;
#11609=ORIENTED_EDGE ( 'NONE', *, *, #14593, .F. ) ;
#11613=CARTESIAN_POINT ( 'NONE',  ( -0.1306872919485614903, 0.3155070326520293400, 0.1074305555555573888 ) ) ;
#11614=CARTESIAN_POINT ( 'NONE',  ( -0.3146687483788879192, -0.3722097299877869525, 0.07156199457777932815 ) ) ;
#11636=VERTEX_POINT ( 'NONE', #20404 ) ;
#11651=CARTESIAN_POINT ( 'NONE',  ( 0.1144950937579611444, 0.2764156081756483641, 0.4043055555555599145 ) ) ;
#11662=ORIENTED_EDGE ( 'NONE', *, *, #5716, .T. ) ;
#11663=EDGE_CURVE ( 'NONE', #5916, #22186, #2028, .T. ) ;
#11664=ORIENTED_EDGE ( 'NONE', *, *, #23173, .T. ) ;
#11666=DIRECTION ( 'NONE',  ( 1.000000000000000000, 0.000000000000000000, 0.000000000000000000 ) ) ;
#11673=CARTESIAN_POINT ( 'NONE',  ( 0.01172578639831966391, -0.5344959914317446437, 0.04874733047933994118 ) ) ;
#11674=CARTESIAN_POINT ( 'NONE',  ( -0.2764156081756484196, 0.1144950937579609918, 0.3070833333333369830 ) ) ;
#11676=CARTESIAN_POINT ( 'NONE',  ( 0.2764156081756483641, -0.1144950937579611167, 0.4529166666666714636 ) ) ;
#11695=CARTESIAN_POINT ( 'NONE',  ( -0.1144950937579609918, -0.2764156081756484196, 0.4320833333333379822 ) ) ;
#11697=EDGE_CURVE ( 'NONE', #6549, #21116, #7244, .T. ) ;
#11698=ORIENTED_EDGE ( 'NONE', *, *, #3944, .T. ) ;
#11704=CARTESIAN_POINT ( 'NONE',  ( -0.2887653152721422756, -0.08545421435185589221, -0.08979496337181655519 ) ) ;
#11705=CARTESIAN_POINT ( 'NONE',  ( -3.385114897866767815E-17, -0.2764156081756484196, 0.2202777777777806811 ) ) ;
#11707=CARTESIAN_POINT ( 'NONE',  ( 0.000000000000000000, 3.738758431839877614E-19, 0.4425000000000000044 ) ) ;
#11713=CARTESIAN_POINT ( 'NONE',  ( -0.2676934969451049695, 0.3758505236666521698, 0.4334994210334168208 ) ) ;
#11716=CARTESIAN_POINT ( 'NONE',  ( -0.1294417382415922746, -0.3125000000000000000, 0.1334722222222246568 ) ) ;
#11718=CARTESIAN_POINT ( 'NONE',  ( 0.01848103877824576122, 0.5441716683897390716, 0.04413116910601656839 ) ) ;
#11722=CIRCLE ( 'NONE', #1192, 0.01874999999999999237 ) ;
#11723=EDGE_CURVE ( 'NONE', #12731, #18391, #15246, .T. ) ;
#11730=CARTESIAN_POINT ( 'NONE',  ( -3.385114897866767815E-17, -0.2764156081756484196, -0.05749999999999930167 ) ) ;
#11736=CARTESIAN_POINT ( 'NONE',  ( 0.3125000000000000000, -5.740531871003217465E-17, -0.02277777777777697382 ) ) ;
#11737=CARTESIAN_POINT ( 'NONE',  ( -0.1306872919485614903, 0.3155070326520293400, 0.2185416666666694097 ) ) ;
#11749=EDGE_LOOP ( 'NONE', ( #19370, #18922, #7892, #6425, #17936, #17132, #15451 ) ) ;
#11750=CARTESIAN_POINT ( 'NONE',  ( 0.1294417382415924134, 0.3124999999999999445, 0.09875000000000175304 ) ) ;
#11753=CARTESIAN_POINT ( 'NONE',  ( 0.1484667313406524691, -0.2653928060426358204, -0.09280364848304442638 ) ) ;
#11754=ORIENTED_EDGE ( 'NONE', *, *, #1278, .T. ) ;
#11770=CARTESIAN_POINT ( 'NONE',  ( 0.2764156081756483641, 0.1144950937579610056, 0.4529166666666715191 ) ) ;
#11772=CARTESIAN_POINT ( 'NONE',  ( -0.4581189881604794123, -0.2644951211353319120, 0.3941886329748525153 ) ) ;
#11786=CARTESIAN_POINT ( 'NONE',  ( -0.2209708691207961373, -0.2209708691207961095, -0.09222222222222160870 ) ) ;
#11787=CARTESIAN_POINT ( 'NONE',  ( 0.3103970466387488414, -0.3620580589327280219, 0.08855978515307991183 ) ) ;
#11788=CARTESIAN_POINT ( 'NONE',  ( -0.2764156081756484196, 1.692557448933383907E-17, 0.2550000000000032241 ) ) ;
#11790=CARTESIAN_POINT ( 'NONE',  ( -0.2764156081756484196, 0.1144950937579609918, -0.08180555555555503455 ) ) ;
#11791=VERTEX_POINT ( 'NONE', #16510 ) ;
#11793=DIRECTION ( 'NONE',  ( 0.000000000000000000, 0.000000000000000000, -1.000000000000000000 ) ) ;
#11796=CARTESIAN_POINT ( 'NONE',  ( 0.4584481579615881097, -0.2211256433011207223, 0.4059661290276580514 ) ) ;
#11803=CARTESIAN_POINT ( 'NONE',  ( 0.000000000000000000, 3.738758431839877614E-19, 0.4241666666666665253 ) ) ;
#11808=DIMENSIONAL_EXPONENTS ( 1.000000000000000000, 0.000000000000000000, 0.000000000000000000, 0.000000000000000000, 0.000000000000000000, 0.000000000000000000, 0.000000000000000000 ) ;
#11809=CARTESIAN_POINT ( 'NONE',  ( 0.3124999999999993339, 0.1294417382415928297, 0.2029166666666692709 ) ) ;
#11816=CARTESIAN_POINT ( 'NONE',  ( 0.000000000000000000, 0.3155070326520292845, -0.1703472222222222054 ) ) ;
#11823=CARTESIAN_POINT ( 'NONE',  ( -0.3125000000000000000, 1.913510623667739771E-17, 0.4008333333333378712 ) ) ;
#11824=CARTESIAN_POINT ( 'NONE',  ( -0.07165243469752499705, -0.2702856358549580174, -0.06824753933085654645 ) ) ;
#11825=CARTESIAN_POINT ( 'NONE',  ( -0.1954553509668046918, -0.1954553509668046640, 0.2688888888888921747 ) ) ;
#11834=VECTOR ( 'NONE', #19495, 39.37007874015748143 ) ;
#11839=ORIENTED_EDGE ( 'NONE', *, *, #18713, .T. ) ;
#11843=EDGE_CURVE ( 'NONE', #22186, #175, #4707, .T. ) ;
#11844=CARTESIAN_POINT ( 'NONE',  ( 0.009374999999999683933, 0.5358532185916218271, 0.06112444011295371793 ) ) ;
#11845=CARTESIAN_POINT ( 'NONE',  ( 0.3291860208797072196, -0.3512102395969137758, 0.4108348780186337201 ) ) ;
#11848=CARTESIAN_POINT ( 'NONE',  ( 0.2694453590030795320, 0.3748737188716305679, 0.4343212420608417168 ) ) ;
#11849=CARTESIAN_POINT ( 'NONE',  ( -0.1144950937579609918, -0.2764156081756484196, -0.1234722222222220528 ) ) ;
#11855=CARTESIAN_POINT ( 'NONE',  ( -0.2764156081756484196, 0.1144950937579609918, 0.03625000000000144079 ) ) ;
#11862=CARTESIAN_POINT ( 'NONE',  ( 0.1306872919485614071, -0.3155070326520293955, 0.07965277777777936274 ) ) ;
#11866=CARTESIAN_POINT ( 'NONE',  ( -0.2209708691207961095, 0.2209708691207961373, 0.3869444444444485320 ) ) ;
#11876=CARTESIAN_POINT ( 'NONE',  ( 0.3125000000000000555, -5.740531871003217465E-17, 0.08833333333333501236 ) ) ;
#11880=CARTESIAN_POINT ( 'NONE',  ( 0.09798969090652687175, -0.2586227216849679156, 0.3880822748423150004 ) ) ;
#11892=FACE_OUTER_BOUND ( 'NONE', #22490, .T. ) ;
#11899=CARTESIAN_POINT ( 'NONE',  ( -0.3125000000000000000, 1.913510623667739771E-17, 0.06055555555555702796 ) ) ;
#11901=CARTESIAN_POINT ( 'NONE',  ( -0.2725502669324379457, -0.3839089073841076560, 0.4290249205313916292 ) ) ;
#11902=PRODUCT_DEFINITION_FORMATION_WITH_SPECIFIED_SOURCE ( 'ANY', '', #1355, .NOT_KNOWN. ) ;
#11906=VERTEX_POINT ( 'NONE', #13780 ) ;
#11911=EDGE_LOOP ( 'NONE', ( #18052, #9886, #22452, #19000 ) ) ;
#11921=CARTESIAN_POINT ( 'NONE',  ( 0.1144950937579611444, 0.2764156081756483641, 0.2376388888888919526 ) ) ;
#11923=CARTESIAN_POINT ( 'NONE',  ( -0.1954553509668046918, -0.1954553509668046640, -0.1269444444444442766 ) ) ;
#11931=DIRECTION ( 'NONE',  ( 0.000000000000000000, 1.000000000000000000, 0.000000000000000000 ) ) ;
#11933=DIRECTION ( 'NONE',  ( 1.000000000000000000, 0.000000000000000000, 0.000000000000000000 ) ) ;
#11940=ORIENTED_EDGE ( 'NONE', *, *, #8157, .F. ) ;
#11945=CARTESIAN_POINT ( 'NONE',  ( -0.3155070326520292845, 1.931923388228935888E-17, 0.06576388888889080075 ) ) ;
#11946=CARTESIAN_POINT ( 'NONE',  ( 0.2774186958558277349, 0.3935988683107602415, 0.07439726544912801665 ) ) ;
#11953=CARTESIAN_POINT ( 'NONE',  ( -3.827021247335479543E-17, -0.3125000000000000000, 0.4147222222222268773 ) ) ;
#11956=ORIENTED_EDGE ( 'NONE', *, *, #3944, .F. ) ;
#11959=CARTESIAN_POINT ( 'NONE',  ( -0.2209708691207961095, 0.2209708691207961373, 0.3383333333333373716 ) ) ;
#11966=DIRECTION ( 'NONE',  ( 0.000000000000000000, 0.000000000000000000, -1.000000000000000000 ) ) ;
#11971=CARTESIAN_POINT ( 'NONE',  ( 0.1591012008044834503, 0.4494087562524295421, 0.07655254331174679572 ) ) ;
#11972=CARTESIAN_POINT ( 'NONE',  ( 0.04611292249197068011, -0.5146425691514149303, 0.3901966308178844711 ) ) ;
#11975=ADVANCED_FACE ( 'NONE', ( #4619 ), #23005, .T. ) ;
#11976=CARTESIAN_POINT ( 'NONE',  ( 0.2764156081756484196, -5.077672346800151106E-17, 0.06055555555555720143 ) ) ;
#11980=CARTESIAN_POINT ( 'NONE',  ( 0.000000000000000000, 0.2764156081756484196, 0.2480555555555586933 ) ) ;
#11987=CARTESIAN_POINT ( 'NONE',  ( 0.3155070326520292845, -5.795770164686806123E-17, 0.1456250000000021139 ) ) ;
#11989=CARTESIAN_POINT ( 'NONE',  ( 0.1294417382415924134, 0.3124999999999999445, 0.04319444444444578424 ) ) ;
#12001=SHAPE_REPRESENTATION ( '94902A107_High-Strength Steel Flange Nut_94902A107', ( #9127 ), #20827 ) ;
#12006=ORIENTED_EDGE ( 'NONE', *, *, #11260, .T. ) ;
#12011=AXIS2_PLACEMENT_3D ( 'NONE', #18241, #1540, #14591 ) ;
#12028=AXIS2_PLACEMENT_3D ( 'NONE', #12517, #10442, #17868 ) ;
#12034=ORIENTED_EDGE ( 'NONE', *, *, #5219, .T. ) ;
#12036=CARTESIAN_POINT ( 'NONE',  ( -0.1334180974147631815, -0.4531173396632154349, 0.4271664148355316382 ) ) ;
#12039=CARTESIAN_POINT ( 'NONE',  ( -0.4581189881604794678, -0.2644951211353318010, 0.3941886329748525153 ) ) ;
#12044=CARTESIAN_POINT ( 'NONE',  ( -0.1954553509668046918, -0.1954553509668046640, 0.09527777777777970969 ) ) ;
#12048=CARTESIAN_POINT ( 'NONE',  ( -0.2799731695447704727, 0.01905728454626067631, -0.06962859169959349781 ) ) ;
#12051=DIRECTION ( 'NONE',  ( 0.000000000000000000, -0.2142211582677922832, 0.9767851838303064360 ) ) ;
#12059=CARTESIAN_POINT ( 'NONE',  ( -0.3125000000000000000, -0.1294417382415921913, 0.07097222222222411558 ) ) ;
#12062=DIRECTION ( 'NONE',  ( 1.000000000000000000, 0.000000000000000000, 0.000000000000000000 ) ) ;
#12063=CARTESIAN_POINT ( 'NONE',  ( 0.3155070326520292290, -0.1306872919485616569, 0.1456250000000025580 ) ) ;
#12064=ADVANCED_FACE ( 'NONE', ( #21689 ), #2157, .F. ) ;
#12069=CARTESIAN_POINT ( 'NONE',  ( 0.2764156081756483641, 0.1144950937579610056, 0.1265277777777799595 ) ) ;
#12072=CARTESIAN_POINT ( 'NONE',  ( -3.385114897866767815E-17, -0.2764156081756484196, 0.4425000000000046119 ) ) ;
#12076=CARTESIAN_POINT ( 'NONE',  ( 0.2209708691207961651, 0.2209708691207959985, 0.3244444444444484210 ) ) ;
#12084=CARTESIAN_POINT ( 'NONE',  ( -0.4212185919419081936, 0.2861805174102238225, 0.4063787963957418148 ) ) ;
#12092=CARTESIAN_POINT ( 'NONE',  ( -1.889944503261478141E-16, 0.5289902422706634910, 0.3941886329748526263 ) ) ;
#12095=CARTESIAN_POINT ( 'NONE',  ( -0.2764156081756484196, 1.692557448933383907E-17, 0.03277777777777921009 ) ) ;
#12101=CARTESIAN_POINT ( 'NONE',  ( 0.2764156081756483641, 0.1144950937579610195, 0.2376388888888919526 ) ) ;
#12104=CARTESIAN_POINT ( 'NONE',  ( 0.4795759095149518814, -0.04342522374607015595, 0.07439890854714663326 ) ) ;
#12108=CARTESIAN_POINT ( 'NONE',  ( 0.2230971623002954429, 0.2230971623002953319, 0.4859027777777825685 ) ) ;
#12111=CARTESIAN_POINT ( 'NONE',  ( 0.1294417382415924134, 0.3124999999999999445, 0.3765277777777817358 ) ) ;
#12119=AXIS2_PLACEMENT_3D ( 'NONE', #11707, #597, #15480 ) ;
#12122=EDGE_LOOP ( 'NONE', ( #7631, #6452, #22707, #15225 ) ) ;
#12131=ORIENTED_EDGE ( 'NONE', *, *, #11112, .T. ) ;
#12158=CARTESIAN_POINT ( 'NONE',  ( 7.478516849590708700E-17, -0.5289902422706634910, 0.3941886329748525153 ) ) ;
#12159=CARTESIAN_POINT ( 'NONE',  ( 0.5601250000000235207, 0.000000000000000000, -0.05999999999999999084 ) ) ;
#12162=CARTESIAN_POINT ( 'NONE',  ( -2.038214714022946347E-16, 0.5196152422706634688, 0.4425000000000000044 ) ) ;
#12166=CARTESIAN_POINT ( 'NONE',  ( -0.1954553509668046918, -0.1954553509668046640, 0.03972222222222369925 ) ) ;
#12170=CARTESIAN_POINT ( 'NONE',  ( 0.02575435819785588942, 0.2888475187005514200, -0.07854616851683961232 ) ) ;
#12172=CARTESIAN_POINT ( 'NONE',  ( 0.3125000000000000000, -5.740531871003217465E-17, -0.01583333333333210996 ) ) ;
#12178=CARTESIAN_POINT ( 'NONE',  ( 0.4570242136016807732, 0.2774028246161672207, 0.04874733047933993424 ) ) ;
#12179=ORIENTED_EDGE ( 'NONE', *, *, #5432, .T. ) ;
#12186=CARTESIAN_POINT ( 'NONE',  ( -0.1306872919485615459, -0.3155070326520293400, 0.07618055555555755531 ) ) ;
#12190=ADVANCED_FACE ( 'NONE', ( #5420 ), #6659, .F. ) ;
#12193=CARTESIAN_POINT ( 'NONE',  ( 0.1954553509668046640, -0.1954553509668047195, 0.06055555555555720143 ) ) ;
#12195=CARTESIAN_POINT ( 'NONE',  ( 0.2764156081756484196, -5.077672346800151106E-17, 0.4008333333333376491 ) ) ;
#12208=CARTESIAN_POINT ( 'NONE',  ( -3.827021247335479543E-17, -0.3125000000000000000, -0.02972222222222110216 ) ) ;
#12214=CARTESIAN_POINT ( 'NONE',  ( -0.1954553509668046640, 0.1954553509668046918, 0.02583333333333472440 ) ) ;
#12217=CARTESIAN_POINT ( 'NONE',  ( -0.1294417382415922746, -0.3125000000000000000, 0.2931944444444478104 ) ) ;
#12218=CARTESIAN_POINT ( 'NONE',  ( -0.2764156081756484196, -0.1144950937579609362, 0.2098611111111139405 ) ) ;
#12221=CARTESIAN_POINT ( 'NONE',  ( 0.4687500000000002776, 0.04414013450030943031, 0.09139228974507368486 ) ) ;
#12222=CARTESIAN_POINT ( 'NONE',  ( 0.3125000000000000000, -5.740531871003217465E-17, 0.3105555555555590819 ) ) ;
#12223=CARTESIAN_POINT ( 'NONE',  ( -0.3850708708653799439, 0.3189451064140638170, 0.07813342133392807420 ) ) ;
#12225=CARTESIAN_POINT ( 'NONE',  ( 0.1306872919485616846, 0.3155070326520292290, 0.3227083333333368720 ) ) ;
#12240=CARTESIAN_POINT ( 'NONE',  ( 0.4593750000000003664, -0.2760455974562899817, 0.06112444011295372487 ) ) ;
#12242=ORIENTED_EDGE ( 'NONE', *, *, #22626, .F. ) ;
#12251=CARTESIAN_POINT ( 'NONE',  ( 0.3125000000000000000, 3.864408831653876942E-17, -0.1016666666666665164 ) ) ;
#12260=CARTESIAN_POINT ( 'NONE',  ( -0.4805070082343983473, -0.2560807851245620048, 0.04413116910602134235 ) ) ;
#12273=CARTESIAN_POINT ( 'NONE',  ( -0.2209708691207961373, -0.2209708691207961095, 0.2411111111111144123 ) ) ;
#12276=EDGE_CURVE ( 'NONE', #10173, #5967, #5542, .T. ) ;
#12277=DIRECTION ( 'NONE',  ( 0.000000000000000000, 0.000000000000000000, -1.000000000000000000 ) ) ;
#12279=( BOUNDED_CURVE ( )  B_SPLINE_CURVE ( 2, ( #1172, #8610, #4943, #19826, #1051, #1295, #16171, #21528, #21774 ),
 .UNSPECIFIED., .F., .T. ) 
 B_SPLINE_CURVE_WITH_KNOTS ( ( 3, 2, 2, 2, 3 ),
 ( 0.7708333333333333703, 0.7812500000000000000, 0.7916666666666667407, 0.8020833333333334814, 0.8125000000000001110 ),
 .UNSPECIFIED. ) 
 CURVE ( )  GEOMETRIC_REPRESENTATION_ITEM ( )  RATIONAL_B_SPLINE_CURVE ( ( 1.000000000000000000, 0.9238795325112867385, 1.000000000000000000, 0.9238795325112867385, 1.000000000000000000, 0.9238795325112867385, 1.000000000000000000, 0.9238795325112859613, 1.000000000000000888 ) ) 
 REPRESENTATION_ITEM ( '' )  );
#12284=CARTESIAN_POINT ( 'NONE',  ( 0.1144950937579609085, -0.2764156081756484751, 0.05013888888889045381 ) ) ;
#12300=CARTESIAN_POINT ( 'NONE',  ( -0.1306872919485614903, 0.3155070326520293400, -0.05576388888888796774 ) ) ;
#12306=CARTESIAN_POINT ( 'NONE',  ( -0.1954553509668046640, 0.1954553509668046918, 0.08833333333333517889 ) ) ;
#12309=CARTESIAN_POINT ( 'NONE',  ( -0.2764156081756484196, -0.1144950937579609362, 0.3209722222222259891 ) ) ;
#12315=CARTESIAN_POINT ( 'NONE',  ( -0.4581189881604794678, -0.2644951211353319120, 0.3941886329748524598 ) ) ;
#12321=CARTESIAN_POINT ( 'NONE',  ( -0.3858656996965449948, 0.3184862117744308718, 0.4002370417399356284 ) ) ;
#12324=CARTESIAN_POINT ( 'NONE',  ( -0.1294417382415922746, -0.3125000000000000000, -0.03319444444444336062 ) ) ;
#12331=CARTESIAN_POINT ( 'NONE',  ( -0.1144950937579609918, -0.2764156081756484196, -0.01236111111111004406 ) ) ;
#12337=CARTESIAN_POINT ( 'NONE',  ( 0.1144950937579609085, -0.2764156081756484751, 0.1681944444444469222 ) ) ;
#12344=CARTESIAN_POINT ( 'NONE',  ( 0.1144950937579609085, -0.2764156081756484751, 0.05013888888889046075 ) ) ;
#12345=CARTESIAN_POINT ( 'NONE',  ( 0.1306872919485614071, -0.3155070326520293955, 0.3574305555555593594 ) ) ;
#12364=ORIENTED_EDGE ( 'NONE', *, *, #17117, .T. ) ;
#12371=DIRECTION ( 'NONE',  ( 0.7071067811865484609, 8.659560562354943952E-17, -0.7071067811865464625 ) ) ;
#12381=DIRECTION ( 'NONE',  ( -1.000000000000000000, 0.000000000000000000, 0.000000000000000000 ) ) ;
#12385=CARTESIAN_POINT ( 'NONE',  ( -0.4687500000000022760, -0.2630304559196449121, 0.05971082423031025266 ) ) ;
#12400=CARTESIAN_POINT ( 'NONE',  ( -0.4593752539607652285, 0.04502204785529886899, 0.4343880498115386124 ) ) ;
#12405=CARTESIAN_POINT ( 'NONE',  ( -0.1144950937579609918, -0.2764156081756484196, 0.09875000000000196121 ) ) ;
#12407=CARTESIAN_POINT ( 'NONE',  ( 0.1347750699935957031, 0.2587654721081569797, -0.08077297511795365759 ) ) ;
#12415=EDGE_LOOP ( 'NONE', ( #5509, #23686, #5453, #4064 ) ) ;
#12418=ADVANCED_FACE ( 'NONE', ( #6495 ), #4635, .F. ) ;
#12419=CARTESIAN_POINT ( 'NONE',  ( -3.863846776457871776E-17, -0.3155070326520292845, -0.03145833333333220710 ) ) ;
#12427=CARTESIAN_POINT ( 'NONE',  ( 0.1144950937579609085, -0.2764156081756484751, 0.05708333333333493603 ) ) ;
#12430=CARTESIAN_POINT ( 'NONE',  ( 0.1954553509668046640, -0.1954553509668047195, 0.3938888888888931739 ) ) ;
#12441=CARTESIAN_POINT ( 'NONE',  ( 0.2209708691207961651, 0.2209708691207959985, 0.1022222222222243793 ) ) ;
#12447=CARTESIAN_POINT ( 'NONE',  ( -0.4500000000000003997, -0.2598076211353319009, 0.4425000000000000044 ) ) ;
#12448=CARTESIAN_POINT ( 'NONE',  ( 0.1144950937579611444, 0.2764156081756483641, 0.01541666666666797678 ) ) ;
#12452=CARTESIAN_POINT ( 'NONE',  ( -3.385114897866767815E-17, -0.2764156081756484196, 0.1091666666666686880 ) ) ;
#12455=CARTESIAN_POINT ( 'NONE',  ( -0.1261236974911686404, 0.2628820852880375813, 0.4030844371307044094 ) ) ;
#12457=DIRECTION ( 'NONE',  ( -1.000000000000000000, 0.000000000000000000, 0.000000000000000000 ) ) ;
#12458=CARTESIAN_POINT ( 'NONE',  ( -0.01833836887209681216, -0.2764156081756484751, -0.06500058086764817777 ) ) ;
#12459=CARTESIAN_POINT ( 'NONE',  ( -0.3155070326520293400, -0.1306872919485614626, 0.3990972222222263777 ) ) ;
#12461=CARTESIAN_POINT ( 'NONE',  ( 0.4687500000000002220, 0.2630787017013384577, 0.3892820121258428467 ) ) ;
#12472=EDGE_CURVE ( 'NONE', #4536, #6549, #5077, .T. ) ;
#12504=CARTESIAN_POINT ( 'NONE',  ( -0.4621664414996935477, -0.2744339579550151287, 0.05971062996526614597 ) ) ;
#12511=EDGE_CURVE ( 'NONE', #20369, #18391, #18726, .T. ) ;
#12517=CARTESIAN_POINT ( 'NONE',  ( -0.6211549996190571798, 0.000000000000000000, -0.1012499999999999928 ) ) ;
#12528=CARTESIAN_POINT ( 'NONE',  ( -0.2764156081756484196, 1.692557448933383907E-17, 0.3661111111111152172 ) ) ;
#12538=VERTEX_POINT ( 'NONE', #6222 ) ;
#12541=CARTESIAN_POINT ( 'NONE',  ( 0.000000000000000000, 0.3155070326520292845, 0.3296527777777817358 ) ) ;
#12547=CARTESIAN_POINT ( 'NONE',  ( -0.1954553509668046640, 0.1954553509668046918, 0.03277777777777921009 ) ) ;
#12550=EDGE_LOOP ( 'NONE', ( #6518, #6785, #4574, #2150 ) ) ;
#12560=CARTESIAN_POINT ( 'NONE',  ( -0.009375000000000169656, 0.5358532185916217161, 0.06112444011295373875 ) ) ;
#12561=ORIENTED_EDGE ( 'NONE', *, *, #22586, .F. ) ;
#12567=CARTESIAN_POINT ( 'NONE',  ( -0.4593750000000004219, -0.2760455974562901482, 0.06112444011295364160 ) ) ;
#12568=CARTESIAN_POINT ( 'NONE',  ( -0.1954553509668046640, 0.1954553509668046918, 0.1369444444444467002 ) ) ;
#12571=CARTESIAN_POINT ( 'NONE',  ( 0.4620259694561523744, 0.2880908832651560281, 0.04413116910601654758 ) ) ;
#12572=CARTESIAN_POINT ( 'NONE',  ( -0.006454613307746792129, -0.5491961284534644383, 0.04193467568257210759 ) ) ;
#12575=CARTESIAN_POINT ( 'NONE',  ( 0.4687500000000002776, 0.1743477725058785177, 0.07807923930880629471 ) ) ;
#12579=CARTESIAN_POINT ( 'NONE',  ( -0.2764156081756484196, 1.692557448933383907E-17, 0.03277777777777921009 ) ) ;
#12580=CARTESIAN_POINT ( 'NONE',  ( 0.3155070326520292845, -5.795770164686806123E-17, 0.3678472222222261001 ) ) ;
#12600=ORIENTED_EDGE ( 'NONE', *, *, #4199, .T. ) ;
#12604=EDGE_LOOP ( 'NONE', ( #18466, #23699, #3493, #24069, #12768, #4224, #5997, #22771, #12936, #688 ) ) ;
#12610=CARTESIAN_POINT ( 'NONE',  ( 0.000000000000000000, 0.000000000000000000, 1.326383476483184332 ) ) ;
#12613=DIRECTION ( 'NONE',  ( 0.000000000000000000, 0.000000000000000000, -1.000000000000000000 ) ) ;
#12614=CARTESIAN_POINT ( 'NONE',  ( 0.2998642343065497373, 0.08796414601275419354, 0.4241666666666771834 ) ) ;
#12622=DIRECTION ( 'NONE',  ( -1.000000000000000000, 0.000000000000000000, 0.000000000000000000 ) ) ;
#12631=VERTEX_POINT ( 'NONE', #13917 ) ;
#12637=ORIENTED_EDGE ( 'NONE', *, *, #8564, .F. ) ;
#12640=CARTESIAN_POINT ( 'NONE',  ( 0.3096898932022673079, 0.3624663341596540134, 0.07654795713851909877 ) ) ;
#12646=ORIENTED_EDGE ( 'NONE', *, *, #4005, .F. ) ;
#12648=APPLICATION_CONTEXT ( 'configuration controlled 3d designs of mechanical parts and assemblies' ) ;
#12650=CARTESIAN_POINT ( 'NONE',  ( 0.2764156081756483641, -0.1144950937579611167, 0.3904166666666709085 ) ) ;
#12651=EDGE_CURVE ( 'NONE', #7279, #3958, #18688, .T. ) ;
#12654=CARTESIAN_POINT ( 'NONE',  ( 0.1054825322676819915, -0.2618223909956544082, 0.3934028307984435147 ) ) ;
#12662=CARTESIAN_POINT ( 'NONE',  ( -0.2230971623002954152, -0.2230971623002953874, 0.1838194444444472553 ) ) ;
#12665=CARTESIAN_POINT ( 'NONE',  ( 0.4581189881604794678, -0.2644951211353317455, 0.3941886329748525153 ) ) ;
#12666=PRODUCT_DEFINITION_SHAPE ( 'NONE', 'NONE',  #14477 ) ;
#12669=CARTESIAN_POINT ( 'NONE',  ( 0.1144950937579611444, 0.2764156081756483641, 0.2445833333333364279 ) ) ;
#12675=EDGE_CURVE ( 'NONE', #9702, #2053, #13836, .T. ) ;
#12680=CARTESIAN_POINT ( 'NONE',  ( 0.3124999999999999445, 0.1294417382415923023, 0.3140277777777812362 ) ) ;
#12687=ORIENTED_EDGE ( 'NONE', *, *, #20031, .F. ) ;
#12688=CARTESIAN_POINT ( 'NONE',  ( 0.006674681701965033860, -0.5374122480878900099, 0.05975678175779891577 ) ) ;
#12691=AXIS2_PLACEMENT_3D ( 'NONE', #21905, #10702, #1434 ) ;
#12692=CARTESIAN_POINT ( 'NONE',  ( -0.4687500000000003886, -0.2598076211353319009, 0.06112444011295369711 ) ) ;
#12693=CARTESIAN_POINT ( 'NONE',  ( 0.2764156081756483641, -0.1144950937579611167, 0.3348611111111149952 ) ) ;
#12695=DIRECTION ( 'NONE',  ( -1.000000000000000000, 0.000000000000000000, 0.000000000000000000 ) ) ;
#12706=CARTESIAN_POINT ( 'NONE',  ( 0.1954553509668047195, 0.1954553509668046085, 0.06750000000000172529 ) ) ;
#12707=CARTESIAN_POINT ( 'NONE',  ( 0.2764156081756484196, -5.077672346800151106E-17, 0.06750000000000168365 ) ) ;
#12710=CARTESIAN_POINT ( 'NONE',  ( 0.01848103877824584448, 0.5441716683897389606, 0.04413116910601658227 ) ) ;
#12711=CARTESIAN_POINT ( 'NONE',  ( 0.4584464601845412712, -0.2220115010439547287, 0.4062888617107747180 ) ) ;
#12730=CARTESIAN_POINT ( 'NONE',  ( 0.2977072594216367274, -5.468793635004571549E-17, -0.08687392608830331320 ) ) ;
#12731=VERTEX_POINT ( 'NONE', #19392 ) ;
#12737=CARTESIAN_POINT ( 'NONE',  ( 0.1306872919485614071, -0.3155070326520293955, -0.03145833333333261650 ) ) ;
#12747=CARTESIAN_POINT ( 'NONE',  ( 0.4687500000000003886, -0.08745052389986661401, 0.08858773447093017117 ) ) ;
#12751=CARTESIAN_POINT ( 'NONE',  ( -0.1965595339002992048, 0.4277821775562039019, 0.07944544255962410206 ) ) ;
#12768=ORIENTED_EDGE ( 'NONE', *, *, #6236, .F. ) ;
#12771=CARTESIAN_POINT ( 'NONE',  ( 0.1144950937579611444, 0.2764156081756483641, 0.2931944444444479769 ) ) ;
#12775=CARTESIAN_POINT ( 'NONE',  ( 0.05416907386903872107, -0.2729753724328379261, 0.3894056226408110222 ) ) ;
#12781=CARTESIAN_POINT ( 'NONE',  ( 0.01874999999999976685, 0.5520911949125799634, 0.06112444011295372487 ) ) ;
#12782=CARTESIAN_POINT ( 'NONE',  ( 0.1419551320365925184, -0.2751926619865908696, 0.4208614314731936590 ) ) ;
#12786=EDGE_CURVE ( 'NONE', #15581, #8592, #16281, .T. ) ;
#12787=CARTESIAN_POINT ( 'NONE',  ( 0.000000000000000000, 0.3155070326520292845, 0.1629861111111137739 ) ) ;
#12793=CARTESIAN_POINT ( 'NONE',  ( -0.2764156081756484196, 1.692557448933383907E-17, 0.2063888888888917028 ) ) ;
#12809=ORIENTED_EDGE ( 'NONE', *, *, #11214, .T. ) ;
#12816=CARTESIAN_POINT ( 'NONE',  ( -0.1144950937579609779, 0.2764156081756484196, 0.2445833333333364834 ) ) ;
#12819=CARTESIAN_POINT ( 'NONE',  ( -0.01848103877824600061, -0.5441716683897390716, 0.04413116910601655452 ) ) ;
#12825=CARTESIAN_POINT ( 'NONE',  ( 0.000000000000000000, 0.2764156081756484196, -0.1408333333333332826 ) ) ;
#12829=CARTESIAN_POINT ( 'NONE',  ( 0.4687500000000195954, 0.08968933634053308235, 0.4243607940295692216 ) ) ;
#12868=CARTESIAN_POINT ( 'NONE',  ( -0.4581189881604794678, 0.2644951211353315235, 0.3941886329748525153 ) ) ;
#12875=ORIENTED_EDGE ( 'NONE', *, *, #6401, .T. ) ;
#12880=CARTESIAN_POINT ( 'NONE',  ( 0.4620259694561340003, -0.2880908832651663531, 0.04413116910602139092 ) ) ;
#12883=DIRECTION ( 'NONE',  ( 0.000000000000000000, 0.000000000000000000, -1.000000000000000000 ) ) ;
#12886=AXIS2_PLACEMENT_3D ( 'NONE', #10103, #13992, #17526 ) ;
#12887=CARTESIAN_POINT ( 'NONE',  ( -0.2209708691207961373, -0.2209708691207961095, 0.1855555555555583880 ) ) ;
#12895=CARTESIAN_POINT ( 'NONE',  ( 0.2764156081756483641, 0.1144950937579610056, 0.2306944444444475328 ) ) ;
#12898=CARTESIAN_POINT ( 'NONE',  ( 0.2353592251390298207, -0.1755526922479773988, 0.4047588300480876589 ) ) ;
#12905=B_SPLINE_CURVE_WITH_KNOTS ( 'NONE', 3,
 ( #3894, #9504, #16938, #23484, #21318, #14241, #3024, #4841 ),
 .UNSPECIFIED., .F., .F.,
 ( 4, 2, 2, 4 ),
 ( 0.000000000000000000, 0.0004997454757086380699, 0.0007496182135629584058, 0.0009994909514172787418 ),
 .UNSPECIFIED. ) ;
#12908=CARTESIAN_POINT ( 'NONE',  ( -0.3155070326520293400, 0.1306872919485614903, 0.2289583333333365389 ) ) ;
#12910=CARTESIAN_POINT ( 'NONE',  ( 0.4254812175019097586, -0.2956141819053919040, 0.4012599972958754702 ) ) ;
#12918=CARTESIAN_POINT ( 'NONE',  ( 0.2764156081756484196, -5.077672346800151106E-17, 0.2897222222222257115 ) ) ;
#12924=CYLINDRICAL_SURFACE ( 'NONE', #22199, 0.3125000000000000000 ) ;
#12926=CARTESIAN_POINT ( 'NONE',  ( 0.000000000000000000, 0.3125000000000000000, 0.3244444444444480324 ) ) ;
#12936=ORIENTED_EDGE ( 'NONE', *, *, #1301, .T. ) ;
#12939=CARTESIAN_POINT ( 'NONE',  ( 0.2764156081756483641, 0.1144950937579610056, 0.1751388888888914530 ) ) ;
#12943=CARTESIAN_POINT ( 'NONE',  ( -0.1144950937579609918, -0.2764156081756484196, 0.3834722222222265997 ) ) ;
#12949=CARTESIAN_POINT ( 'NONE',  ( -0.2764156081756484196, -0.1144950937579609362, -0.1234722222222220528 ) ) ;
#12964=B_SPLINE_CURVE_WITH_KNOTS ( 'NONE', 3,
 ( #16619, #15036, #384, #7824, #17098, #20870, #1980, #2095, #22333, #24039, #3809, #11255 ),
 .UNSPECIFIED., .F., .F.,
 ( 4, 2, 2, 2, 2, 4 ),
 ( 0.000000000000000000, 0.003350371137362711908, 0.006700742274725423817, 0.01005111341208813659, 0.01172629898076949471, 0.01340148454945085110 ),
 .UNSPECIFIED. ) ;
#12976=CARTESIAN_POINT ( 'NONE',  ( 0.3155070326520292290, -0.1306872919485616569, 0.03104166666666787963 ) ) ;
#12978=CARTESIAN_POINT ( 'NONE',  ( -0.4224968603155689340, -0.2973372013303092753, 0.07046346805499673072 ) ) ;
#12990=CARTESIAN_POINT ( 'NONE',  ( -0.3064624847683589115, 0.3533192024756441341, 0.4298724737630857384 ) ) ;
#12999=CARTESIAN_POINT ( 'NONE',  ( -0.2969103404914473776, -0.03343391069993188053, 0.4099802347466152130 ) ) ;
#13002=ORIENTED_EDGE ( 'NONE', *, *, #13931, .T. ) ;
#13004=VERTEX_POINT ( 'NONE', #13857 ) ;
#13012=CARTESIAN_POINT ( 'NONE',  ( 0.1954553509668046640, -0.1954553509668047195, 0.2758333333333367055 ) ) ;
#13017=CARTESIAN_POINT ( 'NONE',  ( -0.01848103877824625041, 0.5441716683897389606, 0.04413116910601661003 ) ) ;
#13024=ADVANCED_FACE ( 'NONE', ( #4579 ), #15117, .F. ) ;
#13029=CARTESIAN_POINT ( 'NONE',  ( -0.3155070326520292845, 1.931923388228935888E-17, 0.1768750000000028078 ) ) ;
#13031=CARTESIAN_POINT ( 'NONE',  ( -2.617362320975981593E-17, -0.5289902422706636020, 0.3941886329748526263 ) ) ;
#13035=CARTESIAN_POINT ( 'NONE',  ( -0.1144950937579609918, -0.2764156081756484196, 0.2723611111111143845 ) ) ;
#13046=DIRECTION ( 'NONE',  ( 0.000000000000000000, 0.000000000000000000, -1.000000000000000000 ) ) ;
#13054=CARTESIAN_POINT ( 'NONE',  ( -0.2764156081756484196, 1.692557448933383907E-17, 0.1994444444444472553 ) ) ;
#13058=CARTESIAN_POINT ( 'NONE',  ( 0.4805456235326253656, 0.2624941757204518611, 0.04270874187135768885 ) ) ;
#13064=CARTESIAN_POINT ( 'NONE',  ( 0.1144950937579609085, -0.2764156081756484751, 0.001527777777778949230 ) ) ;
#13077=ORIENTED_EDGE ( 'NONE', *, *, #23286, .F. ) ;
#13100=CARTESIAN_POINT ( 'NONE',  ( -3.863846776457871776E-17, -0.3155070326520292845, -0.03493055555555487496 ) ) ;
#13102=DIRECTION ( 'NONE',  ( -1.000000000000000000, 0.000000000000000000, 0.000000000000000000 ) ) ;
#13111=CARTESIAN_POINT ( 'NONE',  ( -0.3103970466387204197, 0.3620580589327443422, 0.08855978515309881338 ) ) ;
#13115=CARTESIAN_POINT ( 'NONE',  ( 0.2144047338281417914, -0.2134821532158128754, -0.09126195324992800173 ) ) ;
#13119=CARTESIAN_POINT ( 'NONE',  ( -0.2879402880768345274, -0.08326397218408013168, 0.4109361999077702499 ) ) ;
#13125=VERTEX_POINT ( 'NONE', #5896 ) ;
#13129=CARTESIAN_POINT ( 'NONE',  ( -0.3125000000000000000, 0.000000000000000000, 1.326383476483184332 ) ) ;
#13132=CIRCLE ( 'NONE', #2599, 0.01875000000000000625 ) ;
#13138=CARTESIAN_POINT ( 'NONE',  ( -0.4687500000000003886, -0.04388698013647557988, 0.09139229829490845558 ) ) ;
#13150=CARTESIAN_POINT ( 'NONE',  ( -0.1306872919485614903, 0.3155070326520293400, 0.3886805555555600256 ) ) ;
#13156=CARTESIAN_POINT ( 'NONE',  ( 0.1954553509668047195, 0.1954553509668046085, 0.1230555555555576941 ) ) ;
#13158=CARTESIAN_POINT ( 'NONE',  ( -0.2764156081756484196, 0.1144950937579609918, 0.3140277777777814583 ) ) ;
#13160=CARTESIAN_POINT ( 'NONE',  ( 0.008437752171426261827, -0.5369270166837818437, 0.04763592618480781693 ) ) ;
#13175=CARTESIAN_POINT ( 'NONE',  ( -0.3125000000000000000, 0.000000000000000000, 1.326383476483184332 ) ) ;
#13177=CARTESIAN_POINT ( 'NONE',  ( 0.2230971623002954429, 0.2230971623002953319, -0.1217361111111106980 ) ) ;
#13181=ORIENTED_EDGE ( 'NONE', *, *, #3978, .T. ) ;
#13184=CARTESIAN_POINT ( 'NONE',  ( 0.3125000000000004996, 0.1294417382415917750, 0.1543055555555580549 ) ) ;
#13187=CARTESIAN_POINT ( 'NONE',  ( 0.1954553509668047195, 0.1954553509668046085, 0.01888888888889020401 ) ) ;
#13195=DIRECTION ( 'NONE',  ( 0.000000000000000000, 0.000000000000000000, -1.000000000000000000 ) ) ;
#13201=CARTESIAN_POINT ( 'NONE',  ( -0.3125000000000000000, 1.913510623667739771E-17, 0.01194444444444589179 ) ) ;
#13206=CARTESIAN_POINT ( 'NONE',  ( -0.4620259694561341668, 0.2880908832651660756, 0.04413116910602139092 ) ) ;
#13208=CARTESIAN_POINT ( 'NONE',  ( 0.1144950937579609085, -0.2764156081756484751, 0.05708333333333493603 ) ) ;
#13211=CIRCLE ( 'NONE', #19040, 0.01875000000000000625 ) ;
#13215=DIRECTION ( 'NONE',  ( -1.000000000000000000, 0.000000000000000000, 0.000000000000000000 ) ) ;
#13218=CARTESIAN_POINT ( 'NONE',  ( -0.3155070326520293400, 0.1306872919485614903, -0.05229166666666613256 ) ) ;
#13219=CARTESIAN_POINT ( 'NONE',  ( -0.1966284714786305232, -0.4277423764267367923, 0.07944889038203660492 ) ) ;
#13233=CARTESIAN_POINT ( 'NONE',  ( 0.2460300421372865198, -0.1745426587113542150, -0.09035713772767853258 ) ) ;
#13234=ORIENTED_EDGE ( 'NONE', *, *, #1111, .T. ) ;
#13241=ORIENTED_EDGE ( 'NONE', *, *, #7969, .F. ) ;
#13242=CARTESIAN_POINT ( 'NONE',  ( -0.3125000000000000000, 1.913510623667739771E-17, 0.1786111111111139127 ) ) ;
#13253=CARTESIAN_POINT ( 'NONE',  ( -0.4622078388679875527, -0.2744100571732869254, 0.3892820121258429023 ) ) ;
#13258=EDGE_CURVE ( 'NONE', #17766, #13298, #1514, .T. ) ;
#13267=FACE_OUTER_BOUND ( 'NONE', #12415, .T. ) ;
#13272=CARTESIAN_POINT ( 'NONE',  ( -0.1954553509668046918, -0.1954553509668046640, 0.2619444444444477549 ) ) ;
#13274=CARTESIAN_POINT ( 'NONE',  ( -0.1144950937579609779, 0.2764156081756484196, 0.3626388888888929518 ) ) ;
#13276=CARTESIAN_POINT ( 'NONE',  ( -0.004187250022457828999, -0.5383673285787258234, 0.04698409998688798245 ) ) ;
#13293=EDGE_CURVE ( 'NONE', #16468, #23807, #18709, .T. ) ;
#13294=CARTESIAN_POINT ( 'NONE',  ( 0.2230971623002953874, -0.2230971623002954429, -0.08006944444444370756 ) ) ;
#13298=VERTEX_POINT ( 'NONE', #13242 ) ;
#13304=CARTESIAN_POINT ( 'NONE',  ( -0.2764156081756484196, -0.1144950937579609362, 0.09875000000000193345 ) ) ;
#13306=DIRECTION ( 'NONE',  ( 1.000000000000000000, 0.000000000000000000, 0.000000000000000000 ) ) ;
#13310=FACE_OUTER_BOUND ( 'NONE', #8913, .T. ) ;
#13312=EDGE_LOOP ( 'NONE', ( #1753, #9212, #4362, #11071 ) ) ;
#13319=CARTESIAN_POINT ( 'NONE',  ( 8.643737792453333225E-17, -0.5196152422706635798, 0.3779506566538943235 ) ) ;
#13320=CARTESIAN_POINT ( 'NONE',  ( -0.2764156081756484196, 1.692557448933383907E-17, 0.03972222222222369925 ) ) ;
#13327=CARTESIAN_POINT ( 'NONE',  ( 0.3155070326520292290, -0.1306872919485616569, 0.1977083333333359005 ) ) ;
#13328=EDGE_CURVE ( 'NONE', #7496, #19658, #11038, .T. ) ;
#13329=CARTESIAN_POINT ( 'NONE',  ( -0.1650495903302308942, -0.4585922144775718690, 0.07156651416104609087 ) ) ;
#13348=CARTESIAN_POINT ( 'NONE',  ( 0.1458082941847509140, 0.2460910087212031805, 0.3975519585608662254 ) ) ;
#13351=ORIENTED_EDGE ( 'NONE', *, *, #8759, .T. ) ;
#13363=CARTESIAN_POINT ( 'NONE',  ( -0.1954553509668046918, -0.1954553509668046640, 0.4286111111111157168 ) ) ;
#13379=CARTESIAN_POINT ( 'NONE',  ( -0.1306872919485614903, 0.3155070326520293400, 0.4442361111111159389 ) ) ;
#13383=CARTESIAN_POINT ( 'NONE',  ( -0.2764156081756484196, -0.1144950937579609362, 0.3209722222222259891 ) ) ;
#13384=CARTESIAN_POINT ( 'NONE',  ( 0.09134320533036652257, -0.5015400784327699313, 0.06108448616840793377 ) ) ;
#13386=CARTESIAN_POINT ( 'NONE',  ( -0.1954553509668046640, 0.1954553509668046918, 0.3036111111111147176 ) ) ;
#13388=CARTESIAN_POINT ( 'NONE',  ( -0.2764156081756484196, 0.1144950937579609918, -0.1373611111111110172 ) ) ;
#13389=ORIENTED_EDGE ( 'NONE', *, *, #10580, .F. ) ;
#13396=CARTESIAN_POINT ( 'NONE',  ( 0.4679241437345806887, 0.2662683654317170578, 0.05892738626661209178 ) ) ;
#13400=FACE_OUTER_BOUND ( 'NONE', #20874, .T. ) ;
#13405=CARTESIAN_POINT ( 'NONE',  ( -0.2209708691207961373, -0.2209708691207961095, 0.07444444444444638098 ) ) ;
#13406=CARTESIAN_POINT ( 'NONE',  ( 0.1954553509668047195, 0.1954553509668046085, 0.4008333333333377047 ) ) ;
#13415=CARTESIAN_POINT ( 'NONE',  ( 0.6288319206375506676, 7.738357572422988565E-17, 0.004799741732707325965 ) ) ;
#13416=CARTESIAN_POINT ( 'NONE',  ( 0.1144950937579611444, 0.2764156081756483641, 0.1890277777777804036 ) ) ;
#13421=CARTESIAN_POINT ( 'NONE',  ( 0.000000000000000000, 0.3125000000000000000, 0.3313888888888928408 ) ) ;
#13429=ORIENTED_EDGE ( 'NONE', *, *, #9494, .T. ) ;
#13433=CARTESIAN_POINT ( 'NONE',  ( 0.04811092099939980049, 0.5134890241753962137, 0.05816431335571147637 ) ) ;
#13443=CARTESIAN_POINT ( 'NONE',  ( 0.1144950937579611444, 0.2764156081756483641, 0.02236111111111246594 ) ) ;
#13446=ORIENTED_EDGE ( 'NONE', *, *, #23865, .T. ) ;
#13449=DIRECTION ( 'NONE',  ( 0.000000000000000000, 0.000000000000000000, -1.000000000000000000 ) ) ;
#13451=CARTESIAN_POINT ( 'NONE',  ( -0.1306872919485614903, 0.3155070326520293400, 0.2740972222222253785 ) ) ;
#13452=CARTESIAN_POINT ( 'NONE',  ( -0.2022257292156467434, -0.4370114112024232611, 0.07440066028686581623 ) ) ;
#13464=CARTESIAN_POINT ( 'NONE',  ( -0.2209708691207961373, -0.2209708691207961095, 0.2341666666666694929 ) ) ;
#13468=CARTESIAN_POINT ( 'NONE',  ( 0.1898046044843661184, -0.2363956207629887840, -0.09186489914520645783 ) ) ;
#13469=VERTEX_POINT ( 'NONE', #4190 ) ;
#13472=EDGE_LOOP ( 'NONE', ( #18367, #15671, #21970 ) ) ;
#13473=AXIS2_PLACEMENT_3D ( 'NONE', #9332, #14945, #20309 ) ;
#13474=LINE ( 'NONE', #6374, #7044 ) ;
#13481=CARTESIAN_POINT ( 'NONE',  ( 0.4251436100156877895, 0.2958090996783798721, 0.4013701042764563076 ) ) ;
#13488=CARTESIAN_POINT ( 'NONE',  ( 0.000000000000000000, 3.738758431839877614E-19, -0.1016666666666665164 ) ) ;
#13489=CARTESIAN_POINT ( 'NONE',  ( 0.1954553509668046640, -0.1954553509668047195, 0.4425000000000047229 ) ) ;
#13491=CARTESIAN_POINT ( 'NONE',  ( -0.2142276530138171042, -0.4175814842298855023, 0.4181133580835095231 ) ) ;
#13506=CARTESIAN_POINT ( 'NONE',  ( -0.3155070326520293400, -0.1306872919485614626, 0.4025694444444489761 ) ) ;
#13511=CARTESIAN_POINT ( 'NONE',  ( -0.4687500000000003886, -0.2598076211353319009, 0.3779506566538942125 ) ) ;
#13512=FACE_OUTER_BOUND ( 'NONE', #21714, .T. ) ;
#13513=CARTESIAN_POINT ( 'NONE',  ( 0.1954553509668047195, 0.1954553509668046085, 0.2897222222222257115 ) ) ;
#13515=CARTESIAN_POINT ( 'NONE',  ( -3.385114897866767815E-17, -0.2764156081756484196, 0.4425000000000046119 ) ) ;
#13522=EDGE_CURVE ( 'NONE', #10074, #22264, #3889, .T. ) ;
#13524=CARTESIAN_POINT ( 'NONE',  ( 0.4593750000000003664, 0.2760455974562901482, 0.06112444011295366936 ) ) ;
#13536=CARTESIAN_POINT ( 'NONE',  ( -0.1306872919485615459, -0.3155070326520293400, -0.1460416666666664309 ) ) ;
#13544=CARTESIAN_POINT ( 'NONE',  ( -0.2944048850341824952, -0.06890421275380248511, -0.09102616896780499345 ) ) ;
#13545=CARTESIAN_POINT ( 'NONE',  ( 0.1954553509668047195, 0.1954553509668046085, 0.1300000000000021694 ) ) ;
#13549=CARTESIAN_POINT ( 'NONE',  ( -0.3124999999999997224, 0.1294417382415924966, 0.3418055555555596370 ) ) ;
#13555=CARTESIAN_POINT ( 'NONE',  ( -0.3253415854805812857, 3.738758431839877614E-19, -0.1145082521472477743 ) ) ;
#13561=CARTESIAN_POINT ( 'NONE',  ( -0.2998642343065030524, 0.08796414601291394075, -0.1016666666666771329 ) ) ;
#13564=( BOUNDED_CURVE ( )  B_SPLINE_CURVE ( 2, ( #21344, #3279, #974, #17805, #1459, #1337, #2802, #10611, #8766 ),
 .UNSPECIFIED., .F., .F. ) 
 B_SPLINE_CURVE_WITH_KNOTS ( ( 3, 2, 2, 2, 3 ),
 ( 0.06250000000000002776, 0.07291666666666669905, 0.08333333333333335646, 0.09375000000000002776, 0.1041666666666666990 ),
 .UNSPECIFIED. ) 
 CURVE ( )  GEOMETRIC_REPRESENTATION_ITEM ( )  RATIONAL_B_SPLINE_CURVE ( ( 0.9999999999999997780, 0.9238795325112869605, 1.000000000000000000, 0.9238795325112867385, 1.000000000000000000, 0.9238795325112867385, 1.000000000000000000, 0.9238795325112865164, 1.000000000000000222 ) ) 
 REPRESENTATION_ITEM ( '' )  );
#13576=CARTESIAN_POINT ( 'NONE',  ( -3.863846776457871776E-17, -0.3155070326520292845, 0.1872916666666691043 ) ) ;
#13587=EDGE_LOOP ( 'NONE', ( #9826, #19205, #12600, #12637, #6888, #2153, #9373 ) ) ;
#13590=CARTESIAN_POINT ( 'NONE',  ( -0.1578986201652095300, 0.4501030665082202953, 0.4142710792078266313 ) ) ;
#13600=CARTESIAN_POINT ( 'NONE',  ( 0.2725502669324571525, 0.3839089073841462363, 0.4290249205314688452 ) ) ;
#13606=DIRECTION ( 'NONE',  ( -0.000000000000000000, 0.000000000000000000, -1.000000000000000000 ) ) ;
#13623=CARTESIAN_POINT ( 'NONE',  ( 0.01848103877824584448, 0.5441716683897389606, 0.04413116910601658227 ) ) ;
#13627=CARTESIAN_POINT ( 'NONE',  ( 0.3125000000000000000, -5.740531871003217465E-17, 0.2619444444444478659 ) ) ;
#13628=DIRECTION ( 'NONE',  ( -0.8660254037844397068, -1.060575238724908024E-16, -0.4999999999999979461 ) ) ;
#13629=CARTESIAN_POINT ( 'NONE',  ( -0.2764156081756484196, 1.692557448933383907E-17, 0.1994444444444472553 ) ) ;
#13631=CARTESIAN_POINT ( 'NONE',  ( -0.2764156081756484196, -0.1144950937579609362, 0.3765277777777819579 ) ) ;
#13634=CARTESIAN_POINT ( 'NONE',  ( 0.01848103877824608041, -0.5441716683897390716, 0.04413116910601659615 ) ) ;
#13643=DIRECTION ( 'NONE',  ( 0.000000000000000000, 0.000000000000000000, 1.000000000000000000 ) ) ;
#13644=AXIS2_PLACEMENT_3D ( 'NONE', #18830, #19185, #5898 ) ;
#13645=ORIENTED_EDGE ( 'NONE', *, *, #20732, .T. ) ;
#13650=DIRECTION ( 'NONE',  ( 0.000000000000000000, 1.000000000000000000, 0.000000000000000000 ) ) ;
#13651=EDGE_CURVE ( 'NONE', #17792, #13125, #17162, .T. ) ;
#13652=CARTESIAN_POINT ( 'NONE',  ( -0.1954553509668046918, -0.1954553509668046640, 0.4286111111111157168 ) ) ;
#13663=CARTESIAN_POINT ( 'NONE',  ( 0.2764156081756484196, -5.077672346800151106E-17, 0.2341666666666696595 ) ) ;
#13664=ADVANCED_FACE ( 'NONE', ( #21316 ), #1068, .T. ) ;
#13677=CARTESIAN_POINT ( 'NONE',  ( -0.4739766090219371120, -0.2774257203002796213, 0.04193793378272819145 ) ) ;
#13687=DIRECTION ( 'NONE',  ( 0.000000000000000000, 0.000000000000000000, -1.000000000000000000 ) ) ;
#13688=DIRECTION ( 'NONE',  ( 0.8320502943378439431, -0.4803844614152621428, -0.2773500981126125753 ) ) ;
#13693=CARTESIAN_POINT ( 'NONE',  ( -0.3155070326520293400, -0.1306872919485614626, 0.2324305555555583602 ) ) ;
#13717=CARTESIAN_POINT ( 'NONE',  ( 0.4622078388679875527, 0.2744100571732868143, 0.3892820121258429023 ) ) ;
#13729=ORIENTED_EDGE ( 'NONE', *, *, #18869, .T. ) ;
#13736=CARTESIAN_POINT ( 'NONE',  ( -0.2694453590030796430, -0.3748737188716306790, 0.4343212420608418278 ) ) ;
#13743=CARTESIAN_POINT ( 'NONE',  ( -0.1954553509668046918, -0.1954553509668046640, 0.1508333333333357063 ) ) ;
#13745=CARTESIAN_POINT ( 'NONE',  ( 0.1144950937579611444, 0.2764156081756483641, 0.4668055555555604141 ) ) ;
#13757=ORIENTED_EDGE ( 'NONE', *, *, #165, .F. ) ;
#13763=FACE_OUTER_BOUND ( 'NONE', #11278, .T. ) ;
#13764=CARTESIAN_POINT ( 'NONE',  ( -0.3155070326520293400, -0.1306872919485614626, 0.1247916666666690211 ) ) ;
#13770=PLANE ( 'NONE',  #7431 ) ;
#13775=CARTESIAN_POINT ( 'NONE',  ( -0.1294417382415922191, 0.3125000000000000000, 0.3348611111111151617 ) ) ;
#13780=CARTESIAN_POINT ( 'NONE',  ( 0.009375000000000067307, -0.5358532185916218271, 0.06112444011295370405 ) ) ;
#13791=CARTESIAN_POINT ( 'NONE',  ( -0.4800180268475474632, 0.1716606712744873642, 0.06108529706132549003 ) ) ;
#13797=CARTESIAN_POINT ( 'NONE',  ( 0.1144950937579611444, 0.2764156081756483641, 0.3001388888888924522 ) ) ;
#13802=CARTESIAN_POINT ( 'NONE',  ( -0.3155070326520292845, 1.931923388228935888E-17, 0.1734027777777800983 ) ) ;
#13811=ORIENTED_EDGE ( 'NONE', *, *, #15304, .T. ) ;
#13814=CARTESIAN_POINT ( 'NONE',  ( -0.1294417382415922191, 0.3125000000000000000, 0.3904166666666711860 ) ) ;
#13816=VECTOR ( 'NONE', #10519, 39.37007874015748143 ) ;
#13822=CARTESIAN_POINT ( 'NONE',  ( 0.2437787738197950693, 0.1452258864492554369, 0.3947958900003602500 ) ) ;
#13826=ORIENTED_EDGE ( 'NONE', *, *, #5352, .F. ) ;
#13829=DIRECTION ( 'NONE',  ( 1.000000000000000000, 0.000000000000000000, 0.000000000000000000 ) ) ;
#13836=( BOUNDED_CURVE ( )  B_SPLINE_CURVE ( 2, ( #4746, #1220, #6950, #12217, #6701, #6825, #21345, #8404, #8288 ),
 .UNSPECIFIED., .F., .F. ) 
 B_SPLINE_CURVE_WITH_KNOTS ( ( 3, 2, 2, 2, 3 ),
 ( 0.6041666666666667407, 0.6145833333333334814, 0.6250000000000000000, 0.6354166666666666297, 0.6458333333333333703 ),
 .UNSPECIFIED. ) 
 CURVE ( )  GEOMETRIC_REPRESENTATION_ITEM ( )  RATIONAL_B_SPLINE_CURVE ( ( 0.9999999999999992228, 0.9238795325112875156, 1.000000000000000000, 0.9238795325112867385, 1.000000000000000000, 0.9238795325112867385, 1.000000000000000000, 0.9238795325112867385, 1.000000000000000000 ) ) 
 REPRESENTATION_ITEM ( '' )  );
#13848=VECTOR ( 'NONE', #16337, 39.37007874015748854 ) ;
#13852=CARTESIAN_POINT ( 'NONE',  ( -0.1916493530484528196, -0.4197546306156789697, 0.4334994210334168208 ) ) ;
#13857=CARTESIAN_POINT ( 'NONE',  ( -0.2195630361087207438, -0.1679215936615484350, -0.06558227484231504700 ) ) ;
#13859=CARTESIAN_POINT ( 'NONE',  ( -0.3125000000000000555, 1.913510623667739771E-17, 0.2897222222222258226 ) ) ;
#13861=DIRECTION ( 'NONE',  ( -0.000000000000000000, -0.000000000000000000, -1.000000000000000000 ) ) ;
#13863=CARTESIAN_POINT ( 'NONE',  ( -0.1144950937579609779, 0.2764156081756484196, 0.07791666666666847985 ) ) ;
#13868=CARTESIAN_POINT ( 'NONE',  ( -0.2802773643484119392, 0.009513829220699217271, -0.06944403101507866383 ) ) ;
#13871=SPHERICAL_SURFACE ( 'NONE', #19747, 0.01874999999999999931 ) ;
#13877=EDGE_LOOP ( 'NONE', ( #11184, #7143, #17492, #12561 ) ) ;
#13884=CARTESIAN_POINT ( 'NONE',  ( 0.1306872919485616846, 0.3155070326520292290, -0.06270833333333244997 ) ) ;
#13885=CARTESIAN_POINT ( 'NONE',  ( -0.009374999999999905978, -0.5358532185916218271, 0.06112444011295371793 ) ) ;
#13889=CARTESIAN_POINT ( 'NONE',  ( -0.2764156081756484196, 0.1144950937579609918, 0.09180555555555744429 ) ) ;
#13906=CARTESIAN_POINT ( 'NONE',  ( 0.3125000000000009437, 0.1294417382415912476, 0.09875000000000208611 ) ) ;
#13912=CARTESIAN_POINT ( 'NONE',  ( -0.2764156081756484196, 0.1144950937579609918, -0.08180555555555503455 ) ) ;
#13917=CARTESIAN_POINT ( 'NONE',  ( -0.3308333333333332571, 4.088927411497558688E-17, 0.4425000000000000044 ) ) ;
#13918=CARTESIAN_POINT ( 'NONE',  ( -0.2764156081756484196, 1.692557448933383907E-17, 0.3175000000000036682 ) ) ;
#13919=CARTESIAN_POINT ( 'NONE',  ( -0.1294417382415922746, -0.3125000000000000000, 0.3556944444444486986 ) ) ;
#13922=CARTESIAN_POINT ( 'NONE',  ( -0.08367472778091829266, 0.4929562507565926621, 0.07813238993955247402 ) ) ;
#13924=CARTESIAN_POINT ( 'NONE',  ( -0.2230971623002954152, -0.2230971623002953874, 0.4025694444444485876 ) ) ;
#13926=CARTESIAN_POINT ( 'NONE',  ( -0.4593750000000004219, -0.2760455974562901482, 0.3779506566538942125 ) ) ;
#13931=EDGE_CURVE ( 'NONE', #19658, #3680, #18028, .T. ) ;
#13939=DIRECTION ( 'NONE',  ( 0.000000000000000000, 0.000000000000000000, -1.000000000000000000 ) ) ;
#13949=ORIENTED_EDGE ( 'NONE', *, *, #2887, .F. ) ;
#13955=CARTESIAN_POINT ( 'NONE',  ( -0.4687500000000003886, -0.2598076211353319009, 0.4425000000000000044 ) ) ;
#13974=CARTESIAN_POINT ( 'NONE',  ( -0.4592086519660381616, -0.09034263136374838521, 0.4297010434978499327 ) ) ;
#13976=( BOUNDED_SURFACE ( )  B_SPLINE_SURFACE ( 3, 2, ( 
 ( #8107, #6045, #20687 ),
 ( #9595, #2282, #2637 ),
 ( #15204, #9841, #4336 ),
 ( #20926, #2402, #11787 ),
 ( #19212, #19096, #17391 ),
 ( #3979, #7874, #15090 ),
 ( #4456, #4219, #11430 ),
 ( #13384, #17153, #20807 ),
 ( #684, #15562, #22513 ),
 ( #17273, #11673, #22984 ) ),
 .UNSPECIFIED., .F., .F., .T. ) 
 B_SPLINE_SURFACE_WITH_KNOTS ( ( 4, 2, 2, 2, 4 ),
 ( 3, 3 ),
 ( 0.04463809143445898742, 0.04796255359614957914, 0.05128701575784017086, 0.05461147791953076258, 0.05793594008122136124 ),
 ( 0.000000000000000000, 1.000000000000000000 ),
 .UNSPECIFIED. ) 
 GEOMETRIC_REPRESENTATION_ITEM ( )  RATIONAL_B_SPLINE_SURFACE ( (
 ( 1.000000000000000000, 0.8285407536241361504, 1.000000000000000000),
 ( 1.000000000000000000, 0.8326168960428316224, 1.000000000000000000),
 ( 1.000000000000000000, 0.8363786027323955041, 1.000000000000000000),
 ( 1.000000000000000000, 0.8417912930207277489, 1.000000000000000000),
 ( 1.000000000000000000, 0.8433923807913777937, 1.000000000000000000),
 ( 1.000000000000000000, 0.8433905099820321327, 1.000000000000000000),
 ( 1.000000000000000000, 0.8417888685867314091, 1.000000000000000000),
 ( 1.000000000000000000, 0.8363766775004335408, 1.000000000000000000),
 ( 1.000000000000000000, 0.8326159398059326255, 1.000000000000000000),
 ( 1.000000000000000000, 0.8285407536241353732, 1.000000000000000000) ) ) 
 REPRESENTATION_ITEM ( '' )  SURFACE ( )  );
#13982=CARTESIAN_POINT ( 'NONE',  ( -0.2764156081756484196, 1.692557448933383907E-17, -0.02277777777777679341 ) ) ;
#13988=CARTESIAN_POINT ( 'NONE',  ( -0.1294417382415922746, -0.3125000000000000000, -0.04013888888888822448 ) ) ;
#13992=DIRECTION ( 'NONE',  ( 0.000000000000000000, 0.000000000000000000, -1.000000000000000000 ) ) ;
#13993=EDGE_LOOP ( 'NONE', ( #19084, #22453, #16034, #16558 ) ) ;
#13996=CARTESIAN_POINT ( 'NONE',  ( 0.4687500000000003886, -0.2598076211353317344, 0.06112444011295375262 ) ) ;
#13997=CARTESIAN_POINT ( 'NONE',  ( 0.3155070326520292845, -5.795770164686806123E-17, 0.09354166666666878516 ) ) ;
#13998=CARTESIAN_POINT ( 'NONE',  ( 0.2022257292156428021, 0.4370114112024169328, 0.07440066028686925792 ) ) ;
#14002=CARTESIAN_POINT ( 'NONE',  ( -0.1954553509668046640, 0.1954553509668046918, -0.07833333333333279691 ) ) ;
#14003=CARTESIAN_POINT ( 'NONE',  ( -0.3125000000000000000, 1.913510623667739771E-17, -0.04361111111111011518 ) ) ;
#14004=CARTESIAN_POINT ( 'NONE',  ( -3.827021247335479543E-17, -0.3125000000000000000, 0.07444444444444603404 ) ) ;
#14005=CARTESIAN_POINT ( 'NONE',  ( -0.1144950937579609779, 0.2764156081756484196, 0.4737500000000048894 ) ) ;
#14017=CARTESIAN_POINT ( 'NONE',  ( -0.2727340197566736069, 0.3838028176415902437, 0.4171892680188218905 ) ) ;
#14019=ORIENTED_EDGE ( 'NONE', *, *, #20031, .T. ) ;
#14027=CARTESIAN_POINT ( 'NONE',  ( -0.4796774085936771903, 0.08639205856936141292, 0.07156340032552072072 ) ) ;
#14028=CARTESIAN_POINT ( 'NONE',  ( -0.2764156081756484196, 1.692557448933383907E-17, -0.02277777777777679341 ) ) ;
#14033=CARTESIAN_POINT ( 'NONE',  ( 0.1954553509668047195, 0.1954553509668046085, 0.1300000000000021694 ) ) ;
#14036=CARTESIAN_POINT ( 'NONE',  ( 0.4805070082343983473, 0.2560807851245831546, 0.04413116910601659615 ) ) ;
#14040=CARTESIAN_POINT ( 'NONE',  ( -0.1306872919485614903, 0.3155070326520293400, 0.4963194444444493092 ) ) ;
#14041=CARTESIAN_POINT ( 'NONE',  ( -0.3125000000000000000, 1.913510623667739771E-17, 0.06055555555555702796 ) ) ;
#14043=CARTESIAN_POINT ( 'NONE',  ( -0.2209708691207961373, -0.2209708691207961095, 0.01194444444444552056 ) ) ;
#14050=VECTOR ( 'NONE', #13449, 39.37007874015748143 ) ;
#14055=ADVANCED_FACE ( 'NONE', ( #8543 ), #18963, .T. ) ;
#14067=CARTESIAN_POINT ( 'NONE',  ( -0.6391249999999999432, 3.738758431839877614E-19, 0.000000000000000000 ) ) ;
#14080=ORIENTED_EDGE ( 'NONE', *, *, #562, .F. ) ;
#14088=CARTESIAN_POINT ( 'NONE',  ( 0.000000000000000000, 0.000000000000000000, 1.326383476483184332 ) ) ;
#14092=CARTESIAN_POINT ( 'NONE',  ( -0.4584471372235523479, -0.2219236676878912906, 0.4063138784971527251 ) ) ;
#14098=CARTESIAN_POINT ( 'NONE',  ( -0.1954553509668046640, 0.1954553509668046918, -0.02972222222222128257 ) ) ;
#14101=CARTESIAN_POINT ( 'NONE',  ( 0.1976201361917928889, 0.2172293928240130179, -0.08221809433988200300 ) ) ;
#14108=EDGE_CURVE ( 'NONE', #13469, #5331, #9029, .T. ) ;
#14112=CARTESIAN_POINT ( 'NONE',  ( -0.4500000000000003997, 0.2598076211353315124, 0.3779506566538943790 ) ) ;
#14113=CARTESIAN_POINT ( 'NONE',  ( -0.2230971623002954152, -0.2230971623002953874, -0.03840277777777671014 ) ) ;
#14114=DIRECTION ( 'NONE',  ( 0.000000000000000000, 0.000000000000000000, 1.000000000000000000 ) ) ;
#14120=CARTESIAN_POINT ( 'NONE',  ( 0.1144950937579609085, -0.2764156081756484751, -0.05402777777777704321 ) ) ;
#14123=CARTESIAN_POINT ( 'NONE',  ( 0.1954553509668047195, 0.1954553509668046085, 0.3522222222222262111 ) ) ;
#14133=CARTESIAN_POINT ( 'NONE',  ( -0.1959149649064394760, 0.4281543196382655569, 0.4181366382341982213 ) ) ;
#14135=CARTESIAN_POINT ( 'NONE',  ( 0.000000000000000000, 0.3125000000000000000, 0.1091666666666688823 ) ) ;
#14141=CARTESIAN_POINT ( 'NONE',  ( -0.4687500000000003331, -0.04362952321592657862, 0.07944747088523676504 ) ) ;
#14142=CARTESIAN_POINT ( 'NONE',  ( -0.2764156081756484196, -0.1144950937579609362, -0.07486111111111054539 ) ) ;
#14147=CARTESIAN_POINT ( 'NONE',  ( -0.1954553509668046918, -0.1954553509668046640, 0.2688888888888921747 ) ) ;
#14150=CARTESIAN_POINT ( 'NONE',  ( -0.2573004767273367466, 0.1442547113246396839, 0.4064935863995496335 ) ) ;
#14152=CARTESIAN_POINT ( 'NONE',  ( -0.1586325827338088967, 0.4496793130216642509, 0.08858683671056809261 ) ) ;
#14153=CARTESIAN_POINT ( 'NONE',  ( -0.1954553509668046918, -0.1954553509668046640, 0.03972222222222369925 ) ) ;
#14154=CARTESIAN_POINT ( 'NONE',  ( 0.3155070326520292290, 0.1306872919485615736, 0.4268750000000043898 ) ) ;
#14155=AXIS2_PLACEMENT_3D ( 'NONE', #23028, #11966, #8154 ) ;
#14168=CARTESIAN_POINT ( 'NONE',  ( -0.2209708691207961095, 0.2209708691207961373, 0.3938888888888933404 ) ) ;
#14172=AXIS2_PLACEMENT_3D ( 'NONE', #3562, #3203, #3092 ) ;
#14178=ORIENTED_EDGE ( 'NONE', *, *, #22086, .T. ) ;
#14182=DIRECTION ( 'NONE',  ( -0.9063077870366478273, 0.000000000000000000, -0.4226182617407038267 ) ) ;
#14186=EDGE_CURVE ( 'NONE', #17972, #5886, #9789, .T. ) ;
#14189=CARTESIAN_POINT ( 'NONE',  ( -0.05482473137696326770, -0.5228958406531273306, 0.05347130368200832956 ) ) ;
#14204=EDGE_LOOP ( 'NONE', ( #15290, #96 ) ) ;
#14206=AXIS2_PLACEMENT_3D ( 'NONE', #5559, #3737, #16545 ) ;
#14207=CARTESIAN_POINT ( 'NONE',  ( 0.4678785457174672868, 0.2663437566607212981, 0.05892894635879551701 ) ) ;
#14212=CARTESIAN_POINT ( 'NONE',  ( -0.4687500000000003886, -0.08852780644244462316, 0.4134630671871108443 ) ) ;
#14213=VERTEX_POINT ( 'NONE', #11467 ) ;
#14217=CARTESIAN_POINT ( 'NONE',  ( -0.1954553509668046918, -0.1954553509668046640, -0.01583333333333228690 ) ) ;
#14219=CARTESIAN_POINT ( 'NONE',  ( 0.09987075367823565475, 0.2738295200956132880, -0.08002286816158230009 ) ) ;
#14221=CARTESIAN_POINT ( 'NONE',  ( 0.3125000000000000000, -5.740531871003217465E-17, -0.02277777777777697382 ) ) ;
#14224=CARTESIAN_POINT ( 'NONE',  ( 0.3124999999999989453, 0.1294417382415933571, 0.1473611111111133576 ) ) ;
#14226=ADVANCED_FACE ( 'NONE', ( #8146 ), #8182, .F. ) ;
#14228=CARTESIAN_POINT ( 'NONE',  ( -0.3125000000000010547, 0.1294417382415911921, 0.2237500000000028078 ) ) ;
#14230=CARTESIAN_POINT ( 'NONE',  ( 0.3125000000000004996, 0.1294417382415917750, 0.2098611111111141347 ) ) ;
#14231=CARTESIAN_POINT ( 'NONE',  ( 0.3155070326520292290, -0.1306872919485616569, -0.02104166666666545948 ) ) ;
#14233=AXIS2_PLACEMENT_3D ( 'NONE', #17875, #13861, #23336 ) ;
#14240=CARTESIAN_POINT ( 'NONE',  ( 0.1144950937579609085, -0.2764156081756484751, 0.001527777777778949230 ) ) ;
#14241=CARTESIAN_POINT ( 'NONE',  ( 0.4801334617939588822, -0.2624565244266456876, 0.04287645741408795813 ) ) ;
#14243=CARTESIAN_POINT ( 'NONE',  ( 0.2764156081756483641, -0.1144950937579611167, 0.3973611111111153837 ) ) ;
#14255=ORIENTED_EDGE ( 'NONE', *, *, #7472, .F. ) ;
#14256=CIRCLE ( 'NONE', #3354, 0.01874999999999999237 ) ;
#14259=CARTESIAN_POINT ( 'NONE',  ( 0.2658399375774659346, -0.1645562284175245416, 0.4238565772525364483 ) ) ;
#14260=CARTESIAN_POINT ( 'NONE',  ( 0.4620775622572421693, -0.2744852724095710461, 0.05975564523638850906 ) ) ;
#14263=CARTESIAN_POINT ( 'NONE',  ( 0.2764156081756483641, 0.1144950937579610056, 0.008472222222223456389 ) ) ;
#14267=CARTESIAN_POINT ( 'NONE',  ( 0.2764156081756483641, -0.1144950937579611028, 0.2862500000000034461 ) ) ;
#14269=VECTOR ( 'NONE', #19235, 39.37007874015748143 ) ;
#14271=FACE_OUTER_BOUND ( 'NONE', #17955, .T. ) ;
#14274=CARTESIAN_POINT ( 'NONE',  ( -0.1954553509668046640, 0.1954553509668046918, -0.02972222222222128257 ) ) ;
#14275=CARTESIAN_POINT ( 'NONE',  ( 0.2230971623002954429, 0.2230971623002953319, 0.4303472222222265997 ) ) ;
#14278=CARTESIAN_POINT ( 'NONE',  ( 0.3125000000000007772, -0.1294417382415915807, 0.02930555555555680591 ) ) ;
#14282=ADVANCED_FACE ( 'NONE', ( #19248 ), #791, .F. ) ;
#14318=CARTESIAN_POINT ( 'NONE',  ( -0.4675613926561249523, -0.2849392891917814086, 0.04271845132551763818 ) ) ;
#14329=CARTESIAN_POINT ( 'NONE',  ( -0.3124999999999993894, -0.1294417382415926909, 0.2376388888888920914 ) ) ;
#14334=CARTESIAN_POINT ( 'NONE',  ( 0.2209708691207961095, -0.2209708691207961651, -0.08527777777777745261 ) ) ;
#14339=CARTESIAN_POINT ( 'NONE',  ( 0.2764156081756483641, 0.1144950937579610056, 0.008472222222223456389 ) ) ;
#14341=CARTESIAN_POINT ( 'NONE',  ( 0.2973707438694047078, 0.01885122216165743478, -0.08653741053607123812 ) ) ;
#14347=ADVANCED_BREP_SHAPE_REPRESENTATION ( '', ( #17608, #9127 ), #20827 ) ;
#14353=CARTESIAN_POINT ( 'NONE',  ( 0.2230971623002954429, 0.2230971623002953319, 0.1560416666666692986 ) ) ;
#14356=DIRECTION ( 'NONE',  ( -0.000000000000000000, -0.000000000000000000, 1.000000000000000000 ) ) ;
#14360=CARTESIAN_POINT ( 'NONE',  ( 0.1954553509668047195, 0.1954553509668046085, 0.01888888888889020401 ) ) ;
#14363=ORIENTED_EDGE ( 'NONE', *, *, #9382, .F. ) ;
#14369=B_SPLINE_CURVE_WITH_KNOTS ( 'NONE', 3,
 ( #12710, #18176, #10745, #20005, #3416, #23642, #18295, #8779, #21715, #23520 ),
 .UNSPECIFIED., .F., .F.,
 ( 4, 2, 2, 2, 4 ),
 ( 0.000000000000000000, 0.003270554913819859796, 0.006541109827639719591, 0.009811664741459578953, 0.01308221965527943918 ),
 .UNSPECIFIED. ) ;
#14373=CARTESIAN_POINT ( 'NONE',  ( 0.004187250022457379706, 0.5383673285787200502, 0.04698409998689229844 ) ) ;
#14385=CARTESIAN_POINT ( 'NONE',  ( -0.1954553509668046918, -0.1954553509668046640, -0.07138888888888827999 ) ) ;
#14395=CARTESIAN_POINT ( 'NONE',  ( 0.4802534502443344122, 0.2139688138246751414, 0.05347119198895301101 ) ) ;
#14398=CARTESIAN_POINT ( 'NONE',  ( 0.2764156081756483641, 0.1144950937579610195, -0.04708333333333253323 ) ) ;
#14399=CARTESIAN_POINT ( 'NONE',  ( -0.1306872919485615459, -0.3155070326520293400, 0.4615972222222268218 ) ) ;
#14401=EDGE_LOOP ( 'NONE', ( #12875, #19066, #16349, #1028 ) ) ;
#14416=CARTESIAN_POINT ( 'NONE',  ( -0.4687500000000003886, 0.2598076211353315124, 0.4425000000000000044 ) ) ;
#14418=LINE ( 'NONE', #5377, #4517 ) ;
#14424=CARTESIAN_POINT ( 'NONE',  ( -0.01848103877824625041, 0.5441716683897389606, 0.04413116910601661003 ) ) ;
#14436=CIRCLE ( 'NONE', #7034, 0.01874999999999999237 ) ;
#14443=CARTESIAN_POINT ( 'NONE',  ( -0.4607735603406451497, -0.2757708160732098568, 0.04763592618481097413 ) ) ;
#14449=EDGE_LOOP ( 'NONE', ( #9026, #7303, #10826, #18490 ) ) ;
#14462=CARTESIAN_POINT ( 'NONE',  ( -0.2209708691207961373, -0.2209708691207961095, -0.09916666666666647256 ) ) ;
#14465=FACE_OUTER_BOUND ( 'NONE', #21585, .T. ) ;
#14467=CARTESIAN_POINT ( 'NONE',  ( -0.1954553509668046918, -0.1954553509668046640, 0.3730555555555596925 ) ) ;
#14477=PRODUCT_DEFINITION ( 'UNKNOWN', '', #11902, #4601 ) ;
#14479=CARTESIAN_POINT ( 'NONE',  ( 0.1306872919485614071, -0.3155070326520293955, 0.1942361111111139960 ) ) ;
#14481=CARTESIAN_POINT ( 'NONE',  ( 0.2727340197566651137, -0.3838028176415952397, 0.4171892680188027391 ) ) ;
#14484=CARTESIAN_POINT ( 'NONE',  ( 0.000000000000000000, 0.2764156081756484196, 0.2480555555555586933 ) ) ;
#14499=CARTESIAN_POINT ( 'NONE',  ( 0.01848103877826402786, 0.5441716683897283025, 0.04413116910602140480 ) ) ;
#14500=ORIENTED_EDGE ( 'NONE', *, *, #940, .F. ) ;
#14507=CARTESIAN_POINT ( 'NONE',  ( -0.1961415469429297342, -0.1956144934194087859, -0.06558227484231513027 ) ) ;
#14508=CARTESIAN_POINT ( 'NONE',  ( -0.1144950937579609918, -0.2764156081756484196, 0.3209722222222259891 ) ) ;
#14515=CARTESIAN_POINT ( 'NONE',  ( -0.08187103065728323914, 0.2793464338139786673, 0.4021514253947122142 ) ) ;
#14518=CARTESIAN_POINT ( 'NONE',  ( -3.385114897866767815E-17, -0.2764156081756484196, -0.008888888888887782128 ) ) ;
#14519=CARTESIAN_POINT ( 'NONE',  ( -0.1144950937579609918, -0.2764156081756484196, 0.05013888888889045381 ) ) ;
#14525=ADVANCED_FACE ( 'NONE', ( #5458 ), #12924, .F. ) ;
#14532=ORIENTED_EDGE ( 'NONE', *, *, #17117, .F. ) ;
#14549=DIRECTION ( 'NONE',  ( 0.8320502943378439431, -0.4803844614152621428, 0.2773500981126125753 ) ) ;
#14563=CARTESIAN_POINT ( 'NONE',  ( -0.4620259694561524855, 0.2880908832651557505, 0.04413116910601658227 ) ) ;
#14580=AXIS2_PLACEMENT_3D ( 'NONE', #19604, #8505, #15945 ) ;
#14587=CARTESIAN_POINT ( 'NONE',  ( -3.385114897866767815E-17, -0.2764156081756484196, 0.3244444444444482545 ) ) ;
#14590=CARTESIAN_POINT ( 'NONE',  ( -0.1312453311288143964, -0.4543582620183869158, 0.4268234664230690090 ) ) ;
#14591=DIRECTION ( 'NONE',  ( 1.000000000000000000, 0.000000000000000000, -0.000000000000000000 ) ) ;
#14593=EDGE_CURVE ( 'NONE', #19970, #17585, #6344, .T. ) ;
#14601=CARTESIAN_POINT ( 'NONE',  ( 0.000000000000000000, 0.3155070326520292845, 0.2740972222222257670 ) ) ;
#14603=CARTESIAN_POINT ( 'NONE',  ( 0.3880456933851195167, -0.3172275918314949039, 0.4112725064128996966 ) ) ;
#14606=B_SPLINE_CURVE_WITH_KNOTS ( 'NONE', 3,
 ( #13524, #11319, #7653, #13396, #4108, #11568 ),
 .UNSPECIFIED., .F., .F.,
 ( 4, 2, 4 ),
 ( 0.000000000000000000, 0.0002551367231383061714, 0.0005102734462766123427 ),
 .UNSPECIFIED. ) ;
#14608=CARTESIAN_POINT ( 'NONE',  ( -0.2764156081756484196, 0.1144950937579609918, 0.2584722222222254340 ) ) ;
#14610=CARTESIAN_POINT ( 'NONE',  ( -0.4795759075923621273, -5.504308098328212156E-13, 0.07439896364136201756 ) ) ;
#14620=( BOUNDED_SURFACE ( )  B_SPLINE_SURFACE ( 3, 2, ( 
 ( #18680, #16856, #142 ),
 ( #3929, #7585, #7705 ),
 ( #22459, #5758, #2228 ),
 ( #13329, #9537, #15270 ),
 ( #13452, #13219, #11373 ),
 ( #4164, #7348, #16970 ),
 ( #11614, #9175, #14800 ),
 ( #4042, #11495, #22215 ),
 ( #18930, #5515, #12978 ),
 ( #20395, #3686, #18561 ) ),
 .UNSPECIFIED., .F., .F., .T. ) 
 B_SPLINE_SURFACE_WITH_KNOTS ( ( 4, 2, 2, 2, 4 ),
 ( 3, 3 ),
 ( 0.04463809143445898742, 0.04796255359614957914, 0.05128701575784017780, 0.05461147791953077646, 0.05793594008122136818 ),
 ( 0.000000000000000000, 1.000000000000000000 ),
 .UNSPECIFIED. ) 
 GEOMETRIC_REPRESENTATION_ITEM ( )  RATIONAL_B_SPLINE_SURFACE ( (
 ( 1.000000000000000000, 0.8285407536241353732, 1.000000000000000000),
 ( 1.000000000000000000, 0.8326168960428802501, 1.000000000000000000),
 ( 1.000000000000000000, 0.8363786027323344419, 1.000000000000000000),
 ( 1.000000000000000000, 0.8417912930207894773, 1.000000000000000000),
 ( 1.000000000000000000, 0.8433923807920618021, 1.000000000000000000),
 ( 1.000000000000000000, 0.8433905099813472361, 1.000000000000000000),
 ( 1.000000000000000000, 0.8417888685871616206, 1.000000000000000000),
 ( 1.000000000000000000, 0.8363766775000033293, 1.000000000000000000),
 ( 1.000000000000000000, 0.8326159398062557004, 1.000000000000000000),
 ( 1.000000000000000000, 0.8285407536241354842, 1.000000000000000000) ) ) 
 REPRESENTATION_ITEM ( '' )  SURFACE ( )  );
#14631=CARTESIAN_POINT ( 'NONE',  ( -0.2764156081756484196, 0.1144950937579609918, 0.1404166666666689656 ) ) ;
#14633=CARTESIAN_POINT ( 'NONE',  ( 0.4719654084974829189, 0.2800274776536548771, 0.04212966708837325575 ) ) ;
#14634=CARTESIAN_POINT ( 'NONE',  ( 0.3104386443325673484, 0.3620340424930042489, 0.08855526556984563702 ) ) ;
#14643=CARTESIAN_POINT ( 'NONE',  ( -0.1144950937579609779, 0.2764156081756484196, -0.1373611111111110450 ) ) ;
#14645=ORIENTED_EDGE ( 'NONE', *, *, #9464, .F. ) ;
#14666=EDGE_CURVE ( 'NONE', #20003, #11169, #2760, .T. ) ;
#14668=CARTESIAN_POINT ( 'NONE',  ( -0.4675595609217420567, 0.2849403337939152570, 0.04271891838947983189 ) ) ;
#14669=CARTESIAN_POINT ( 'NONE',  ( -0.4593750000000004219, -0.2760455974562901482, 0.06112444011295364160 ) ) ;
#14677=CARTESIAN_POINT ( 'NONE',  ( 0.1306872919485616846, 0.3155070326520292290, -0.01062499999999911779 ) ) ;
#14678=EDGE_CURVE ( 'NONE', #9027, #7279, #5075, .T. ) ;
#14679=DIRECTION ( 'NONE',  ( 0.000000000000000000, -0.2142211582677940040, 0.9767851838303059919 ) ) ;
#14698=VERTEX_POINT ( 'NONE', #520 ) ;
#14709=DIRECTION ( 'NONE',  ( 0.000000000000000000, 0.000000000000000000, 1.000000000000000000 ) ) ;
#14715=CARTESIAN_POINT ( 'NONE',  ( 0.2764156081756484196, -5.077672346800151106E-17, 0.3383333333333372051 ) ) ;
#14718=CARTESIAN_POINT ( 'NONE',  ( -0.4687500000000003886, 0.2598076211353315124, 0.06112444011295379426 ) ) ;
#14727=CARTESIAN_POINT ( 'NONE',  ( 0.2562433651785209210, -0.1785792061920698504, 0.4235489577189899268 ) ) ;
#14730=CARTESIAN_POINT ( 'NONE',  ( 0.3155070326520292290, 0.1306872919485615736, 0.2636805555555590264 ) ) ;
#14732=CARTESIAN_POINT ( 'NONE',  ( 0.4228029066818827508, -0.2971605053783332728, 0.3901413544831415781 ) ) ;
#14738=CARTESIAN_POINT ( 'NONE',  ( 0.2764156081756483641, 0.1144950937579610056, 0.2931944444444479214 ) ) ;
#14741=ORIENTED_EDGE ( 'NONE', *, *, #10536, .F. ) ;
#14746=CARTESIAN_POINT ( 'NONE',  ( -0.4805263112511646284, 0.2592867110628496174, 0.04342012612512790443 ) ) ;
#14751=CARTESIAN_POINT ( 'NONE',  ( 0.009375000000009008072, 0.5358532185916163870, 0.06112444011295854740 ) ) ;
#14753=CARTESIAN_POINT ( 'NONE',  ( 0.003401740878768560843, -0.5383620901250334434, 0.05893285591566548021 ) ) ;
#14757=CARTESIAN_POINT ( 'NONE',  ( -0.09798969090666245774, -0.2586227216849166788, -0.06558227484231510251 ) ) ;
#14758=CARTESIAN_POINT ( 'NONE',  ( -3.385114897866767815E-17, -0.2764156081756484196, 0.1577777777777801815 ) ) ;
#14759=FACE_OUTER_BOUND ( 'NONE', #9435, .T. ) ;
#14765=CARTESIAN_POINT ( 'NONE',  ( 0.4687500000000002776, -0.1725690304443678602, 0.06591562201456047099 ) ) ;
#14768=CARTESIAN_POINT ( 'NONE',  ( -0.1144950937579609918, -0.2764156081756484196, -0.1165277777777775636 ) ) ;
#14770=ORIENTED_EDGE ( 'NONE', *, *, #6726, .F. ) ;
#14776=AXIS2_PLACEMENT_3D ( 'NONE', #18013, #14114, #10345 ) ;
#14799=CARTESIAN_POINT ( 'NONE',  ( 0.3155070326520292290, 0.1306872919485615736, -0.01756944444444362430 ) ) ;
#14800=CARTESIAN_POINT ( 'NONE',  ( -0.3104386443325958256, -0.3620340424929879286, 0.08855526556985501840 ) ) ;
#14818=CARTESIAN_POINT ( 'NONE',  ( 0.09493784612953225233, -0.2937490000082154662, 0.4199197862486553356 ) ) ;
#14834=CARTESIAN_POINT ( 'NONE',  ( -0.1144950937579609918, -0.2764156081756484196, 0.2654166666666700203 ) ) ;
#14837=EDGE_CURVE ( 'NONE', #16949, #17585, #13474, .T. ) ;
#14841=EDGE_CURVE ( 'NONE', #1725, #4460, #7994, .T. ) ;
#14848=EDGE_CURVE ( 'NONE', #2585, #16983, #8838, .T. ) ;
#14851=CARTESIAN_POINT ( 'NONE',  ( 0.2230971623002953874, -0.2230971623002954429, 0.3088194444444482545 ) ) ;
#14853=CARTESIAN_POINT ( 'NONE',  ( 0.1580560128843781220, -0.4500121957794399052, 0.4142946745564982103 ) ) ;
#14855=CYLINDRICAL_SURFACE ( 'NONE', #21925, 0.3125000000000000000 ) ;
#14858=CARTESIAN_POINT ( 'NONE',  ( -0.1954553509668046918, -0.1954553509668046640, 0.2133333333333361503 ) ) ;
#14868=ADVANCED_FACE ( 'NONE', ( #14271 ), #23135, .F. ) ;
#14877=CARTESIAN_POINT ( 'NONE',  ( 0.000000000000000000, 0.2764156081756484196, 0.2411111111111142458 ) ) ;
#14883=CARTESIAN_POINT ( 'NONE',  ( -0.3125000000000000000, 1.913510623667739771E-17, 0.06055555555555702796 ) ) ;
#14884=CARTESIAN_POINT ( 'NONE',  ( 0.2764156081756483641, 0.1144950937579610056, -0.09569444444444405451 ) ) ;
#14902=CARTESIAN_POINT ( 'NONE',  ( -0.4788584550258518369, 0.2689697488930834490, 0.04193801346286365334 ) ) ;
#14907=ORIENTED_EDGE ( 'NONE', *, *, #21071, .T. ) ;
#14912=CARTESIAN_POINT ( 'NONE',  ( -0.3155070326520292845, 1.931923388228935888E-17, 0.006736111111112118993 ) ) ;
#14925=CARTESIAN_POINT ( 'NONE',  ( -0.4224880990050804974, 0.2973422596752779423, 0.07046568677125501778 ) ) ;
#14930=CARTESIAN_POINT ( 'NONE',  ( 0.2879402880768414108, -0.08326397218404227307, -0.08843619990776636908 ) ) ;
#14936=ORIENTED_EDGE ( 'NONE', *, *, #6901, .T. ) ;
#14938=CARTESIAN_POINT ( 'NONE',  ( 0.1294417382415921358, -0.3125000000000002220, 0.1959722222222251287 ) ) ;
#14945=DIRECTION ( 'NONE',  ( -1.000000000000000000, 0.000000000000000000, 0.000000000000000000 ) ) ;
#14946=CARTESIAN_POINT ( 'NONE',  ( -0.1144950937579609779, 0.2764156081756484196, 0.2445833333333364834 ) ) ;
#14952=CARTESIAN_POINT ( 'NONE',  ( 0.3050515993604266951, -0.01759458571372691030, 0.4170999431000476099 ) ) ;
#14969=VERTEX_POINT ( 'NONE', #18288 ) ;
#14970=CARTESIAN_POINT ( 'NONE',  ( 0.2764156081756483641, 0.1144950937579610195, 0.008472222222223454655 ) ) ;
#14972=CARTESIAN_POINT ( 'NONE',  ( 0.2764156081756483641, -0.1144950937579611167, 0.2862500000000034461 ) ) ;
#14977=CARTESIAN_POINT ( 'NONE',  ( -0.4592333586340865414, 0.08963635625773219706, 0.4305718605174581048 ) ) ;
#14980=CARTESIAN_POINT ( 'NONE',  ( 0.2386280844052624528, -0.1440056533833775076, 0.3886972078529389862 ) ) ;
#14987=ORIENTED_EDGE ( 'NONE', *, *, #2968, .T. ) ;
#14991=EDGE_CURVE ( 'NONE', #13298, #22303, #3859, .T. ) ;
#14993=CARTESIAN_POINT ( 'NONE',  ( -0.1954553509668046640, 0.1954553509668046918, 0.1925000000000027245 ) ) ;
#15001=CARTESIAN_POINT ( 'NONE',  ( 0.000000000000000000, 0.3125000000000000000, 0.1647222222222248789 ) ) ;
#15004=CARTESIAN_POINT ( 'NONE',  ( 0.1954553509668047195, 0.1954553509668046085, -0.03666666666666580643 ) ) ;
#15007=DIRECTION ( 'NONE',  ( 0.000000000000000000, -1.000000000000000000, 0.000000000000000000 ) ) ;
#15015=CARTESIAN_POINT ( 'NONE',  ( 0.000000000000000000, 0.000000000000000000, -0.1019043464467004889 ) ) ;
#15036=CARTESIAN_POINT ( 'NONE',  ( 0.4687500000000003886, 0.2173969584302052338, 0.3901935604185519102 ) ) ;
#15041=ORIENTED_EDGE ( 'NONE', *, *, #8159, .T. ) ;
#15052=CARTESIAN_POINT ( 'NONE',  ( -0.2658399375755275962, -0.1645562284205263071, -0.1013565772524682301 ) ) ;
#15055=CARTESIAN_POINT ( 'NONE',  ( -0.1764095973158986419, -0.2469329051808260012, 0.4146780700801321329 ) ) ;
#15056=CARTESIAN_POINT ( 'NONE',  ( 0.2481776206062809020, -0.3871563449089071018, 0.4344098397133765443 ) ) ;
#15061=ORIENTED_EDGE ( 'NONE', *, *, #21670, .F. ) ;
#15073=CARTESIAN_POINT ( 'NONE',  ( -0.4620259694561524855, -0.2880908832651560281, 0.04413116910601651982 ) ) ;
#15086=CARTESIAN_POINT ( 'NONE',  ( 0.3155070326520292290, 0.1306872919485615736, 0.3747916666666710750 ) ) ;
#15090=CARTESIAN_POINT ( 'NONE',  ( 0.1961225106001930063, -0.4280344930761078581, 0.09139053646024343502 ) ) ;
#15092=CARTESIAN_POINT ( 'NONE',  ( 0.1144950937579609085, -0.2764156081756484751, 0.2723611111111144956 ) ) ;
#15094=CARTESIAN_POINT ( 'NONE',  ( -0.2764156081756484196, -0.1144950937579609362, -0.07486111111111054539 ) ) ;
#15096=CYLINDRICAL_SURFACE ( 'NONE', #3078, 0.3125000000000000000 ) ;
#15108=CARTESIAN_POINT ( 'NONE',  ( -0.4593750000000004219, 0.2760455974562897596, 0.4425000000000000044 ) ) ;
#15114=CARTESIAN_POINT ( 'NONE',  ( -0.1954553509668046918, -0.1954553509668046640, 0.3730555555555596925 ) ) ;
#15117=CYLINDRICAL_SURFACE ( 'NONE', #5833, 0.3125000000000000000 ) ;
#15124=CARTESIAN_POINT ( 'NONE',  ( 0.1954553509668046640, -0.1954553509668047195, 0.1716666666666691599 ) ) ;
#15126=CARTESIAN_POINT ( 'NONE',  ( 0.4687500000000002776, 0.08844770643847373048, 0.4134734246479533359 ) ) ;
#15143=CARTESIAN_POINT ( 'NONE',  ( -0.2764156081756484196, 1.692557448933383907E-17, 0.09527777777777970969 ) ) ;
#15145=VECTOR ( 'NONE', #7377, 39.37007874015748143 ) ;
#15146=VERTEX_POINT ( 'NONE', #23014 ) ;
#15151=CARTESIAN_POINT ( 'NONE',  ( 0.1306872919485616846, 0.3155070326520292290, 0.1560416666666688823 ) ) ;
#15153=CARTESIAN_POINT ( 'NONE',  ( -0.2728104005625175965, -0.05992465826476112839, -0.06807390018913435370 ) ) ;
#15162=CARTESIAN_POINT ( 'NONE',  ( 0.4805070082343983473, -0.2560807851245830435, 0.04413116910601658921 ) ) ;
#15174=EDGE_LOOP ( 'NONE', ( #13241, #7546, #18595, #22506 ) ) ;
#15176=CARTESIAN_POINT ( 'NONE',  ( 0.1893589898698054830, 0.4210708385985185154, 0.4333520680959464522 ) ) ;
#15183=CARTESIAN_POINT ( 'NONE',  ( 0.1954553509668047195, 0.1954553509668046085, 0.4008333333333377047 ) ) ;
#15185=CARTESIAN_POINT ( 'NONE',  ( -0.1557525356064938249, -0.4513421090059194229, 0.4242370903633182477 ) ) ;
#15186=CARTESIAN_POINT ( 'NONE',  ( -0.05485615681475838196, 0.5228774440028900461, 0.05347937985141015815 ) ) ;
#15192=ORIENTED_EDGE ( 'NONE', *, *, #20114, .F. ) ;
#15197=ORIENTED_EDGE ( 'NONE', *, *, #14848, .T. ) ;
#15203=CARTESIAN_POINT ( 'NONE',  ( -3.385114897866767815E-17, -0.2764156081756484196, 0.3313888888888926743 ) ) ;
#15204=CARTESIAN_POINT ( 'NONE',  ( 0.3886563986011730143, -0.3298860868734675433, 0.06108838700205718175 ) ) ;
#15206=CARTESIAN_POINT ( 'NONE',  ( 0.1144950937579611444, 0.2764156081756483641, 0.3487500000000039457 ) ) ;
#15208=CARTESIAN_POINT ( 'NONE',  ( 0.000000000000000000, 0.2764156081756484196, -0.1477777777777777857 ) ) ;
#15210=CARTESIAN_POINT ( 'NONE',  ( -0.008438385721254092545, -0.5369265497013727684, 0.04763613967036315483 ) ) ;
#15212=CARTESIAN_POINT ( 'NONE',  ( -0.2631830812676746456, 0.1021974198356742081, -0.07133656933612833595 ) ) ;
#15213=( BOUNDED_SURFACE ( )  B_SPLINE_SURFACE ( 3, 2, ( 
 ( #6545, #10343, #13996 ),
 ( #21426, #4714, #21543 ),
 ( #19118, #2423, #9864 ),
 ( #17292, #21067, #18343 ),
 ( #20296, #23810, #16873 ),
 ( #12880, #11155, #16402 ) ),
 .UNSPECIFIED., .F., .F., .F. ) 
 B_SPLINE_SURFACE_WITH_KNOTS ( ( 4, 2, 4 ),
 ( 3, 3 ),
 ( 0.001022076388580720786, 0.001521441877679464375, 0.002020807366778207964 ),
 ( 0.000000000000000000, 1.000000000000000000 ),
 .UNSPECIFIED. ) 
 GEOMETRIC_REPRESENTATION_ITEM ( )  RATIONAL_B_SPLINE_SURFACE ( (
 ( 1.000000000000000000, 0.8285407536241365944, 1.000000000000000000),
 ( 1.000000000000000000, 0.8382697314792307841, 1.000000000000000000),
 ( 1.000000000000000000, 0.8433836253084445733, 1.000000000000000000),
 ( 1.000000000000000000, 0.8433992480894338950, 1.000000000000000000),
 ( 1.000000000000000000, 0.8382827608170095868, 1.000000000000000000),
 ( 1.000000000000000000, 0.8285407536241039539, 1.000000000000000000) ) ) 
 REPRESENTATION_ITEM ( '' )  SURFACE ( )  );
#15225=ORIENTED_EDGE ( 'NONE', *, *, #21301, .F. ) ;
#15228=CARTESIAN_POINT ( 'NONE',  ( -0.1964672255785171739, -0.4278354717905788474, 0.4172182224143143880 ) ) ;
#15230=CARTESIAN_POINT ( 'NONE',  ( -0.1954553509668046640, 0.1954553509668046918, 0.4702777777777827350 ) ) ;
#15233=ORIENTED_EDGE ( 'NONE', *, *, #7092, .F. ) ;
#15239=CARTESIAN_POINT ( 'NONE',  ( 0.2764156081756483641, -0.1144950937579611167, 0.1195833333333354426 ) ) ;
#15246=LINE ( 'NONE', #11144, #17179 ) ;
#15248=CARTESIAN_POINT ( 'NONE',  ( 0.2209708691207961095, -0.2209708691207961651, 0.1438888888888913697 ) ) ;
#15250=CARTESIAN_POINT ( 'NONE',  ( 0.05483022876054116646, 0.5228926224321454042, 0.05347271648848982151 ) ) ;
#15255=CARTESIAN_POINT ( 'NONE',  ( 0.2764156081756484196, -5.077672346800151106E-17, -0.1061111111111107813 ) ) ;
#15260=CARTESIAN_POINT ( 'NONE',  ( 0.1954553509668047195, 0.1954553509668046085, 0.01888888888889020401 ) ) ;
#15263=ADVANCED_FACE ( 'NONE', ( #4485 ), #20668, .F. ) ;
#15266=FACE_OUTER_BOUND ( 'NONE', #10276, .T. ) ;
#15267=CARTESIAN_POINT ( 'NONE',  ( -0.2209708691207961373, -0.2209708691207961095, 0.1786111111111135241 ) ) ;
#15269=CARTESIAN_POINT ( 'NONE',  ( 0.3155070326520292290, -0.1306872919485616569, 0.2532638888888918971 ) ) ;
#15270=CARTESIAN_POINT ( 'NONE',  ( -0.1583529533612729467, -0.4498407571151714079, 0.08855978515309881338 ) ) ;
#15280=CARTESIAN_POINT ( 'NONE',  ( -0.05482159418620013297, 0.5228976771666257184, 0.05347049744907691332 ) ) ;
#15286=EDGE_LOOP ( 'NONE', ( #6033, #15640, #21608, #667 ) ) ;
#15290=ORIENTED_EDGE ( 'NONE', *, *, #1692, .T. ) ;
#15292=EDGE_CURVE ( 'NONE', #21037, #19685, #6251, .T. ) ;
#15302=DIRECTION ( 'NONE',  ( 0.000000000000000000, 0.000000000000000000, -1.000000000000000000 ) ) ;
#15304=EDGE_CURVE ( 'NONE', #4460, #12631, #21385, .T. ) ;
#15306=CARTESIAN_POINT ( 'NONE',  ( -0.4224645524279253550, -0.2973558542979372055, 0.3902541392329982317 ) ) ;
#15307=CARTESIAN_POINT ( 'NONE',  ( -0.1653103785569667583, 0.4584405057248003845, 0.07159583130656674288 ) ) ;
#15312=ORIENTED_EDGE ( 'NONE', *, *, #6373, .F. ) ;
#15315=EDGE_CURVE ( 'NONE', #18304, #4025, #17895, .T. ) ;
#15325=CARTESIAN_POINT ( 'NONE',  ( -0.2764156081756484196, 0.1144950937579609918, 0.1404166666666689656 ) ) ;
#15327=CARTESIAN_POINT ( 'NONE',  ( 0.2764156081756483641, -0.1144950937579611167, -0.1095833333333330328 ) ) ;
#15331=CARTESIAN_POINT ( 'NONE',  ( -0.006464354918053499821, -0.5491938321437417336, 0.04193567535760733128 ) ) ;
#15340=CARTESIAN_POINT ( 'NONE',  ( 0.009374999999999772404, 0.5358532185916217161, 0.3779506566538943790 ) ) ;
#15347=CARTESIAN_POINT ( 'NONE',  ( 0.2764156081756483641, -0.1144950937579611167, 0.3904166666666709085 ) ) ;
#15349=EDGE_LOOP ( 'NONE', ( #10281, #10559, #20797, #13949 ) ) ;
#15350=( BOUNDED_CURVE ( )  B_SPLINE_CURVE ( 2, ( #10672, #1402, #8707, #16158, #8830, #6886, #12273, #14329, #23690 ),
 .UNSPECIFIED., .F., .F. ) 
 B_SPLINE_CURVE_WITH_KNOTS ( ( 3, 2, 2, 2, 3 ),
 ( 0.2812500000000000555, 0.2916666666666667407, 0.3020833333333333703, 0.3125000000000000000, 0.3229166666666666852 ),
 .UNSPECIFIED. ) 
 CURVE ( )  GEOMETRIC_REPRESENTATION_ITEM ( )  RATIONAL_B_SPLINE_CURVE ( ( 0.9999999999999995559, 0.9238795325112871826, 1.000000000000000000, 0.9238795325112867385, 1.000000000000000000, 0.9238795325112867385, 1.000000000000000000, 0.9238795325112871826, 0.9999999999999995559 ) ) 
 REPRESENTATION_ITEM ( '' )  );
#15353=CARTESIAN_POINT ( 'NONE',  ( -0.1144950937579609779, 0.2764156081756484196, -0.1373611111111110450 ) ) ;
#15356=CARTESIAN_POINT ( 'NONE',  ( 0.2764156081756483641, -0.1144950937579611167, 0.2306944444444474218 ) ) ;
#15369=VERTEX_POINT ( 'NONE', #11899 ) ;
#15373=ADVANCED_FACE ( 'NONE', ( #19317 ), #2842, .F. ) ;
#15382=CARTESIAN_POINT ( 'NONE',  ( -0.2764156081756484196, 0.1144950937579609918, 0.09180555555555744429 ) ) ;
#15389=CARTESIAN_POINT ( 'NONE',  ( 0.3155070326520292290, 0.1306872919485615736, 0.1490972222222243793 ) ) ;
#15391=CARTESIAN_POINT ( 'NONE',  ( -0.2798077087188347578, -0.01523944824431633545, -0.06897437538550148239 ) ) ;
#15416=CARTESIAN_POINT ( 'NONE',  ( 0.08208976641704460175, 0.4938713286266801505, 0.4000323696459243128 ) ) ;
#15432=ADVANCED_FACE ( 'NONE', ( #10899 ), #17945, .T. ) ;
#15448=CARTESIAN_POINT ( 'NONE',  ( 0.1954553509668046640, -0.1954553509668047195, 0.2758333333333367055 ) ) ;
#15450=CARTESIAN_POINT ( 'NONE',  ( -0.2764156081756484196, -0.1144950937579609362, 0.4320833333333378157 ) ) ;
#15451=ORIENTED_EDGE ( 'NONE', *, *, #19771, .T. ) ;
#15453=CARTESIAN_POINT ( 'NONE',  ( 0.000000000000000000, 0.000000000000000000, 1.326383476483184332 ) ) ;
#15455=CARTESIAN_POINT ( 'NONE',  ( 0.4581189881604794123, -0.2644951211353317455, 0.3941886329748525153 ) ) ;
#15458=CARTESIAN_POINT ( 'NONE',  ( 0.2728104005625097139, -0.05992465826480871532, 0.3905739001891366802 ) ) ;
#15464=LINE ( 'NONE', #15108, #3882 ) ;
#15468=CARTESIAN_POINT ( 'NONE',  ( -0.3155070326520292845, 1.931923388228935888E-17, -0.1009027777777772028 ) ) ;
#15476=DIRECTION ( 'NONE',  ( -0.4999999999999995559, -0.8660254037844389297, 0.000000000000000000 ) ) ;
#15477=CARTESIAN_POINT ( 'NONE',  ( -0.2764156081756484196, 0.1144950937579609918, 0.09180555555555744429 ) ) ;
#15480=DIRECTION ( 'NONE',  ( 1.000000000000000000, 0.000000000000000000, 0.000000000000000000 ) ) ;
#15489=CARTESIAN_POINT ( 'NONE',  ( -0.4805070082343984583, -0.2560807851245831546, 0.04413116910601652676 ) ) ;
#15493=CIRCLE ( 'NONE', #20941, 0.01874999999999999237 ) ;
#15496=CARTESIAN_POINT ( 'NONE',  ( -0.4795758971731803877, -0.04341642064210738533, 0.07439926260594938168 ) ) ;
#15501=CARTESIAN_POINT ( 'NONE',  ( 0.1144950937579611444, 0.2764156081756483641, -0.03319444444444354797 ) ) ;
#15502=CARTESIAN_POINT ( 'NONE',  ( -0.3125000000000000000, 1.913510623667739771E-17, 0.3452777777777818469 ) ) ;
#15507=CARTESIAN_POINT ( 'NONE',  ( -0.2230971623002954152, -0.2230971623002953874, 0.1803472222222246291 ) ) ;
#15509=CARTESIAN_POINT ( 'NONE',  ( -0.1294417382415922191, 0.3125000000000000000, 0.3834722222222263222 ) ) ;
#15512=ORIENTED_EDGE ( 'NONE', *, *, #21873, .T. ) ;
#15522=CARTESIAN_POINT ( 'NONE',  ( 0.3125000000000000000, 3.827021247335477694E-17, 1.326383476483184332 ) ) ;
#15525=CIRCLE ( 'NONE', #23296, 0.6396424860381280109 ) ;
#15529=VERTEX_POINT ( 'NONE', #10784 ) ;
#15532=CARTESIAN_POINT ( 'NONE',  ( 0.2681267372835091090, 0.3756399061183655630, 0.4344383781808607847 ) ) ;
#15554=CARTESIAN_POINT ( 'NONE',  ( -0.3077469291169039889, -0.3525961953783998126, 0.4304954382810342595 ) ) ;
#15558=B_SPLINE_CURVE_WITH_KNOTS ( 'NONE', 3,
 ( #9317, #5414, #12999, #7486, #13119, #18701, #21996, #9072, #16520, #2000, #9437, #7604, #15055, #1755, #4830, #3342, #10798, #9198, #7133, #5295, #23937, #24059, #7368, #14818, #22236, #12782, #2914, #10488, #23501, #1662, #6817, #14727, #14259, #22142 ),
 .UNSPECIFIED., .F., .F.,
 ( 4, 2, 2, 2, 2, 2, 2, 2, 2, 2, 2, 2, 2, 2, 2, 2, 4 ),
 ( 0.02754951627422656119, 0.02882399678901069462, 0.03009847730379482805, 0.03137295781857896149, 0.03264743833336309492, 0.03392191884814722835, 0.03519639936293136179, 0.03647087987771549522, 0.03774536039249962865, 0.03901984090728376209, 0.04029432142206789552, 0.04156880193685202896, 0.04284328245163616239, 0.04411776296642029582, 0.04539224348120442926, 0.04666672399598856269, 0.04794120451077269612 ),
 .UNSPECIFIED. ) ;
#15561=CARTESIAN_POINT ( 'NONE',  ( -0.4687500000000003886, 0.2598076211353315124, 0.3779506566538943790 ) ) ;
#15562=CARTESIAN_POINT ( 'NONE',  ( 0.04810232026109438619, -0.5134939898138474179, 0.05816208736415689334 ) ) ;
#15563=CARTESIAN_POINT ( 'NONE',  ( 0.1144950937579609085, -0.2764156081756484751, 0.1612500000000024469 ) ) ;
#15565=CARTESIAN_POINT ( 'NONE',  ( 0.2764156081756484196, -5.077672346800151106E-17, 0.4563888888888936735 ) ) ;
#15579=ORIENTED_EDGE ( 'NONE', *, *, #8853, .T. ) ;
#15580=CARTESIAN_POINT ( 'NONE',  ( 0.2209708691207961651, 0.2209708691207959985, 0.2063888888888915363 ) ) ;
#15581=VERTEX_POINT ( 'NONE', #15717 ) ;
#15583=UNCERTAINTY_MEASURE_WITH_UNIT (LENGTH_MEASURE( 1.000000000000000082E-05 ), #5744, 'distance_accuracy_value', 'NONE');
#15585=CARTESIAN_POINT ( 'NONE',  ( -0.3155070326520293400, 0.1306872919485614903, 0.006736111111112530123 ) ) ;
#15590=EDGE_CURVE ( 'NONE', #23326, #1317, #22231, .T. ) ;
#15594=CARTESIAN_POINT ( 'NONE',  ( 0.003366903179264894679, 0.5383683782340862312, 0.05892738626661216117 ) ) ;
#15595=CARTESIAN_POINT ( 'NONE',  ( -0.1954553509668046918, -0.1954553509668046640, 0.1577777777777801815 ) ) ;
#15606=CARTESIAN_POINT ( 'NONE',  ( -0.3309966345752030081, 0.3501648812924316179, 0.4216785431538761508 ) ) ;
#15612=CARTESIAN_POINT ( 'NONE',  ( 0.08494034609768591482, 0.4922255456806988727, 0.06591861138178030377 ) ) ;
#15617=CARTESIAN_POINT ( 'NONE',  ( -0.4805070082343984583, -0.2560807851245831546, 0.04413116910601656145 ) ) ;
#15622=CARTESIAN_POINT ( 'NONE',  ( -0.2764156081756484196, 0.1144950937579609918, -0.01930555555555454883 ) ) ;
#15628=CARTESIAN_POINT ( 'NONE',  ( 0.3155070326520292845, -5.795770164686806123E-17, 0.2567361111111141070 ) ) ;
#15630=CARTESIAN_POINT ( 'NONE',  ( 0.3124999999999999445, 0.1294417382415923023, 0.3695833333333372606 ) ) ;
#15640=ORIENTED_EDGE ( 'NONE', *, *, #21645, .F. ) ;
#15641=CARTESIAN_POINT ( 'NONE',  ( -0.08492194567810140704, 0.4922361691679148499, 0.06591465713331619292 ) ) ;
#15644=ORIENTED_EDGE ( 'NONE', *, *, #6637, .F. ) ;
#15668=ORIENTED_EDGE ( 'NONE', *, *, #19742, .T. ) ;
#15669=AXIS2_PLACEMENT_3D ( 'NONE', #6299, #10096, #812 ) ;
#15671=ORIENTED_EDGE ( 'NONE', *, *, #7509, .T. ) ;
#15674=CARTESIAN_POINT ( 'NONE',  ( -0.07572755880264375739, -0.4860218594902851463, 0.4166771511014251694 ) ) ;
#15675=CARTESIAN_POINT ( 'NONE',  ( -0.3125000000000010547, 0.1294417382415911921, 0.2793055555555588598 ) ) ;
#15679=CARTESIAN_POINT ( 'NONE',  ( -0.4584472689070020479, 0.2219065841078094181, 0.4063187442602073651 ) ) ;
#15680=CARTESIAN_POINT ( 'NONE',  ( 0.3124999999999989453, -0.1294417382415934403, -0.07486111111111042049 ) ) ;
#15683=CYLINDRICAL_SURFACE ( 'NONE', #14172, 0.3125000000000000000 ) ;
#15684=CARTESIAN_POINT ( 'NONE',  ( 0.1144950937579609085, -0.2764156081756484751, 0.3834722222222265997 ) ) ;
#15686=CARTESIAN_POINT ( 'NONE',  ( 0.2764156081756484196, -5.077672346800151106E-17, 0.1716666666666692431 ) ) ;
#15691=CARTESIAN_POINT ( 'NONE',  ( -0.3125000000000000000, 1.913510623667739771E-17, 0.3383333333333369830 ) ) ;
#15694=CARTESIAN_POINT ( 'NONE',  ( 8.768852782367848672E-17, -0.5412658773652745392, 0.4425000000000000044 ) ) ;
#15705=CARTESIAN_POINT ( 'NONE',  ( 0.000000000000000000, 0.3155070326520292845, -0.003680555555554220534 ) ) ;
#15706=CARTESIAN_POINT ( 'NONE',  ( -0.08367912913462059732, -0.4929537096338480473, 0.07813342133392800481 ) ) ;
#15710=CARTESIAN_POINT ( 'NONE',  ( 0.1144950937579609085, -0.2764156081756484751, 0.1126388888888909395 ) ) ;
#15711=CARTESIAN_POINT ( 'NONE',  ( -0.1294417382415922746, -0.3125000000000000000, 0.4112500000000045008 ) ) ;
#15712=CARTESIAN_POINT ( 'NONE',  ( -0.1537937564252621903, -0.2409193255903078756, -0.07485594907830336875 ) ) ;
#15713=CARTESIAN_POINT ( 'NONE',  ( 0.1144950937579611444, 0.2764156081756483641, 0.3001388888888924522 ) ) ;
#15717=CARTESIAN_POINT ( 'NONE',  ( 0.4805070082343983473, 0.2560807851245830991, 0.04413116910601658921 ) ) ;
#15723=SPHERICAL_SURFACE ( 'NONE', #5349, 0.01874999999999999931 ) ;
#15725=CYLINDRICAL_SURFACE ( 'NONE', #14155, 0.01874999999999997155 ) ;
#15735=CARTESIAN_POINT ( 'NONE',  ( -0.4687500000000003886, 0.08781630462512594881, 0.08855667131757492816 ) ) ;
#15736=CARTESIAN_POINT ( 'NONE',  ( 0.1144950937579611444, 0.2764156081756483641, 0.1265277777777799595 ) ) ;
#15740=DIRECTION ( 'NONE',  ( -1.000000000000000000, 0.000000000000000000, 0.000000000000000000 ) ) ;
#15741=EDGE_CURVE ( 'NONE', #8540, #6009, #22680, .T. ) ;
#15743=CARTESIAN_POINT ( 'NONE',  ( -0.1144950937579609918, -0.2764156081756484196, 0.2168055555555584990 ) ) ;
#15747=CARTESIAN_POINT ( 'NONE',  ( -0.4223122635727385998, 0.2974437783094735499, 0.07051021533369884742 ) ) ;
#15749=CARTESIAN_POINT ( 'NONE',  ( -0.2230971623002953874, 0.2230971623002954152, 0.4442361111111156058 ) ) ;
#15771=VERTEX_POINT ( 'NONE', #950 ) ;
#15779=DIRECTION ( 'NONE',  ( -0.7071067811865435759, 8.659560562354884787E-17, 0.7071067811865514585 ) ) ;
#15793=DIRECTION ( 'NONE',  ( 0.000000000000000000, 0.000000000000000000, -1.000000000000000000 ) ) ;
#15798=CYLINDRICAL_SURFACE ( 'NONE', #22413, 0.01874999999999999584 ) ;
#15799=CARTESIAN_POINT ( 'NONE',  ( -0.4687500000000004441, 0.08804416056838103299, 0.4143091105369764438 ) ) ;
#15800=CLOSED_SHELL ( 'NONE', ( #874, #7129, #21535, #15373, #18396, #9429, #15925, #21950, #1398, #7828, #16348, #1843, #17651, #9525, #14525, #18640, #22417, #21397, #13024, #22286, #17495, #21158, #2702, #11385, #23341, #22156, #14226, #14282, #8098, #10929, #3814, #11277, #5589, #4482, #9999, #3614, #23592, #22535, #10974, #15432, #12190, #10275, #10372, #11975, #13664, #785, #4986, #22878, #8130, #23719, #22954, #10278, #12064, #12418, #4568, #14055, #21679, #966, #307, #526, #16783, #22597, #9070, #21511, #11451, #3569, #17849, #14868, #18873, #10022, #817, #7114, #18514, #9314, #9924, #4957, #1665, #21383, #15263, #6947 ) ) ;
#15803=CARTESIAN_POINT ( 'NONE',  ( 0.2764156081756483641, 0.1144950937579610056, 0.06402777777777945989 ) ) ;
#15806=CARTESIAN_POINT ( 'NONE',  ( 0.4500000000000003442, -0.2598076211353317344, 0.3779506566538943235 ) ) ;
#15807=CARTESIAN_POINT ( 'NONE',  ( -0.3124999999999997224, -0.1294417382415924411, -0.04708333333333271364 ) ) ;
#15808=CARTESIAN_POINT ( 'NONE',  ( -0.4645572405553155537, 0.2721000128023691178, 0.05892738626661214729 ) ) ;
#15810=CARTESIAN_POINT ( 'NONE',  ( 0.2209708691207961651, 0.2209708691207959985, 0.1508333333333355120 ) ) ;
#15819=CARTESIAN_POINT ( 'NONE',  ( -0.2230971623002953874, 0.2230971623002954152, 0.05881944444444627690 ) ) ;
#15824=CARTESIAN_POINT ( 'NONE',  ( -0.2764156081756484196, -0.1144950937579609362, -0.01236111111111004406 ) ) ;
#15826=CARTESIAN_POINT ( 'NONE',  ( -0.3023734573831343142, -0.03492818159267604278, -0.09342498493132676829 ) ) ;
#15827=CARTESIAN_POINT ( 'NONE',  ( 0.1144950937579609085, -0.2764156081756484751, 0.4459722222222269328 ) ) ;
#15835=EDGE_CURVE ( 'NONE', #16983, #8442, #10477, .T. ) ;
#15839=CARTESIAN_POINT ( 'NONE',  ( -0.4581189881604794678, 0.2644951211353315235, 0.3941886329748526263 ) ) ;
#15843=CARTESIAN_POINT ( 'NONE',  ( 0.3125000000000000000, -5.740531871003217465E-17, 0.09527777777777987622 ) ) ;
#15845=EDGE_CURVE ( 'NONE', #12538, #10074, #5363, .T. ) ;
#15849=CARTESIAN_POINT ( 'NONE',  ( 0.1916493530484527641, 0.4197546306156790252, 0.4334994210334169318 ) ) ;
#15850=CARTESIAN_POINT ( 'NONE',  ( -0.1144950937579609779, 0.2764156081756484196, 0.07791666666666847985 ) ) ;
#15851=VECTOR ( 'NONE', #15893, 39.37007874015748143 ) ;
#15855=CARTESIAN_POINT ( 'NONE',  ( -0.1954553509668046640, 0.1954553509668046918, 0.2550000000000031686 ) ) ;
#15858=CARTESIAN_POINT ( 'NONE',  ( -0.2209708691207961095, 0.2209708691207961373, -0.05055555555555459740 ) ) ;
#15862=CARTESIAN_POINT ( 'NONE',  ( 0.3155070326520292845, -5.795770164686806123E-17, 0.3122916666666701313 ) ) ;
#15878=CARTESIAN_POINT ( 'NONE',  ( 0.000000000000000000, 0.000000000000000000, 0.000000000000000000 ) ) ;
#15893=DIRECTION ( 'NONE',  ( -0.000000000000000000, -0.000000000000000000, 1.000000000000000000 ) ) ;
#15906=VERTEX_POINT ( 'NONE', #23729 ) ;
#15907=CARTESIAN_POINT ( 'NONE',  ( 0.4687500000000022204, 0.2630304559196462444, 0.05971082423031254943 ) ) ;
#15911=CARTESIAN_POINT ( 'NONE',  ( -0.4687500000000003886, -0.1752855097131576501, 0.4001617384052038595 ) ) ;
#15916=CARTESIAN_POINT ( 'NONE',  ( 0.000000000000000000, 0.2764156081756484196, 0.07444444444444621445 ) ) ;
#15922=LINE ( 'NONE', #16053, #118 ) ;
#15925=ADVANCED_FACE ( 'NONE', ( #8381 ), #10712, .F. ) ;
#15934=CARTESIAN_POINT ( 'NONE',  ( 0.2230971623002953874, -0.2230971623002954429, 0.08659722222222429600 ) ) ;
#15940=CARTESIAN_POINT ( 'NONE',  ( -0.2764156081756484196, 1.692557448933383907E-17, 0.03972222222222369925 ) ) ;
#15943=CARTESIAN_POINT ( 'NONE',  ( -0.2764156081756484196, 0.1144950937579609918, 0.4251388888888933959 ) ) ;
#15945=DIRECTION ( 'NONE',  ( -1.000000000000000000, 1.224646799147353700E-16, 0.000000000000000000 ) ) ;
#15948=CARTESIAN_POINT ( 'NONE',  ( -0.4875000000000003220, 0.2598076211353315124, 0.06112444011295373181 ) ) ;
#15956=FACE_OUTER_BOUND ( 'NONE', #12122, .T. ) ;
#15959=CARTESIAN_POINT ( 'NONE',  ( 0.4593750000000003664, 0.2760455974562901482, 0.3779506566538943235 ) ) ;
#15965=CARTESIAN_POINT ( 'NONE',  ( -0.4687500000000003886, -0.1725638498522215902, 0.06591651963122398261 ) ) ;
#15968=CARTESIAN_POINT ( 'NONE',  ( 0.1954553509668046640, -0.1954553509668047195, 0.05361111111111271227 ) ) ;
#15974=CARTESIAN_POINT ( 'NONE',  ( -0.2764156081756484196, -0.1144950937579609362, 0.2654166666666699093 ) ) ;
#15977=CARTESIAN_POINT ( 'NONE',  ( -0.1347750699935967023, 0.2587654721081596998, 0.4032729751179568445 ) ) ;
#15980=CARTESIAN_POINT ( 'NONE',  ( 0.1306872919485614071, -0.3155070326520293955, 0.3018750000000033906 ) ) ;
#15985=CARTESIAN_POINT ( 'NONE',  ( 0.4687500000000002776, 0.2598076211353320120, 0.3779506566538942125 ) ) ;
#15997=CARTESIAN_POINT ( 'NONE',  ( 0.1294417382415924134, 0.3124999999999999445, 0.3834722222222266552 ) ) ;
#16004=EDGE_LOOP ( 'NONE', ( #3339, #2131, #19050, #14645 ) ) ;
#16030=EDGE_LOOP ( 'NONE', ( #4473, #20245, #21690, #13826 ) ) ;
#16034=ORIENTED_EDGE ( 'NONE', *, *, #3638, .F. ) ;
#16043=CARTESIAN_POINT ( 'NONE',  ( -0.4687500000000004441, -0.2208948773569446300, 0.4011966096125590964 ) ) ;
#16047=CARTESIAN_POINT ( 'NONE',  ( -0.2764156081756484196, 0.1144950937579609918, 0.3626388888888929518 ) ) ;
#16049=CARTESIAN_POINT ( 'NONE',  ( 0.1954553509668047195, 0.1954553509668046085, -0.04361111111111028865 ) ) ;
#16051=CARTESIAN_POINT ( 'NONE',  ( 0.2365780681204331104, 0.1757304751630093809, -0.08326837151785088098 ) ) ;
#16053=CARTESIAN_POINT ( 'NONE',  ( -0.009375000000000190473, 0.5358532185916217161, 0.4425000000000000044 ) ) ;
#16059=FACE_OUTER_BOUND ( 'NONE', #15174, .T. ) ;
#16061=CARTESIAN_POINT ( 'NONE',  ( 0.000000000000000000, 0.3125000000000000000, 0.2202777777777809309 ) ) ;
#16062=CARTESIAN_POINT ( 'NONE',  ( -0.2230971623002953874, 0.2230971623002954152, 0.1143750000000022804 ) ) ;
#16071=CARTESIAN_POINT ( 'NONE',  ( 0.2764156081756484196, -5.077672346800151106E-17, 0.06750000000000168365 ) ) ;
#16074=CARTESIAN_POINT ( 'NONE',  ( -0.1954553509668046640, 0.1954553509668046918, 0.4772222222222271548 ) ) ;
#16084=CARTESIAN_POINT ( 'NONE',  ( -0.3880456933851578194, 0.3172275918314566012, 0.4112725064128996966 ) ) ;
#16086=ORIENTED_EDGE ( 'NONE', *, *, #479, .F. ) ;
#16093=CARTESIAN_POINT ( 'NONE',  ( 0.1144950937579609085, -0.2764156081756484751, 0.05013888888889045381 ) ) ;
#16097=CARTESIAN_POINT ( 'NONE',  ( 0.1144950937579609085, -0.2764156081756484751, 0.2793055555555589708 ) ) ;
#16100=CARTESIAN_POINT ( 'NONE',  ( -0.1976201361917970800, 0.2172293928240131011, 0.4047180943398852038 ) ) ;
#16103=CARTESIAN_POINT ( 'NONE',  ( 0.2764156081756484196, -5.077672346800151106E-17, 0.1161111111111132049 ) ) ;
#16104=CARTESIAN_POINT ( 'NONE',  ( -0.1306872919485614903, 0.3155070326520293400, 0.3296527777777813473 ) ) ;
#16105=CIRCLE ( 'NONE', #16886, 0.6398935782932173577 ) ;
#16108=CARTESIAN_POINT ( 'NONE',  ( 0.4587617856195390087, 0.1788014388648739572, 0.4163859416987428785 ) ) ;
#16117=ORIENTED_EDGE ( 'NONE', *, *, #18095, .T. ) ;
#16118=CARTESIAN_POINT ( 'NONE',  ( 0.2209708691207961651, 0.2209708691207959985, 0.3800000000000043898 ) ) ;
#16129=ORIENTED_EDGE ( 'NONE', *, *, #11289, .F. ) ;
#16145=CARTESIAN_POINT ( 'NONE',  ( -0.3125000000000000000, 1.913510623667739771E-17, 0.1716666666666689933 ) ) ;
#16146=CARTESIAN_POINT ( 'NONE',  ( -0.4723638629038571235, -0.2802187124228194826, 0.04193801346286257781 ) ) ;
#16147=CARTESIAN_POINT ( 'NONE',  ( 0.3385998376278290256, 4.184039657745742702E-17, -0.1012499999999999928 ) ) ;
#16157=CARTESIAN_POINT ( 'NONE',  ( 7.478516849590708700E-17, -0.5289902422706634910, 0.3941886329748525153 ) ) ;
#16158=CARTESIAN_POINT ( 'NONE',  ( 0.1294417382415921358, -0.3125000000000002220, 0.2515277777777811807 ) ) ;
#16162=CARTESIAN_POINT ( 'NONE',  ( -0.4687499999999812372, -0.02254683357178352554, 0.4289648683083041036 ) ) ;
#16168=CARTESIAN_POINT ( 'NONE',  ( -0.2764156081756484196, 1.692557448933383907E-17, 0.1438888888888912032 ) ) ;
#16171=CARTESIAN_POINT ( 'NONE',  ( 0.2209708691207961095, -0.2209708691207961651, 0.4147222222222265442 ) ) ;
#16174=CARTESIAN_POINT ( 'NONE',  ( -0.3125000000000000000, 1.913510623667739771E-17, 0.4008333333333378712 ) ) ;
#16180=ORIENTED_EDGE ( 'NONE', *, *, #6342, .T. ) ;
#16187=CARTESIAN_POINT ( 'NONE',  ( -3.863846776457871776E-17, -0.3155070326520292845, 0.2463194444444477549 ) ) ;
#16189=CIRCLE ( 'NONE', #3338, 0.01874999999999999931 ) ;
#16190=CARTESIAN_POINT ( 'NONE',  ( -0.4593750000000004219, -0.2760455974562901482, 0.06112444011295364160 ) ) ;
#16194=CARTESIAN_POINT ( 'NONE',  ( 0.000000000000000000, 0.2764156081756484196, 0.08138888888889070361 ) ) ;
#16196=CARTESIAN_POINT ( 'NONE',  ( 0.2764156081756484196, -5.077672346800151106E-17, 0.3452777777777816803 ) ) ;
#16209=EDGE_LOOP ( 'NONE', ( #18411, #11662, #12687, #16279, #16876 ) ) ;
#16215=CARTESIAN_POINT ( 'NONE',  ( -0.1541993830833572054, -0.2301090524146454375, -0.06558227484231497761 ) ) ;
#16216=CARTESIAN_POINT ( 'NONE',  ( 0.2764156081756483641, 0.1144950937579610056, 0.1195833333333354703 ) ) ;
#16223=AXIS2_PLACEMENT_3D ( 'NONE', #23192, #1255, #21615 ) ;
#16225=CARTESIAN_POINT ( 'NONE',  ( 0.4687500000000002776, 0.2598076211353319009, 0.06112444011295373875 ) ) ;
#16228=CARTESIAN_POINT ( 'NONE',  ( -0.1954553509668046918, -0.1954553509668046640, 0.09527777777777970969 ) ) ;
#16229=CARTESIAN_POINT ( 'NONE',  ( -0.3155070326520293400, -0.1306872919485614626, 0.4546527777777822910 ) ) ;
#16232=B_SPLINE_CURVE_WITH_KNOTS ( 'NONE', 3,
 ( #608, #19140, #21091, #17073 ),
 .UNSPECIFIED., .F., .F.,
 ( 4, 4 ),
 ( 0.000000000000000000, 0.002245614500282211434 ),
 .UNSPECIFIED. ) ;
#16263=VECTOR ( 'NONE', #6992, 39.37007874015748143 ) ;
#16278=DIRECTION ( 'NONE',  ( 0.000000000000000000, 0.000000000000000000, -1.000000000000000000 ) ) ;
#16279=ORIENTED_EDGE ( 'NONE', *, *, #6901, .F. ) ;
#16281=B_SPLINE_CURVE_WITH_KNOTS ( 'NONE', 3,
 ( #857, #13058, #22296, #9381, #14633, #7310, #20113, #12571 ),
 .UNSPECIFIED., .F., .F.,
 ( 4, 2, 2, 4 ),
 ( 0.000000000000000000, 0.0004997454757086400214, 0.0007496182135629598153, 0.0009994909514172796092 ),
 .UNSPECIFIED. ) ;
#16290=CARTESIAN_POINT ( 'NONE',  ( 0.000000000000000000, 0.2764156081756484196, 0.2966666666666702423 ) ) ;
#16293=CARTESIAN_POINT ( 'NONE',  ( 0.2663714005177876265, 0.1275804160634896045, -0.08436226472404015353 ) ) ;
#16294=DIRECTION ( 'NONE',  ( -0.000000000000000000, -0.000000000000000000, -1.000000000000000000 ) ) ;
#16302=CARTESIAN_POINT ( 'NONE',  ( 0.1306872919485614071, -0.3155070326520293955, 0.3609027777777820134 ) ) ;
#16310=CARTESIAN_POINT ( 'NONE',  ( -0.2764156081756484196, -0.1144950937579609362, 0.3209722222222259891 ) ) ;
#16318=CARTESIAN_POINT ( 'NONE',  ( -0.1294417382415922191, 0.3125000000000000000, 0.3279166666666702423 ) ) ;
#16332=DIRECTION ( 'NONE',  ( 0.000000000000000000, 0.000000000000000000, -1.000000000000000000 ) ) ;
#16333=CARTESIAN_POINT ( 'NONE',  ( -0.2764156081756484196, -0.1144950937579609362, 0.3140277777777815138 ) ) ;
#16337=DIRECTION ( 'NONE',  ( -0.7071067811865484609, 0.000000000000000000, -0.7071067811865464625 ) ) ;
#16341=AXIS2_PLACEMENT_3D ( 'NONE', #1451, #9006, #22048 ) ;
#16343=CARTESIAN_POINT ( 'NONE',  ( -0.02575435819785533778, 0.2888475187005544176, 0.4010461685168428270 ) ) ;
#16346=CARTESIAN_POINT ( 'NONE',  ( 0.1144950937579609085, -0.2764156081756484751, -0.005416666666665539281 ) ) ;
#16347=CARTESIAN_POINT ( 'NONE',  ( 0.1144950937579609085, -0.2764156081756484751, 0.05708333333333493603 ) ) ;
#16348=ADVANCED_FACE ( 'NONE', ( #2647 ), #4466, .F. ) ;
#16349=ORIENTED_EDGE ( 'NONE', *, *, #1357, .F. ) ;
#16352=CARTESIAN_POINT ( 'NONE',  ( -0.3124999999999997224, -0.1294417382415924411, 0.008472222222223286386 ) ) ;
#16365=CIRCLE ( 'NONE', #22594, 0.01875000000000000971 ) ;
#16376=DIRECTION ( 'NONE',  ( -1.749783102806362652E-15, -0.9607689228305231754, -0.2773500981126138520 ) ) ;
#16394=CARTESIAN_POINT ( 'NONE',  ( -0.3838096539023497233, 0.3196732703672032772, 0.06591861138174955059 ) ) ;
#16398=ORIENTED_EDGE ( 'NONE', *, *, #23008, .F. ) ;
#16399=ORIENTED_EDGE ( 'NONE', *, *, #10812, .F. ) ;
#16400=ORIENTED_EDGE ( 'NONE', *, *, #16482, .F. ) ;
#16402=CARTESIAN_POINT ( 'NONE',  ( 0.4593749999999910960, -0.2760455974562953108, 0.06112444011295854740 ) ) ;
#16415=DIRECTION ( 'NONE',  ( -0.000000000000000000, 4.205955132072524856E-15, -1.000000000000000000 ) ) ;
#16416=CARTESIAN_POINT ( 'NONE',  ( -0.2764156081756484196, 0.1144950937579609918, 0.1959722222222249899 ) ) ;
#16429=CARTESIAN_POINT ( 'NONE',  ( 0.1306872919485616846, 0.3155070326520292290, 0.1595138888888915640 ) ) ;
#16435=CARTESIAN_POINT ( 'NONE',  ( 0.1144950937579609085, -0.2764156081756484751, 0.2237500000000028910 ) ) ;
#16438=ORIENTED_EDGE ( 'NONE', *, *, #10578, .T. ) ;
#16450=EDGE_CURVE ( 'NONE', #9622, #960, #9776, .T. ) ;
#16455=FACE_OUTER_BOUND ( 'NONE', #22721, .T. ) ;
#16456=CARTESIAN_POINT ( 'NONE',  ( -0.2764156081756484196, 1.692557448933383907E-17, 0.1438888888888912032 ) ) ;
#16459=CARTESIAN_POINT ( 'NONE',  ( 0.2764156081756484196, -5.077672346800151106E-17, 0.3452777777777816803 ) ) ;
#16465=CARTESIAN_POINT ( 'NONE',  ( 0.1144950937579611444, 0.2764156081756483641, -0.08874999999999956535 ) ) ;
#16468=VERTEX_POINT ( 'NONE', #12172 ) ;
#16472=CARTESIAN_POINT ( 'NONE',  ( 0.4593754077519624501, -0.04467882043364388572, 0.4343923118385376592 ) ) ;
#16482=EDGE_CURVE ( 'NONE', #23140, #280, #15922, .T. ) ;
#16499=CARTESIAN_POINT ( 'NONE',  ( -0.1306872919485615459, -0.3155070326520293400, -0.09395833333333311610 ) ) ;
#16500=CARTESIAN_POINT ( 'NONE',  ( 0.3125000000000000000, -5.740531871003217465E-17, 0.4216666666666709085 ) ) ;
#16510=CARTESIAN_POINT ( 'NONE',  ( -0.6396424860381280109, 0.000000000000000000, -0.01143517789850382292 ) ) ;
#16511=CARTESIAN_POINT ( 'NONE',  ( -0.1590601067977006067, 0.4494324818882923789, 0.07654795713853398964 ) ) ;
#16513=CIRCLE ( 'NONE', #8712, 0.01874999999999999584 ) ;
#16516=EDGE_CURVE ( 'NONE', #8318, #11791, #2056, .T. ) ;
#16520=CARTESIAN_POINT ( 'NONE',  ( -0.2460300421372414448, -0.1745426587114260741, 0.4128571377276832877 ) ) ;
#16529=DIRECTION ( 'NONE',  ( 1.000000000000000000, 0.000000000000000000, 0.000000000000000000 ) ) ;
#16530=ORIENTED_EDGE ( 'NONE', *, *, #20114, .T. ) ;
#16534=CARTESIAN_POINT ( 'NONE',  ( -0.1954553509668046640, 0.1954553509668046918, 0.2480555555555586933 ) ) ;
#16543=DIRECTION ( 'NONE',  ( 0.000000000000000000, 0.000000000000000000, -1.000000000000000000 ) ) ;
#16544=CIRCLE ( 'NONE', #6420, 0.01874999999999997155 ) ;
#16545=DIRECTION ( 'NONE',  ( -0.5000000000000003331, 0.8660254037844383745, 0.000000000000000000 ) ) ;
#16547=CARTESIAN_POINT ( 'NONE',  ( 0.1306872919485614071, -0.3155070326520293955, 0.2497916666666700480 ) ) ;
#16554=CARTESIAN_POINT ( 'NONE',  ( -0.2764156081756484196, 1.692557448933383907E-17, 0.2619444444444476994 ) ) ;
#16558=ORIENTED_EDGE ( 'NONE', *, *, #20607, .F. ) ;
#16568=CARTESIAN_POINT ( 'NONE',  ( 0.008438385721237055825, 0.5369265497013592237, 0.04763613967037114844 ) ) ;
#16570=ORIENTED_EDGE ( 'NONE', *, *, #2572, .T. ) ;
#16572=CARTESIAN_POINT ( 'NONE',  ( 0.2209708691207961095, -0.2209708691207961651, 0.1369444444444465059 ) ) ;
#16573=CARTESIAN_POINT ( 'NONE',  ( -0.2156887100776810617, -0.4167379425407622962, 0.4181572966874574915 ) ) ;
#16574=AXIS2_PLACEMENT_3D ( 'NONE', #22009, #5179, #16652 ) ;
#16576=CARTESIAN_POINT ( 'NONE',  ( 0.1954553509668046640, -0.1954553509668047195, 0.1647222222222247123 ) ) ;
#16577=CARTESIAN_POINT ( 'NONE',  ( 0.3125000000000000000, -5.740531871003217465E-17, 0.1508333333333358728 ) ) ;
#16582=CARTESIAN_POINT ( 'NONE',  ( 0.4802534614900670906, -0.2139706815658275474, 0.05347077774226097896 ) ) ;
#16586=CARTESIAN_POINT ( 'NONE',  ( -0.2764156081756484196, 1.692557448933383907E-17, -0.01583333333333230425 ) ) ;
#16608=CARTESIAN_POINT ( 'NONE',  ( -0.4805453593044316518, 0.2624503992731411772, 0.04271845132551600754 ) ) ;
#16618=CARTESIAN_POINT ( 'NONE',  ( 0.000000000000000000, 0.3155070326520292845, -0.06270833333333286630 ) ) ;
#16619=CARTESIAN_POINT ( 'NONE',  ( 0.4687500000000002776, 0.2598076211353318454, 0.3779506566538942125 ) ) ;
#16631=AXIS2_PLACEMENT_3D ( 'NONE', #2344, #9782, #13215 ) ;
#16632=CARTESIAN_POINT ( 'NONE',  ( 0.000000000000000000, 0.000000000000000000, -0.05999999999999999084 ) ) ;
#16637=ORIENTED_EDGE ( 'NONE', *, *, #21241, .F. ) ;
#16641=EDGE_CURVE ( 'NONE', #6063, #23807, #22081, .T. ) ;
#16642=DIRECTION ( 'NONE',  ( 0.5000000000000004441, -0.8660254037844384856, 0.000000000000000000 ) ) ;
#16647=DIRECTION ( 'NONE',  ( 1.000000000000000000, 0.000000000000000000, 0.000000000000000000 ) ) ;
#16650=ORIENTED_EDGE ( 'NONE', *, *, #5716, .F. ) ;
#16652=DIRECTION ( 'NONE',  ( 0.4999999999999987788, 0.8660254037844393737, 0.000000000000000000 ) ) ;
#16653=CARTESIAN_POINT ( 'NONE',  ( 0.2764156081756484196, -5.077672346800151106E-17, 0.2827777777777812362 ) ) ;
#16656=CARTESIAN_POINT ( 'NONE',  ( 0.1459302940035057949, -0.2450006702336079423, 0.3966998585268076694 ) ) ;
#16666=CARTESIAN_POINT ( 'NONE',  ( -0.2230971623002953874, 0.2230971623002954152, 0.2254861111111142458 ) ) ;
#16669=CARTESIAN_POINT ( 'NONE',  ( 0.3858656996964998642, -0.3184862117744570176, 0.4002370417399356284 ) ) ;
#16673=CARTESIAN_POINT ( 'NONE',  ( 0.000000000000000000, 0.2764156081756484196, 0.1369444444444467002 ) ) ;
#16678=EDGE_CURVE ( 'NONE', #8540, #549, #18820, .T. ) ;
#16683=CARTESIAN_POINT ( 'NONE',  ( -0.3125000000000000000, 1.913510623667739771E-17, 0.1161111111111130384 ) ) ;
#16687=CYLINDRICAL_SURFACE ( 'NONE', #1533, 0.3125000000000000000 ) ;
#16691=CARTESIAN_POINT ( 'NONE',  ( -0.4593750000000004219, -0.2760455974562901482, 0.3779506566538942125 ) ) ;
#16694=CARTESIAN_POINT ( 'NONE',  ( 0.000000000000000000, 0.2764156081756484196, 0.1855555555555581937 ) ) ;
#16695=DIRECTION ( 'NONE',  ( -0.8459207832372986902, -0.4883925919151528294, 0.2142211582677917003 ) ) ;
#16704=CARTESIAN_POINT ( 'NONE',  ( -3.385114897866767815E-17, -0.2764156081756484196, -0.1130555555555552844 ) ) ;
#16708=CARTESIAN_POINT ( 'NONE',  ( 0.4581189881604794123, -0.2644951211353317455, 0.3941886329748525153 ) ) ;
#16716=EDGE_CURVE ( 'NONE', #17904, #22501, #6599, .T. ) ;
#16726=CARTESIAN_POINT ( 'NONE',  ( -0.4593749999999912070, 0.2760455974562950887, 0.06112444011295854046 ) ) ;
#16730=EDGE_LOOP ( 'NONE', ( #12131, #3394, #5236, #10942 ) ) ;
#16734=CARTESIAN_POINT ( 'NONE',  ( 0.3155070326520292845, -5.795770164686806123E-17, -0.07659722222222187238 ) ) ;
#16747=AXIS2_PLACEMENT_3D ( 'NONE', #21014, #4308, #2494 ) ;
#16751=CARTESIAN_POINT ( 'NONE',  ( -0.3103034095256952951, 0.3621121203451553860, 0.4135550951626318361 ) ) ;
#16752=CARTESIAN_POINT ( 'NONE',  ( 0.1338087529396776443, -0.2734308413693284923, -0.09311885657517415815 ) ) ;
#16770=CARTESIAN_POINT ( 'NONE',  ( -0.1954553509668046918, -0.1954553509668046640, 0.3175000000000037237 ) ) ;
#16773=CARTESIAN_POINT ( 'NONE',  ( -0.1380212367034723275, -0.4615792792006397915, 0.4105854900893666226 ) ) ;
#16774=CARTESIAN_POINT ( 'NONE',  ( 0.3125000000000000000, -5.740531871003217465E-17, 0.2550000000000030020 ) ) ;
#16783=ADVANCED_FACE ( 'NONE', ( #3481 ), #6491, .T. ) ;
#16785=VERTEX_POINT ( 'NONE', #16888 ) ;
#16790=FACE_OUTER_BOUND ( 'NONE', #11911, .T. ) ;
#16797=CARTESIAN_POINT ( 'NONE',  ( 0.000000000000000000, 0.2764156081756484196, 0.07444444444444621445 ) ) ;
#16799=CARTESIAN_POINT ( 'NONE',  ( -0.2764156081756484196, 1.692557448933383907E-17, 0.3175000000000036682 ) ) ;
#16801=CARTESIAN_POINT ( 'NONE',  ( -0.4805070082343984583, -0.2560807851245831546, 0.04413116910601652676 ) ) ;
#16813=ORIENTED_EDGE ( 'NONE', *, *, #14678, .T. ) ;
#16814=DIRECTION ( 'NONE',  ( 0.000000000000000000, 1.000000000000000000, 0.000000000000000000 ) ) ;
#16819=CARTESIAN_POINT ( 'NONE',  ( -0.2764156081756484196, 0.1144950937579609918, 0.1959722222222249899 ) ) ;
#16820=CARTESIAN_POINT ( 'NONE',  ( -0.3125000000000000000, 3.738758431839877614E-19, -0.1016666666666665164 ) ) ;
#16823=EDGE_LOOP ( 'NONE', ( #16650, #13234, #1705 ) ) ;
#16829=CARTESIAN_POINT ( 'NONE',  ( -0.1144950937579609779, 0.2764156081756484196, 0.02930555555555695163 ) ) ;
#16854=CARTESIAN_POINT ( 'NONE',  ( 0.000000000000000000, 0.3155070326520292845, 0.04840277777777911294 ) ) ;
#16856=CARTESIAN_POINT ( 'NONE',  ( -0.01172578639831953380, -0.5344959914317446437, 0.04874733047933992036 ) ) ;
#16858=DIRECTION ( 'NONE',  ( -0.8660254037844388186, 0.4999999999999997224, 0.000000000000000000 ) ) ;
#16865=DIRECTION ( 'NONE',  ( 0.000000000000000000, 0.000000000000000000, -1.000000000000000000 ) ) ;
#16873=CARTESIAN_POINT ( 'NONE',  ( 0.4621660567954134491, -0.2744341800641368345, 0.05971082423030580483 ) ) ;
#16875=LINE ( 'NONE', #20651, #17862 ) ;
#16876=ORIENTED_EDGE ( 'NONE', *, *, #2572, .F. ) ;
#16886=AXIS2_PLACEMENT_3D ( 'NONE', #15015, #22437, #18659 ) ;
#16888=CARTESIAN_POINT ( 'NONE',  ( -0.4593750000000004219, 0.2760455974562897596, 0.3779506566538943790 ) ) ;
#16889=CARTESIAN_POINT ( 'NONE',  ( 0.1586325827338087857, -0.4496793130216646950, 0.08858683671056813425 ) ) ;
#16908=CARTESIAN_POINT ( 'NONE',  ( -0.1144950937579609779, 0.2764156081756484196, 0.07791666666666846597 ) ) ;
#16910=CARTESIAN_POINT ( 'NONE',  ( 0.1144950937579609085, -0.2764156081756484751, -0.1165277777777775636 ) ) ;
#16912=DIRECTION ( 'NONE',  ( -1.000000000000000000, 0.000000000000000000, 0.000000000000000000 ) ) ;
#16917=CARTESIAN_POINT ( 'NONE',  ( 0.3125000000000000000, -5.740531871003217465E-17, 0.09527777777777987622 ) ) ;
#16930=CARTESIAN_POINT ( 'NONE',  ( -0.1144950937579609779, 0.2764156081756484196, 0.3556944444444484765 ) ) ;
#16934=ORIENTED_EDGE ( 'NONE', *, *, #4380, .T. ) ;
#16937=CARTESIAN_POINT ( 'NONE',  ( -0.3125000000000004996, 0.1294417382415917195, 0.1751388888888916473 ) ) ;
#16938=CARTESIAN_POINT ( 'NONE',  ( 0.4723904922468885048, -0.2801879233228460331, 0.04193467568257214922 ) ) ;
#16940=CARTESIAN_POINT ( 'NONE',  ( -0.2764156081756484196, -0.1144950937579609362, 0.2098611111111139405 ) ) ;
#16949=VERTEX_POINT ( 'NONE', #4792 ) ;
#16953=AXIS2_PLACEMENT_3D ( 'NONE', #17622, #15793, #10079 ) ;
#16954=CARTESIAN_POINT ( 'NONE',  ( -0.1294417382415922191, 0.3125000000000000000, 0.001527777777779144386 ) ) ;
#16969=CARTESIAN_POINT ( 'NONE',  ( -0.1306872919485615459, -0.3155070326520293400, 0.2393750000000029465 ) ) ;
#16970=CARTESIAN_POINT ( 'NONE',  ( -0.2726274893998237858, -0.3838643229717944583, 0.09139053646026255862 ) ) ;
#16983=VERTEX_POINT ( 'NONE', #6874 ) ;
#16990=EDGE_LOOP ( 'NONE', ( #8421, #11754, #6736, #7917, #9398 ) ) ;
#16993=ORIENTED_EDGE ( 'NONE', *, *, #21301, .T. ) ;
#17006=CARTESIAN_POINT ( 'NONE',  ( 0.000000000000000000, 0.2764156081756484196, 0.4633333333333382043 ) ) ;
#17013=ORIENTED_EDGE ( 'NONE', *, *, #14991, .T. ) ;
#17016=VERTEX_POINT ( 'NONE', #16145 ) ;
#17022=CARTESIAN_POINT ( 'NONE',  ( 0.000000000000000000, 0.3155070326520292845, 0.4407638888888937845 ) ) ;
#17027=CARTESIAN_POINT ( 'NONE',  ( -0.4453125000000000000, -5.453505277453057578E-17, 0.4425000000000000044 ) ) ;
#17028=ORIENTED_EDGE ( 'NONE', *, *, #18851, .T. ) ;
#17029=CARTESIAN_POINT ( 'NONE',  ( 0.1954553509668046640, -0.1954553509668047195, 0.3313888888888926743 ) ) ;
#17031=CARTESIAN_POINT ( 'NONE',  ( 0.1954553509668046640, -0.1954553509668047195, -0.1130555555555552844 ) ) ;
#17035=CARTESIAN_POINT ( 'NONE',  ( -0.2663171304906524761, 0.09313777201924451632, -0.07114126500001324849 ) ) ;
#17043=B_SPLINE_CURVE_WITH_KNOTS ( 'NONE', 3,
 ( #7937, #22583, #22699, #8061, #15153, #386, #15391, #5759 ),
 .UNSPECIFIED., .F., .F.,
 ( 4, 2, 2, 4 ),
 ( 0.000000000000000000, 0.002297969625092518512, 0.003446954437638777985, 0.004595939250185037024 ),
 .UNSPECIFIED. ) ;
#17047=CARTESIAN_POINT ( 'NONE',  ( 0.4687500000000002776, -0.2598076211353317344, 0.06112444011295376650 ) ) ;
#17050=CARTESIAN_POINT ( 'NONE',  ( 0.1144950937579611444, 0.2764156081756483641, 0.4043055555555599145 ) ) ;
#17061=CARTESIAN_POINT ( 'NONE',  ( 0.2764156081756483641, -0.1144950937579611167, 0.2862500000000034461 ) ) ;
#17073=CARTESIAN_POINT ( 'NONE',  ( 0.3065849364905491314, 4.945545817829770315E-15, 0.4182516031572158233 ) ) ;
#17075=CARTESIAN_POINT ( 'NONE',  ( 0.2026594160797257904, -0.4367605021652135600, 0.07441357458167795202 ) ) ;
#17081=CARTESIAN_POINT ( 'NONE',  ( 0.4800179196285669914, -0.1716494391952127496, 0.06108892084617357360 ) ) ;
#17082=CARTESIAN_POINT ( 'NONE',  ( -0.1954553509668046918, -0.1954553509668046640, -0.1269444444444442766 ) ) ;
#17088=CARTESIAN_POINT ( 'NONE',  ( 0.2764156081756483641, 0.1144950937579610195, -0.04013888888888804407 ) ) ;
#17091=CIRCLE ( 'NONE', #6571, 0.6398935782932173577 ) ;
#17097=CARTESIAN_POINT ( 'NONE',  ( -0.3155070326520293400, 0.1306872919485614903, 0.2254861111111138572 ) ) ;
#17098=CARTESIAN_POINT ( 'NONE',  ( 0.4687500000000003886, 0.04344991094760242145, 0.4181619485698828131 ) ) ;
#17112=CARTESIAN_POINT ( 'NONE',  ( 0.08700723303891660931, -0.2927098606305870709, -0.09407488447002992915 ) ) ;
#17113=ORIENTED_EDGE ( 'NONE', *, *, #21094, .T. ) ;
#17117=EDGE_CURVE ( 'NONE', #13298, #17016, #9669, .T. ) ;
#17118=CARTESIAN_POINT ( 'NONE',  ( 0.1038682246014075439, 0.2678606782618273008, 0.3984990337825972673 ) ) ;
#17132=ORIENTED_EDGE ( 'NONE', *, *, #11663, .T. ) ;
#17134=CARTESIAN_POINT ( 'NONE',  ( -0.2764156081756484196, 1.692557448933383907E-17, 0.4216666666666711860 ) ) ;
#17141=ORIENTED_EDGE ( 'NONE', *, *, #1301, .F. ) ;
#17144=AXIS2_PLACEMENT_3D ( 'NONE', #19788, #16376, #19664 ) ;
#17153=CARTESIAN_POINT ( 'NONE',  ( 0.08492194567809631389, -0.4922361691679447704, 0.06591465713334185295 ) ) ;
#17154=CARTESIAN_POINT ( 'NONE',  ( 0.2764156081756484196, -5.077672346800151106E-17, 0.2827777777777812362 ) ) ;
#17156=CARTESIAN_POINT ( 'NONE',  ( -3.385114897866767815E-17, -0.2764156081756484196, -0.1199999999999997735 ) ) ;
#17159=CARTESIAN_POINT ( 'NONE',  ( 0.01172578639831967605, -0.5344959914317446437, 0.04874733047933996199 ) ) ;
#17161=CARTESIAN_POINT ( 'NONE',  ( -0.1695524133009077561, 0.2302630372892206234, -0.07448633787354336233 ) ) ;
#17162=CIRCLE ( 'NONE', #6238, 0.3253415854805813412 ) ;
#17172=VERTEX_POINT ( 'NONE', #6117 ) ;
#17176=EDGE_CURVE ( 'NONE', #1317, #22119, #5423, .T. ) ;
#17178=CARTESIAN_POINT ( 'NONE',  ( 0.1144950937579609085, -0.2764156081756484751, 0.3834722222222265442 ) ) ;
#17179=VECTOR ( 'NONE', #18573, 39.37007874015748143 ) ;
#17180=CYLINDRICAL_SURFACE ( 'NONE', #4480, 0.3125000000000000000 ) ;
#17187=CARTESIAN_POINT ( 'NONE',  ( -0.1954553509668046640, 0.1954553509668046918, 0.1994444444444471720 ) ) ;
#17193=B_SPLINE_CURVE_WITH_KNOTS ( 'NONE', 3,
 ( #22902, #6078, #10354, #15826, #19368, #13544, #11704, #17300, #17421, #19127, #945, #593, #834, #17658, #21077, #15712, #8375, #23245, #8025, #11824, #19244, #23016 ),
 .UNSPECIFIED., .F., .F.,
 ( 4, 2, 2, 2, 2, 2, 2, 2, 2, 2, 4 ),
 ( 0.002245614500286350051, 0.002912534838771771700, 0.003579455177257192915, 0.004913295854228036212, 0.006247136531198878642, 0.007580977208169723675, 0.008914817885140568707, 0.009581738223625988621, 0.01024865856211140853, 0.01158249923908224836, 0.01291633991605308993 ),
 .UNSPECIFIED. ) ;
#17197=CARTESIAN_POINT ( 'NONE',  ( 0.3308333333333332571, 3.738758431839877614E-19, 0.4425000000000000044 ) ) ;
#17199=ORIENTED_EDGE ( 'NONE', *, *, #10536, .T. ) ;
#17204=CARTESIAN_POINT ( 'NONE',  ( 0.2722827744214832979, -0.3840633442573331280, 0.4172182224143142770 ) ) ;
#17207=CARTESIAN_POINT ( 'NONE',  ( -0.2764156081756484196, 1.692557448933383907E-17, -0.1338888888888887796 ) ) ;
#17211=CARTESIAN_POINT ( 'NONE',  ( -0.2195630361087207438, -0.1679215936615484073, -0.06558227484231504700 ) ) ;
#17217=CARTESIAN_POINT ( 'NONE',  ( 0.2230971623002953874, -0.2230971623002954429, 0.1942361111111136074 ) ) ;
#17220=CARTESIAN_POINT ( 'NONE',  ( 0.000000000000000000, 0.000000000000000000, -0.1012499999999999928 ) ) ;
#17231=CARTESIAN_POINT ( 'NONE',  ( -0.3124999999999989453, -0.1294417382415932460, 0.2306944444444472830 ) ) ;
#17238=CARTESIAN_POINT ( 'NONE',  ( 0.2799731695447734148, 0.01905728454626108223, 0.3921285916995966847 ) ) ;
#17241=B_SPLINE_CURVE_WITH_KNOTS ( 'NONE', 3,
 ( #98, #11208, #7425, #22536, #9617, #15228, #16573, #11450, #20707, #18635, #223, #16691 ),
 .UNSPECIFIED., .F., .F.,
 ( 4, 2, 2, 2, 2, 4 ),
 ( 0.000000000000000000, 0.003345931539952393900, 0.005018897309928591934, 0.006691863079904790401, 0.01003779461985718734, 0.01338372615980958427 ),
 .UNSPECIFIED. ) ;
#17243=ORIENTED_EDGE ( 'NONE', *, *, #6455, .F. ) ;
#17252=CARTESIAN_POINT ( 'NONE',  ( 0.000000000000000000, 0.2764156081756484196, 0.4077777777777822354 ) ) ;
#17255=( BOUNDED_CURVE ( )  B_SPLINE_CURVE ( 2, ( #17675, #17794, #3153, #10247, #12208, #12324, #17555, #21334, #6572 ),
 .UNSPECIFIED., .F., .F. ) 
 B_SPLINE_CURVE_WITH_KNOTS ( ( 3, 2, 2, 2, 3 ),
 ( 0.6979166666666667407, 0.7083333333333333703, 0.7187500000000000000, 0.7291666666666667407, 0.7395833333333333703 ),
 .UNSPECIFIED. ) 
 CURVE ( )  GEOMETRIC_REPRESENTATION_ITEM ( )  RATIONAL_B_SPLINE_CURVE ( ( 1.000000000000000000, 0.9238795325112867385, 1.000000000000000000, 0.9238795325112867385, 1.000000000000000000, 0.9238795325112867385, 1.000000000000000000, 0.9238795325112867385, 1.000000000000000000 ) ) 
 REPRESENTATION_ITEM ( '' )  );
#17273=CARTESIAN_POINT ( 'NONE',  ( 0.01848103877824610469, -0.5441716683897390716, 0.04413116910601656145 ) ) ;
#17274=CARTESIAN_POINT ( 'NONE',  ( -0.1144950937579609779, 0.2764156081756484196, 0.3001388888888924522 ) ) ;
#17276=CARTESIAN_POINT ( 'NONE',  ( -0.1954553509668046640, 0.1954553509668046918, -0.1408333333333332826 ) ) ;
#17277=ORIENTED_EDGE ( 'NONE', *, *, #3221, .T. ) ;
#17280=CARTESIAN_POINT ( 'NONE',  ( 0.4593750000000002554, -1.978974282089605735E-13, 0.4343810118395207698 ) ) ;
#17283=CARTESIAN_POINT ( 'NONE',  ( 0.2533266501255685976, -0.1176800686430039961, 0.3893196305818418801 ) ) ;
#17292=CARTESIAN_POINT ( 'NONE',  ( 0.4723836327791856582, -0.2801952116499829559, 0.04193567535760548554 ) ) ;
#17293=CARTESIAN_POINT ( 'NONE',  ( -0.1144950937579609779, 0.2764156081756484196, 0.4112500000000044453 ) ) ;
#17300=CARTESIAN_POINT ( 'NONE',  ( -0.2744310710835944356, -0.1177455570399758150, -0.08727062790145140303 ) ) ;
#17301=CARTESIAN_POINT ( 'NONE',  ( 0.000000000000000000, 0.2764156081756484196, 0.2480555555555586933 ) ) ;
#17302=CIRCLE ( 'NONE', #14580, 0.01875000000000003747 ) ;
#17305=DIRECTION ( 'NONE',  ( 0.000000000000000000, 0.000000000000000000, 1.000000000000000000 ) ) ;
#17314=ORIENTED_EDGE ( 'NONE', *, *, #15741, .T. ) ;
#17319=CIRCLE ( 'NONE', #18886, 0.01874999999999996461 ) ;
#17327=CARTESIAN_POINT ( 'NONE',  ( 0.1954553509668046640, -0.1954553509668047195, -0.05055555555555479863 ) ) ;
#17334=CARTESIAN_POINT ( 'NONE',  ( 0.1306872919485614071, -0.3155070326520293955, 0.1352083333333353732 ) ) ;
#17337=CARTESIAN_POINT ( 'NONE',  ( 7.043045608665678148E-17, -0.5196152422706635798, 0.4425000000000000044 ) ) ;
#17344=CARTESIAN_POINT ( 'NONE',  ( -0.3125000000000000000, 1.913510623667739771E-17, 0.2897222222222258226 ) ) ;
#17366=ORIENTED_EDGE ( 'NONE', *, *, #16516, .T. ) ;
#17376=ORIENTED_EDGE ( 'NONE', *, *, #23780, .T. ) ;
#17390=( BOUNDED_CURVE ( )  B_SPLINE_CURVE ( 2, ( #17211, #2458, #7818, #20979, #11730, #8051, #17327, #22573, #18920, #17088, #21104, #15501, #495, #739, #5861, #15622, #4393, #22927, #20862, #3920, #2574, #11486, #11365, #377, #2220, #5980, #15260, #13443, #257, #10024, #7697, #11855, #13320, #20742, #19269, #5749, #7928, #13208, #22810, #2341, #17446, #9777, #18792, #4156, #22690, #6101, #2087, #15382, #15143, #6464, #8530, #23395, #12452, #18043, #21463, #2691, #21225, #10144, #14033, #23511, #17926, #3049, #19511, #21576, #8405, #4514, #6584, #2925, #6702, #12337, #19871, #3163, #21346, #2804, #19754, #10259, #4634, #10613, #4747, #4870, #17568, #12218, #10496, #15743, #19628, #1339, #4988, #10385, #17685, #12101, #17807, #977, #11980, #6345, #15855, #23272, #1098, #15974, #14147, #1222, #8648, #16097, #6826, #14267, #21704, #8768, #23040, #13797, #19393, #858, #8289, #23153, #13918, #13383, #6951, #5353, #15203, #22639, #320, #11552, #16459, #10734, #3406, #4094, #18522, #19993, #10978, #24000, #7074, #7191, #3527, #12943, #20237, #20355, #18404 ),
 .UNSPECIFIED., .F., .F. ) 
 B_SPLINE_CURVE_WITH_KNOTS ( ( 3, 2, 2, 2, 2, 2, 2, 2, 2, 2, 2, 2, 2, 2, 2, 2, 2, 2, 2, 2, 2, 2, 2, 2, 2, 2, 2, 2, 2, 2, 2, 2, 2, 2, 2, 2, 2, 2, 2, 2, 2, 2, 2, 2, 2, 2, 2, 2, 2, 2, 2, 2, 2, 2, 2, 2, 2, 2, 2, 2, 2, 2, 2, 2, 2, 2, 2, 3 ),
 ( 0.1128009810283470138, 0.1145833333333333287, 0.1250000000000000000, 0.1354166666666666574, 0.1458333333333333426, 0.1562500000000000000, 0.1666666666666666574, 0.1770833333333333426, 0.1875000000000000000, 0.1979166666666666574, 0.2083333333333333703, 0.2187500000000000000, 0.2291666666666666574, 0.2395833333333333426, 0.2500000000000000000, 0.2604166666666666852, 0.2708333333333333148, 0.2812500000000000000, 0.2916666666666666852, 0.3020833333333333703, 0.3125000000000000000, 0.3229166666666666297, 0.3333333333333333703, 0.3437500000000000000, 0.3541666666666667407, 0.3645833333333333148, 0.3750000000000000000, 0.3854166666666666852, 0.3958333333333333148, 0.4062500000000000000, 0.4166666666666666852, 0.4270833333333333148, 0.4375000000000000000, 0.4479166666666666852, 0.4583333333333333148, 0.4687500000000000000, 0.4791666666666666852, 0.4895833333333333703, 0.4999999999999999445, 0.5104166666666665186, 0.5208333333333333703, 0.5312500000000000000, 0.5416666666666666297, 0.5520833333333332593, 0.5625000000000000000, 0.5729166666666667407, 0.5833333333333333703, 0.5937500000000000000, 0.6041666666666666297, 0.6145833333333333703, 0.6250000000000000000, 0.6354166666666666297, 0.6458333333333333703, 0.6562500000000000000, 0.6666666666666666297, 0.6770833333333333703, 0.6875000000000000000, 0.6979166666666666297, 0.7083333333333333703, 0.7187500000000000000, 0.7291666666666666297, 0.7395833333333333703, 0.7500000000000000000, 0.7604166666666666297, 0.7708333333333333703, 0.7812500000000000000, 0.7916666666666666297, 0.7934490189716459918 ),
 .UNSPECIFIED. ) 
 CURVE ( )  GEOMETRIC_REPRESENTATION_ITEM ( )  RATIONAL_B_SPLINE_CURVE ( ( 0.9784078784059424549, 0.9869753448942262253, 1.000000000000000000, 0.9238795325112867385, 1.000000000000000000, 0.9238795325112867385, 1.000000000000000000, 0.9238795325112867385, 1.000000000000000000, 0.9238795325112867385, 1.000000000000000000, 0.9238795325112867385, 1.000000000000000000, 0.9238795325112867385, 1.000000000000000000, 0.9238795325112867385, 1.000000000000000000, 0.9238795325112867385, 1.000000000000000000, 0.9238795325112867385, 1.000000000000000000, 0.9238795325112867385, 1.000000000000000000, 0.9238795325112867385, 1.000000000000000000, 0.9238795325112867385, 1.000000000000000000, 0.9238795325112867385, 1.000000000000000000, 0.9238795325112867385, 1.000000000000000000, 0.9238795325112867385, 1.000000000000000000, 0.9238795325112867385, 1.000000000000000000, 0.9238795325112867385, 1.000000000000000000, 0.9238795325112867385, 1.000000000000000000, 0.9238795325112867385, 1.000000000000000000, 0.9238795325112867385, 1.000000000000000000, 0.9238795325112867385, 1.000000000000000000, 0.9238795325112867385, 1.000000000000000000, 0.9238795325112867385, 1.000000000000000000, 0.9238795325112867385, 1.000000000000000000, 0.9238795325112867385, 1.000000000000000000, 0.9238795325112867385, 1.000000000000000000, 0.9238795325112867385, 1.000000000000000000, 0.9238795325112867385, 1.000000000000000000, 0.9238795325112867385, 1.000000000000000000, 0.9238795325112867385, 1.000000000000000000, 0.9238795325112867385, 1.000000000000000000, 0.9238795325112867385, 1.000000000000000000, 0.9238795325112867385, 1.000000000000000000, 0.9238795325112867385, 1.000000000000000000, 0.9238795325112867385, 1.000000000000000000, 0.9238795325112867385, 1.000000000000000000, 0.9238795325112867385, 1.000000000000000000, 0.9238795325112867385, 1.000000000000000000, 0.9238795325112867385, 1.000000000000000000, 0.9238795325112867385, 1.000000000000000000, 0.9238795325112867385, 1.000000000000000000, 0.9238795325112867385, 1.000000000000000000, 0.9238795325112867385, 1.000000000000000000, 0.9238795325112867385, 1.000000000000000000, 0.9238795325112867385, 1.000000000000000000, 0.9238795325112867385, 1.000000000000000000, 0.9238795325112867385, 1.000000000000000000, 0.9238795325112867385, 1.000000000000000000, 0.9238795325112867385, 1.000000000000000000, 0.9238795325112867385, 1.000000000000000000, 0.9238795325112867385, 1.000000000000000000, 0.9238795325112867385, 1.000000000000000000, 0.9238795325112867385, 1.000000000000000000, 0.9238795325112867385, 1.000000000000000000, 0.9238795325112867385, 1.000000000000000000, 0.9238795325112867385, 1.000000000000000000, 0.9238795325112867385, 1.000000000000000000, 0.9238795325112867385, 1.000000000000000000, 0.9238795325112867385, 1.000000000000000000, 0.9238795325112867385, 1.000000000000000000, 0.9238795325112867385, 1.000000000000000000, 0.9238795325112867385, 1.000000000000000000, 0.9238795325112867385, 1.000000000000000000, 0.9238795325112867385, 1.000000000000000000, 0.9238795325112867385, 1.000000000000000000, 0.9869753448942770735, 0.9784078784060095124 ) ) 
 REPRESENTATION_ITEM ( '' )  );
#17391=CARTESIAN_POINT ( 'NONE',  ( 0.2725578398252748724, -0.3839045351724091337, 0.09139393128962809698 ) ) ;
#17392=CARTESIAN_POINT ( 'NONE',  ( -0.1954553509668046918, -0.1954553509668046640, 0.3175000000000037237 ) ) ;
#17394=CARTESIAN_POINT ( 'NONE',  ( 0.2764156081756483641, -0.1144950937579611167, 0.3973611111111153837 ) ) ;
#17400=CARTESIAN_POINT ( 'NONE',  ( 0.1294417382415921358, -0.3125000000000002220, 0.3556944444444482545 ) ) ;
#17402=CARTESIAN_POINT ( 'NONE',  ( -0.4593750000000004219, 0.2760455974562897596, 0.06112444011295372487 ) ) ;
#17407=ORIENTED_EDGE ( 'NONE', *, *, #11843, .T. ) ;
#17410=ORIENTED_EDGE ( 'NONE', *, *, #21645, .T. ) ;
#17411=DIRECTION ( 'NONE',  ( 0.000000000000000000, 0.2773500981126144627, 0.9607689228305228424 ) ) ;
#17413=CARTESIAN_POINT ( 'NONE',  ( 0.000000000000000000, 0.2764156081756484196, 0.4633333333333382043 ) ) ;
#17421=CARTESIAN_POINT ( 'NONE',  ( -0.2659300498200202756, -0.1330428112939968099, -0.08601205871610874409 ) ) ;
#17422=CARTESIAN_POINT ( 'NONE',  ( 0.1954553509668047195, 0.1954553509668046085, 0.1855555555555581937 ) ) ;
#17423=ORIENTED_EDGE ( 'NONE', *, *, #22272, .F. ) ;
#17431=CARTESIAN_POINT ( 'NONE',  ( -0.07520958173006352110, 0.4863159908245682228, 0.4165421425001717970 ) ) ;
#17440=CARTESIAN_POINT ( 'NONE',  ( -0.4687500000000003886, -0.08780557671060627845, 0.08855765995869291363 ) ) ;
#17442=CARTESIAN_POINT ( 'NONE',  ( -0.2998642343065030524, 0.08796414601291394075, -0.1016666666666771329 ) ) ;
#17446=CARTESIAN_POINT ( 'NONE',  ( 0.2764156081756484196, -5.077672346800151106E-17, 0.06750000000000168365 ) ) ;
#17452=CARTESIAN_POINT ( 'NONE',  ( -0.2230971623002953874, 0.2230971623002954152, 0.1664583333333356230 ) ) ;
#17464=CARTESIAN_POINT ( 'NONE',  ( -3.827021247335479543E-17, -0.3125000000000000000, 0.2411111111111140515 ) ) ;
#17467=CARTESIAN_POINT ( 'NONE',  ( -0.04611292249197078419, 0.5146425691514149303, 0.3901966308178845266 ) ) ;
#17479=CARTESIAN_POINT ( 'NONE',  ( 0.4581189881604794678, 0.2644951211353318010, 0.3941886329748525153 ) ) ;
#17486=FACE_OUTER_BOUND ( 'NONE', #5361, .T. ) ;
#17492=ORIENTED_EDGE ( 'NONE', *, *, #6401, .F. ) ;
#17495=ADVANCED_FACE ( 'NONE', ( #21953 ), #1668, .T. ) ;
#17500=DIRECTION ( 'NONE',  ( -1.000000000000000000, 0.000000000000000000, 0.000000000000000000 ) ) ;
#17505=CARTESIAN_POINT ( 'NONE',  ( 0.3125000000000000000, -5.740531871003217465E-17, -0.07138888888888809958 ) ) ;
#17509=CARTESIAN_POINT ( 'NONE',  ( 0.2764156081756483641, -0.1144950937579611167, 0.05708333333333497073 ) ) ;
#17518=FACE_OUTER_BOUND ( 'NONE', #20970, .T. ) ;
#17526=DIRECTION ( 'NONE',  ( -1.000000000000000000, 0.000000000000000000, 0.000000000000000000 ) ) ;
#17533=CARTESIAN_POINT ( 'NONE',  ( -0.1306872919485615459, -0.3155070326520293400, 0.1317361111111135519 ) ) ;
#17534=CARTESIAN_POINT ( 'NONE',  ( -0.2723952011404802698, -0.3839984346608560917, 0.09139143879391148362 ) ) ;
#17538=CARTESIAN_POINT ( 'NONE',  ( 0.000000000000000000, 3.738758431839877614E-19, -0.1145082521472477743 ) ) ;
#17542=CARTESIAN_POINT ( 'NONE',  ( -0.1144950937579609779, 0.2764156081756484196, 0.4181944444444490316 ) ) ;
#17551=CARTESIAN_POINT ( 'NONE',  ( -0.08099032061185373887, 0.4945060939582657245, 0.4113389257669837762 ) ) ;
#17555=CARTESIAN_POINT ( 'NONE',  ( -0.2209708691207961373, -0.2209708691207961095, -0.03666666666666560520 ) ) ;
#17562=CARTESIAN_POINT ( 'NONE',  ( -0.4687500000000003886, -0.1743457508753611940, 0.07807959546537707185 ) ) ;
#17563=CARTESIAN_POINT ( 'NONE',  ( -3.385114897866767815E-17, -0.2764156081756484196, 0.04666666666666822311 ) ) ;
#17568=CARTESIAN_POINT ( 'NONE',  ( -0.2764156081756484196, 1.692557448933383907E-17, 0.2063888888888917028 ) ) ;
#17571=CARTESIAN_POINT ( 'NONE',  ( -0.4805070082343984583, 0.2560807851245828770, 0.04413116910601658921 ) ) ;
#17572=CARTESIAN_POINT ( 'NONE',  ( 0.3125000000000000000, 3.827021247335477694E-17, 1.326383476483184332 ) ) ;
#17573=CARTESIAN_POINT ( 'NONE',  ( 0.000000000000000000, 0.3125000000000000000, -0.008888888888887978151 ) ) ;
#17574=CARTESIAN_POINT ( 'NONE',  ( -0.3155070326520293400, -0.1306872919485614626, 0.2879861111111143290 ) ) ;
#17583=CARTESIAN_POINT ( 'NONE',  ( -0.4254287158503465838, 0.3089275304546714174, 0.05347130368200839201 ) ) ;
#17585=VERTEX_POINT ( 'NONE', #9153 ) ;
#17593=ORIENTED_EDGE ( 'NONE', *, *, #1357, .T. ) ;
#17600=EDGE_CURVE ( 'NONE', #9081, #1635, #16105, .T. ) ;
#17608=MANIFOLD_SOLID_BREP ( 'Cut-Extrude3', #15800 ) ;
#17622=CARTESIAN_POINT ( 'NONE',  ( 0.4500000000000003442, 0.2598076211353318454, 0.4425000000000000044 ) ) ;
#17626=DIRECTION ( 'NONE',  ( 0.000000000000000000, 0.000000000000000000, -1.000000000000000000 ) ) ;
#17628=CARTESIAN_POINT ( 'NONE',  ( -0.4687500000000002776, 0.04392189231563564666, 0.4181471319205499748 ) ) ;
#17631=CARTESIAN_POINT ( 'NONE',  ( 0.1144950937579609085, -0.2764156081756484751, -0.005416666666665539281 ) ) ;
#17638=CARTESIAN_POINT ( 'NONE',  ( -0.3125000000000000000, 0.04488961648812229976, -0.1003708124548366720 ) ) ;
#17643=CARTESIAN_POINT ( 'NONE',  ( 0.04643773642726162915, 0.5144550377384379258, 0.07051021533369888905 ) ) ;
#17644=ORIENTED_EDGE ( 'NONE', *, *, #20901, .F. ) ;
#17649=CARTESIAN_POINT ( 'NONE',  ( 0.3155070326520292290, 0.1306872919485615736, -0.01409722222222097032 ) ) ;
#17651=ADVANCED_FACE ( 'NONE', ( #362 ), #18905, .F. ) ;
#17656=CARTESIAN_POINT ( 'NONE',  ( -0.2764156081756484196, 0.1144950937579609918, 0.03625000000000144079 ) ) ;
#17658=CARTESIAN_POINT ( 'NONE',  ( -0.1762772571227776142, -0.2274112121558196364, -0.07676730507356434308 ) ) ;
#17659=CARTESIAN_POINT ( 'NONE',  ( -0.1954553509668046918, -0.1954553509668046640, 0.3244444444444481435 ) ) ;
#17671=CARTESIAN_POINT ( 'NONE',  ( -0.4593750000000004219, 0.2760455974562897596, 0.3779506566538943790 ) ) ;
#17675=CARTESIAN_POINT ( 'NONE',  ( 0.3125000000000000000, -5.740531871003217465E-17, -0.01583333333333210996 ) ) ;
#17680=CARTESIAN_POINT ( 'NONE',  ( -0.4795759180132158628, 0.04343035316921608352, 0.07439866462880882769 ) ) ;
#17681=CARTESIAN_POINT ( 'NONE',  ( 0.000000000000000000, 0.2764156081756484196, 0.07444444444444621445 ) ) ;
#17685=CARTESIAN_POINT ( 'NONE',  ( 0.2764156081756484196, -5.077672346800151106E-17, 0.2341666666666696595 ) ) ;
#17688=CARTESIAN_POINT ( 'NONE',  ( 0.05866837512862279475, 0.2818896272181937723, 0.3994403845921892793 ) ) ;
#17692=CARTESIAN_POINT ( 'NONE',  ( 0.000000000000000000, 0.3155070326520292845, 0.4928472222222270993 ) ) ;
#17693=ORIENTED_EDGE ( 'NONE', *, *, #23606, .F. ) ;
#17695=CARTESIAN_POINT ( 'NONE',  ( 0.000000000000000000, 0.3125000000000000000, 0.3800000000000039457 ) ) ;
#17704=CARTESIAN_POINT ( 'NONE',  ( 0.3125000000000000555, -5.740531871003217465E-17, 0.3730555555555599145 ) ) ;
#17718=EDGE_CURVE ( 'NONE', #7699, #6271, #9759, .T. ) ;
#17725=CARTESIAN_POINT ( 'NONE',  ( -0.3308333333333332571, 4.088927411497558688E-17, 0.4425000000000000044 ) ) ;
#17733=ORIENTED_EDGE ( 'NONE', *, *, #13258, .F. ) ;
#17735=ORIENTED_EDGE ( 'NONE', *, *, #7501, .F. ) ;
#17740=( BOUNDED_CURVE ( )  B_SPLINE_CURVE ( 2, ( #23213, #19566, #8466, #8599, #23452, #796, #23092, #23328, #6402 ),
 .UNSPECIFIED., .F., .F. ) 
 B_SPLINE_CURVE_WITH_KNOTS ( ( 3, 2, 2, 2, 3 ),
 ( 0.5729166666666667407, 0.5833333333333333703, 0.5937500000000000000, 0.6041666666666667407, 0.6145833333333333703 ),
 .UNSPECIFIED. ) 
 CURVE ( )  GEOMETRIC_REPRESENTATION_ITEM ( )  RATIONAL_B_SPLINE_CURVE ( ( 1.000000000000000000, 0.9238795325112867385, 1.000000000000000000, 0.9238795325112867385, 1.000000000000000000, 0.9238795325112867385, 1.000000000000000000, 0.9238795325112867385, 1.000000000000000000 ) ) 
 REPRESENTATION_ITEM ( '' )  );
#17747=DIRECTION ( 'NONE',  ( -1.000000000000000000, 0.000000000000000000, 0.000000000000000000 ) ) ;
#17751=CARTESIAN_POINT ( 'NONE',  ( -0.1954553509668046918, -0.1954553509668046640, 0.3730555555555596925 ) ) ;
#17753=CARTESIAN_POINT ( 'NONE',  ( 0.1954553509668047195, 0.1954553509668046085, 0.06750000000000172529 ) ) ;
#17765=DIRECTION ( 'NONE',  ( -1.000000000000000000, 0.000000000000000000, 0.000000000000000000 ) ) ;
#17766=VERTEX_POINT ( 'NONE', #3907 ) ;
#17771=CARTESIAN_POINT ( 'NONE',  ( -3.863846776457871776E-17, -0.3155070326520292845, 0.02409722222222379986 ) ) ;
#17772=DIRECTION ( 'NONE',  ( -1.000000000000000000, 0.000000000000000000, 0.000000000000000000 ) ) ;
#17776=CARTESIAN_POINT ( 'NONE',  ( -0.2764156081756484196, 1.692557448933383907E-17, -0.07138888888888829387 ) ) ;
#17778=CARTESIAN_POINT ( 'NONE',  ( -0.006674681701965155291, 0.5374122480878897878, 0.05975678175779895046 ) ) ;
#17779=CARTESIAN_POINT ( 'NONE',  ( -0.2764156081756484196, 0.1144950937579609918, 0.3695833333333374271 ) ) ;
#17792=VERTEX_POINT ( 'NONE', #13555 ) ;
#17794=CARTESIAN_POINT ( 'NONE',  ( 0.3124999999999999445, -0.1294417382415923856, -0.01930555555555435801 ) ) ;
#17801=CARTESIAN_POINT ( 'NONE',  ( 0.2764156081756483641, -0.1144950937579611167, 0.001527777777778965927 ) ) ;
#17802=AXIS2_PLACEMENT_3D ( 'NONE', #15694, #21298, #17883 ) ;
#17805=CARTESIAN_POINT ( 'NONE',  ( 0.1294417382415924134, 0.3124999999999999445, -0.06791666666666622276 ) ) ;
#17807=CARTESIAN_POINT ( 'NONE',  ( 0.1954553509668047195, 0.1954553509668046085, 0.2411111111111141903 ) ) ;
#17810=CARTESIAN_POINT ( 'NONE',  ( 0.4687500000000002776, -0.08781377892924517592, 0.08855691728830629439 ) ) ;
#17811=CARTESIAN_POINT ( 'NONE',  ( 0.4795759075923610726, 0.04327673138052716417, 0.07439896364138759433 ) ) ;
#17812=CARTESIAN_POINT ( 'NONE',  ( -0.3101024306885724058, 0.3622281555308698997, 0.08858850926231193190 ) ) ;
#17814=CARTESIAN_POINT ( 'NONE',  ( -0.3155070326520293400, 0.1306872919485614903, 0.4477083333333378712 ) ) ;
#17828=ORIENTED_EDGE ( 'NONE', *, *, #12276, .T. ) ;
#17833=CARTESIAN_POINT ( 'NONE',  ( -0.08311813270112132501, 0.4932776010757430885, 0.4002893343786022018 ) ) ;
#17849=ADVANCED_FACE ( 'NONE', ( #15956 ), #15725, .T. ) ;
#17850=( BOUNDED_SURFACE ( )  B_SPLINE_SURFACE ( 3, 2, ( 
 ( #15617, #734, #19621 ),
 ( #10253, #8044, #970 ),
 ( #23388, #15965, #17562 ),
 ( #4627, #6695, #17440 ),
 ( #15496, #14141, #21458 ),
 ( #17680, #4389, #853 ),
 ( #14027, #10016, #15735 ),
 ( #13791, #2568, #23267 ),
 ( #10491, #22923, #2685 ),
 ( #2919, #17920, #8399 ) ),
 .UNSPECIFIED., .F., .F., .F. ) 
 B_SPLINE_SURFACE_WITH_KNOTS ( ( 4, 2, 2, 2, 4 ),
 ( 3, 3 ),
 ( 0.04452332773538494187, 0.04784785823414922090, 0.05117238873291349299, 0.05449691923167777202, 0.05782144973044205105 ),
 ( 0.000000000000000000, 1.000000000000000000 ),
 .UNSPECIFIED. ) 
 GEOMETRIC_REPRESENTATION_ITEM ( )  RATIONAL_B_SPLINE_SURFACE ( (
 ( 1.000000000000000000, 0.8285407536241364834, 1.000000000000000000),
 ( 1.000000000000000000, 0.8326163274272220249, 1.000000000000000000),
 ( 1.000000000000000000, 0.8363775819416653379, 1.000000000000000000),
 ( 1.000000000000000000, 0.8417901505601256273, 1.000000000000000000),
 ( 1.000000000000000000, 0.8433916105626779736, 1.000000000000000000),
 ( 1.000000000000000000, 0.8433912810366652746, 1.000000000000000000),
 ( 1.000000000000000000, 0.8417896183695843249, 1.000000000000000000),
 ( 1.000000000000000000, 0.8363770727355417378, 1.000000000000000000),
 ( 1.000000000000000000, 0.8326160275023869461, 1.000000000000000000),
 ( 1.000000000000000000, 0.8285407536241364834, 1.000000000000000000) ) ) 
 REPRESENTATION_ITEM ( '' )  SURFACE ( )  );
#17862=VECTOR ( 'NONE', #12883, 39.37007874015748143 ) ;
#17864=EDGE_CURVE ( 'NONE', #23410, #5628, #19256, .T. ) ;
#17868=DIRECTION ( 'NONE',  ( 0.000000000000000000, 0.000000000000000000, -1.000000000000000000 ) ) ;
#17874=AXIS2_PLACEMENT_3D ( 'NONE', #18251, #1308, #17772 ) ;
#17875=CARTESIAN_POINT ( 'NONE',  ( 0.000000000000000000, 3.738758431839877614E-19, -0.1016666666666665164 ) ) ;
#17877=CARTESIAN_POINT ( 'NONE',  ( -0.2764156081756484196, 0.1144950937579609918, -0.02624999999999903799 ) ) ;
#17880=CARTESIAN_POINT ( 'NONE',  ( 0.1829869529092248703, 0.2292256185136161140, -0.08186893168610080707 ) ) ;
#17882=CARTESIAN_POINT ( 'NONE',  ( 0.1294417382415921358, -0.3125000000000002220, -0.03319444444444371450 ) ) ;
#17883=DIRECTION ( 'NONE',  ( -0.8660254037844385966, -0.5000000000000001110, 0.000000000000000000 ) ) ;
#17888=CARTESIAN_POINT ( 'NONE',  ( 0.3850752722190822208, 0.3189425652913191467, 0.07813238993955246015 ) ) ;
#17889=ORIENTED_EDGE ( 'NONE', *, *, #24055, .F. ) ;
#17893=CARTESIAN_POINT ( 'NONE',  ( -0.3155070326520293400, -0.1306872919485614626, 0.06923611111111301064 ) ) ;
#17895=B_SPLINE_CURVE_WITH_KNOTS ( 'NONE', 3,
 ( #19551, #14189, #8208, #19797, #22963, #21624, #19671, #4432, #2617, #1020 ),
 .UNSPECIFIED., .F., .F.,
 ( 4, 2, 2, 2, 4 ),
 ( 0.000000000000000000, 0.003270554913819859362, 0.006541109827639718724, 0.009811664741459578953, 0.01308221965527943745 ),
 .UNSPECIFIED. ) ;
#17899=CARTESIAN_POINT ( 'NONE',  ( 0.1954553509668046640, -0.1954553509668047195, 0.005000000000001192726 ) ) ;
#17900=FACE_OUTER_BOUND ( 'NONE', #22366, .T. ) ;
#17903=CARTESIAN_POINT ( 'NONE',  ( 0.2764156081756483641, 0.1144950937579610056, 0.4043055555555599145 ) ) ;
#17904=VERTEX_POINT ( 'NONE', #6329 ) ;
#17915=DIRECTION ( 'NONE',  ( -3.642463991552355691E-15, 0.2773500981126160725, 0.9607689228305223983 ) ) ;
#17920=CARTESIAN_POINT ( 'NONE',  ( -0.4687500000000003331, 0.2570931668155772010, 0.04874733047934005220 ) ) ;
#17922=CARTESIAN_POINT ( 'NONE',  ( -0.1954553509668046640, 0.1954553509668046918, -0.02972222222222128257 ) ) ;
#17926=CARTESIAN_POINT ( 'NONE',  ( 0.000000000000000000, 0.2764156081756484196, 0.1369444444444467002 ) ) ;
#17929=CARTESIAN_POINT ( 'NONE',  ( -0.2977072594216396695, 1.822931211668208286E-17, 0.4093739260883065278 ) ) ;
#17934=CARTESIAN_POINT ( 'NONE',  ( 0.000000000000000000, 0.2764156081756484196, -0.03666666666666578561 ) ) ;
#17935=CARTESIAN_POINT ( 'NONE',  ( 0.000000000000000000, 0.3155070326520292845, 0.3261805555555591374 ) ) ;
#17936=ORIENTED_EDGE ( 'NONE', *, *, #294, .T. ) ;
#17945=TOROIDAL_SURFACE ( 'NONE', #23053, -0.5601250000000235207, 1.200750000000023521 ) ;
#17951=LINE ( 'NONE', #14416, #13816 ) ;
#17955=EDGE_LOOP ( 'NONE', ( #5891, #20021, #18819, #18705, #2543 ) ) ;
#17961=AXIS2_PLACEMENT_3D ( 'NONE', #6449, #8273, #17915 ) ;
#17965=LINE ( 'NONE', #12251, #4540 ) ;
#17969=FACE_OUTER_BOUND ( 'NONE', #4324, .T. ) ;
#17972=VERTEX_POINT ( 'NONE', #13623 ) ;
#17974=EDGE_CURVE ( 'NONE', #21116, #17172, #3357, .T. ) ;
#17978=CARTESIAN_POINT ( 'NONE',  ( -0.4805453480892168949, -0.2624482906435731677, 0.04271891838947986658 ) ) ;
#17984=ORIENTED_EDGE ( 'NONE', *, *, #2481, .T. ) ;
#18000=CARTESIAN_POINT ( 'NONE',  ( -0.1954553509668046640, 0.1954553509668046918, 0.1369444444444467002 ) ) ;
#18003=CARTESIAN_POINT ( 'NONE',  ( 0.2977072594216367274, -5.468793635004571549E-17, -0.08687392608830331320 ) ) ;
#18004=CARTESIAN_POINT ( 'NONE',  ( -0.2998642343065030524, 0.08796414601291395463, -0.1016666666666771329 ) ) ;
#18012=CARTESIAN_POINT ( 'NONE',  ( 0.1306872919485616846, 0.3155070326520292290, 0.04840277777777952234 ) ) ;
#18013=CARTESIAN_POINT ( 'NONE',  ( 0.000000000000000000, 3.738758431839877614E-19, 0.4241666666666665253 ) ) ;
#18015=DIRECTION ( 'NONE',  ( 0.000000000000000000, 1.000000000000000000, 0.000000000000000000 ) ) ;
#18016=CARTESIAN_POINT ( 'NONE',  ( -0.1954553509668046918, -0.1954553509668046640, 0.04666666666666818841 ) ) ;
#18018=CARTESIAN_POINT ( 'NONE',  ( 0.1954553509668046640, -0.1954553509668047195, 0.3383333333333371495 ) ) ;
#18023=DIRECTION ( 'NONE',  ( -1.000000000000000000, 0.000000000000000000, 0.000000000000000000 ) ) ;
#18028=( BOUNDED_CURVE ( )  B_SPLINE_CURVE ( 2, ( #10271, #16352, #14043, #6714, #7084, #21827, #23281, #14278, #3175 ),
 .UNSPECIFIED., .F., .T. ) 
 B_SPLINE_CURVE_WITH_KNOTS ( ( 3, 2, 2, 2, 3 ),
 ( 0.1875000000000000278, 0.1979166666666666852, 0.2083333333333333981, 0.2187500000000000555, 0.2291666666666667407 ),
 .UNSPECIFIED. ) 
 CURVE ( )  GEOMETRIC_REPRESENTATION_ITEM ( )  RATIONAL_B_SPLINE_CURVE ( ( 0.9999999999999997780, 0.9238795325112869605, 1.000000000000000000, 0.9238795325112867385, 1.000000000000000000, 0.9238795325112867385, 1.000000000000000000, 0.9238795325112861834, 1.000000000000000666 ) ) 
 REPRESENTATION_ITEM ( '' )  );
#18038=CARTESIAN_POINT ( 'NONE',  ( 0.2764156081756484196, -5.077672346800151106E-17, 0.1161111111111132049 ) ) ;
#18043=CARTESIAN_POINT ( 'NONE',  ( 0.1144950937579609085, -0.2764156081756484751, 0.1126388888888909395 ) ) ;
#18046=CARTESIAN_POINT ( 'NONE',  ( 0.3125000000000000000, -5.740531871003217465E-17, -0.07138888888888809958 ) ) ;
#18049=CARTESIAN_POINT ( 'NONE',  ( 0.1144950937579609085, -0.2764156081756484751, -0.06097222222222153931 ) ) ;
#18050=CARTESIAN_POINT ( 'NONE',  ( -0.1306872919485614903, 0.3155070326520293400, 0.4407638888888934514 ) ) ;
#18052=ORIENTED_EDGE ( 'NONE', *, *, #521, .T. ) ;
#18060=VERTEX_POINT ( 'NONE', #20980 ) ;
#18077=CARTESIAN_POINT ( 'NONE',  ( -0.3125000000000000000, 3.738758431839877614E-19, -0.1016666666666665164 ) ) ;
#18083=LINE ( 'NONE', #1261, #2250 ) ;
#18095=EDGE_CURVE ( 'NONE', #16949, #23326, #7142, .T. ) ;
#18100=EDGE_LOOP ( 'NONE', ( #8742, #16438, #15579 ) ) ;
#18111=CARTESIAN_POINT ( 'NONE',  ( -0.2527126213443522951, -0.1892291168972398685, -0.1003708124548348124 ) ) ;
#18118=CARTESIAN_POINT ( 'NONE',  ( -0.2764156081756484196, -0.1144950937579609362, 0.2029166666666694652 ) ) ;
#18121=CARTESIAN_POINT ( 'NONE',  ( 0.1595362993632637172, 0.2449369388610288245, -0.08132661693453716034 ) ) ;
#18123=FACE_OUTER_BOUND ( 'NONE', #14204, .T. ) ;
#18127=EDGE_CURVE ( 'NONE', #8682, #17172, #4797, .T. ) ;
#18129=DIRECTION ( 'NONE',  ( 0.4999999999999991673, 0.8660254037844390407, -9.106159978880873451E-16 ) ) ;
#18133=CARTESIAN_POINT ( 'NONE',  ( -0.3155070326520292845, 1.931923388228935888E-17, 0.3435416666666707974 ) ) ;
#18136=CIRCLE ( 'NONE', #4121, 0.3385998376278290256 ) ;
#18137=CARTESIAN_POINT ( 'NONE',  ( 0.08316635082768832066, -0.4932497623273898180, 0.4003041662012485347 ) ) ;
#18140=CARTESIAN_POINT ( 'NONE',  ( 0.2764156081756483641, 0.1144950937579610056, 0.01541666666666794208 ) ) ;
#18148=CARTESIAN_POINT ( 'NONE',  ( -0.4675994362856803477, 0.2849176297964604587, 0.04270874187135767497 ) ) ;
#18159=DIRECTION ( 'NONE',  ( -0.000000000000000000, -0.000000000000000000, -1.000000000000000000 ) ) ;
#18160=CARTESIAN_POINT ( 'NONE',  ( -0.1144950937579609918, -0.2764156081756484196, 0.2098611111111139960 ) ) ;
#18168=CARTESIAN_POINT ( 'NONE',  ( 0.01197057051269882245, 0.2890469299669685688, 0.4003459737656249184 ) ) ;
#18171=CARTESIAN_POINT ( 'NONE',  ( 0.6209078282299125284, 1.869379215919938807E-19, -0.01219352927422984872 ) ) ;
#18172=CARTESIAN_POINT ( 'NONE',  ( 0.1954553509668046640, -0.1954553509668047195, -0.05055555555555479863 ) ) ;
#18173=ORIENTED_EDGE ( 'NONE', *, *, #17176, .T. ) ;
#18174=ORIENTED_EDGE ( 'NONE', *, *, #11723, .F. ) ;
#18176=CARTESIAN_POINT ( 'NONE',  ( 0.05482473137696310811, 0.5228958406531273306, 0.05347130368200837119 ) ) ;
#18233=CARTESIAN_POINT ( 'NONE',  ( 0.1294417382415921358, -0.3125000000000002220, -0.08874999999999971800 ) ) ;
#18237=CARTESIAN_POINT ( 'NONE',  ( 0.2764156081756483641, -0.1144950937579611167, 0.3348611111111149952 ) ) ;
#18240=CARTESIAN_POINT ( 'NONE',  ( -0.006542161132012624253, -0.5374887588746249945, 0.3892820121258429023 ) ) ;
#18241=CARTESIAN_POINT ( 'NONE',  ( 0.000000000000000000, 0.3308333333333332571, 0.4425000000000000044 ) ) ;
#18248=ORIENTED_EDGE ( 'NONE', *, *, #11663, .F. ) ;
#18250=CARTESIAN_POINT ( 'NONE',  ( 0.3155070326520292290, 0.1306872919485615736, 0.1525694444444470055 ) ) ;
#18251=CARTESIAN_POINT ( 'NONE',  ( 0.000000000000000000, 0.000000000000000000, -0.1199999999999999956 ) ) ;
#18254=CARTESIAN_POINT ( 'NONE',  ( 0.009374999999999975367, -0.5358532185916218271, 0.3779506566538943790 ) ) ;
#18259=CARTESIAN_POINT ( 'NONE',  ( 0.2764156081756483641, 0.1144950937579610056, 0.3487500000000040012 ) ) ;
#18275=CARTESIAN_POINT ( 'NONE',  ( -0.009374999999999905978, -0.5358532185916218271, 0.06112444011295371793 ) ) ;
#18276=ORIENTED_EDGE ( 'NONE', *, *, #5497, .F. ) ;
#18280=CARTESIAN_POINT ( 'NONE',  ( 0.1954553509668046640, -0.1954553509668047195, 0.3313888888888926743 ) ) ;
#18282=CARTESIAN_POINT ( 'NONE',  ( -0.4581189881604794678, 0.2644951211353315235, 0.3941886329748525153 ) ) ;
#18288=CARTESIAN_POINT ( 'NONE',  ( 0.3385998376278290256, 4.184039657745742702E-17, -0.1199999999999999956 ) ) ;
#18291=CARTESIAN_POINT ( 'NONE',  ( -0.2764156081756484196, 1.692557448933383907E-17, -0.02277777777777679341 ) ) ;
#18292=CARTESIAN_POINT ( 'NONE',  ( -0.2764156081756484196, 0.1144950937579609918, -0.01930555555555454883 ) ) ;
#18293=ORIENTED_EDGE ( 'NONE', *, *, #14666, .T. ) ;
#18294=ORIENTED_EDGE ( 'NONE', *, *, #10311, .F. ) ;
#18295=CARTESIAN_POINT ( 'NONE',  ( 0.3143659348029790301, 0.3723832402019556231, 0.07159583130656671512 ) ) ;
#18304=VERTEX_POINT ( 'NONE', #20326 ) ;
#18343=CARTESIAN_POINT ( 'NONE',  ( 0.4645997322662998585, -0.2720228281466835485, 0.05892894635879270676 ) ) ;
#18350=CARTESIAN_POINT ( 'NONE',  ( -0.4687500000000003886, 0.2598076211353315679, 0.3779506566538943790 ) ) ;
#18357=CARTESIAN_POINT ( 'NONE',  ( 0.1144950937579609085, -0.2764156081756484751, 0.2168055555555584712 ) ) ;
#18360=CARTESIAN_POINT ( 'NONE',  ( 0.07165243469739802917, -0.2702856358549929894, 0.3907475393308576517 ) ) ;
#18367=ORIENTED_EDGE ( 'NONE', *, *, #23865, .F. ) ;
#18371=CARTESIAN_POINT ( 'NONE',  ( 0.3155070326520292290, -0.1306872919485616569, 0.3678472222222264887 ) ) ;
#18373=CARTESIAN_POINT ( 'NONE',  ( 0.1959149649064702292, -0.4281543196382478489, 0.4181366382341597521 ) ) ;
#18377=CARTESIAN_POINT ( 'NONE',  ( -0.1954553509668046918, -0.1954553509668046640, 0.1577777777777801815 ) ) ;
#18390=CARTESIAN_POINT ( 'NONE',  ( -0.004206913933137605005, 0.5383631510497778327, 0.04698599556840143965 ) ) ;
#18391=VERTEX_POINT ( 'NONE', #18617 ) ;
#18396=ADVANCED_FACE ( 'NONE', ( #11065 ), #14855, .F. ) ;
#18399=LINE ( 'NONE', #100, #642 ) ;
#18400=CARTESIAN_POINT ( 'NONE',  ( -0.1954553509668046640, 0.1954553509668046918, 0.2480555555555586933 ) ) ;
#18404=CARTESIAN_POINT ( 'NONE',  ( 0.03651601414450977162, -0.2739930093161348501, 0.3880822748423153890 ) ) ;
#18407=CARTESIAN_POINT ( 'NONE',  ( -0.2209708691207961095, 0.2209708691207961373, 0.1716666666666694097 ) ) ;
#18410=CARTESIAN_POINT ( 'NONE',  ( 0.1144950937579609085, -0.2764156081756484751, -0.05402777777777704321 ) ) ;
#18411=ORIENTED_EDGE ( 'NONE', *, *, #7472, .T. ) ;
#18412=ORIENTED_EDGE ( 'NONE', *, *, #14678, .F. ) ;
#18418=AXIS2_PLACEMENT_3D ( 'NONE', #5246, #6969, #11110 ) ;
#18421=EDGE_CURVE ( 'NONE', #4536, #12538, #557, .T. ) ;
#18430=AXIS2_PLACEMENT_3D ( 'NONE', #6224, #13688, #21105 ) ;
#18431=CARTESIAN_POINT ( 'NONE',  ( -0.4723836327791814949, 0.2801952116499777934, 0.04193567535760836518 ) ) ;
#18445=DIRECTION ( 'NONE',  ( -0.000000000000000000, -0.000000000000000000, -1.000000000000000000 ) ) ;
#18466=ORIENTED_EDGE ( 'NONE', *, *, #14666, .F. ) ;
#18470=VECTOR ( 'NONE', #13939, 39.37007874015748143 ) ;
#18475=CARTESIAN_POINT ( 'NONE',  ( 0.1954553509668047195, 0.1954553509668046085, 0.2897222222222257115 ) ) ;
#18479=CARTESIAN_POINT ( 'NONE',  ( 0.03651601414450977162, -0.2739930093161348501, 0.3880822748423153890 ) ) ;
#18490=ORIENTED_EDGE ( 'NONE', *, *, #20927, .F. ) ;
#18491=CARTESIAN_POINT ( 'NONE',  ( -0.2230971623002954152, -0.2230971623002953874, 0.2949305555555592484 ) ) ;
#18497=CARTESIAN_POINT ( 'NONE',  ( 0.2764156081756483641, 0.1144950937579610056, 0.1820833333333359283 ) ) ;
#18514=ADVANCED_FACE ( 'NONE', ( #13512 ), #13976, .F. ) ;
#18518=CARTESIAN_POINT ( 'NONE',  ( 0.2764156081756483641, -0.1144950937579611167, 0.1681944444444469777 ) ) ;
#18522=CARTESIAN_POINT ( 'NONE',  ( 0.000000000000000000, 0.2764156081756484196, 0.3591666666666706309 ) ) ;
#18526=CARTESIAN_POINT ( 'NONE',  ( -0.3125000000000000000, 1.913510623667739771E-17, 0.1786111111111139127 ) ) ;
#18528=CARTESIAN_POINT ( 'NONE',  ( 0.04615996209784178905, 0.5146154108223025547, 0.3902123106865083013 ) ) ;
#18529=CARTESIAN_POINT ( 'NONE',  ( -0.1954553509668046640, 0.1954553509668046918, -0.02277777777777679341 ) ) ;
#18549=CIRCLE ( 'NONE', #23202, 0.3125000000000000000 ) ;
#18551=DIRECTION ( 'NONE',  ( 1.000000000000000000, 0.000000000000000000, 0.000000000000000000 ) ) ;
#18560=CARTESIAN_POINT ( 'NONE',  ( 0.2230971623002953874, -0.2230971623002954429, -0.08354166666666636154 ) ) ;
#18561=CARTESIAN_POINT ( 'NONE',  ( -0.4593750000000005329, -0.2760455974562900372, 0.06112444011295364160 ) ) ;
#18573=DIRECTION ( 'NONE',  ( -0.000000000000000000, -0.000000000000000000, 1.000000000000000000 ) ) ;
#18593=CARTESIAN_POINT ( 'NONE',  ( 0.3125000000000002220, -0.1294417382415921358, -0.08180555555555521496 ) ) ;
#18595=ORIENTED_EDGE ( 'NONE', *, *, #19502, .T. ) ;
#18597=VERTEX_POINT ( 'NONE', #16500 ) ;
#18599=CARTESIAN_POINT ( 'NONE',  ( 0.1954553509668047195, 0.1954553509668046085, 0.1786111111111137462 ) ) ;
#18604=EDGE_CURVE ( 'NONE', #1635, #19685, #23864, .T. ) ;
#18607=VECTOR ( 'NONE', #22495, 39.37007874015748143 ) ;
#18612=ORIENTED_EDGE ( 'NONE', *, *, #13651, .T. ) ;
#18614=CARTESIAN_POINT ( 'NONE',  ( 0.000000000000000000, 0.3155070326520292845, 0.2185416666666697982 ) ) ;
#18617=CARTESIAN_POINT ( 'NONE',  ( -0.009374999999999907713, -0.5358532185916218271, 0.3779506566538943235 ) ) ;
#18620=CARTESIAN_POINT ( 'NONE',  ( -0.1954553509668046918, -0.1954553509668046640, 0.3244444444444481435 ) ) ;
#18626=CARTESIAN_POINT ( 'NONE',  ( 0.000000000000000000, 0.000000000000000000, 1.326383476483184332 ) ) ;
#18635=CARTESIAN_POINT ( 'NONE',  ( -0.3856318672988793272, -0.3186212149721687203, 0.4002893343786020908 ) ) ;
#18639=CARTESIAN_POINT ( 'NONE',  ( 0.2764156081756483641, -0.1144950937579611167, 0.2793055555555589153 ) ) ;
#18640=ADVANCED_FACE ( 'NONE', ( #17969 ), #15683, .F. ) ;
#18641=CARTESIAN_POINT ( 'NONE',  ( -0.4687500000000003886, -0.2598076211353319009, 0.3779506566538942125 ) ) ;
#18650=CARTESIAN_POINT ( 'NONE',  ( -0.1144950937579609779, 0.2764156081756484196, -0.08180555555555503455 ) ) ;
#18659=DIRECTION ( 'NONE',  ( 1.000000000000000000, 0.000000000000000000, 0.000000000000000000 ) ) ;
#18667=CIRCLE ( 'NONE', #10124, 0.01875000000000000625 ) ;
#18670=CARTESIAN_POINT ( 'NONE',  ( -0.4621660567954124499, 0.2744341800641371676, 0.05971082423030620728 ) ) ;
#18678=CARTESIAN_POINT ( 'NONE',  ( 0.3155070326520292290, 0.1306872919485615736, 0.03798611111111236532 ) ) ;
#18680=CARTESIAN_POINT ( 'NONE',  ( -0.01848103877824596938, -0.5441716683897390716, 0.04413116910601656145 ) ) ;
#18681=FACE_OUTER_BOUND ( 'NONE', #19354, .T. ) ;
#18688=CIRCLE ( 'NONE', #6621, 0.01874999999999999237 ) ;
#18689=CARTESIAN_POINT ( 'NONE',  ( -0.3125000000000000000, 0.000000000000000000, 1.326383476483184332 ) ) ;
#18691=ORIENTED_EDGE ( 'NONE', *, *, #5432, .F. ) ;
#18701=CARTESIAN_POINT ( 'NONE',  ( -0.2774634594257631148, -0.1150700753241015728, 0.4115780677775827678 ) ) ;
#18705=ORIENTED_EDGE ( 'NONE', *, *, #226, .F. ) ;
#18706=B_SPLINE_CURVE_WITH_KNOTS ( 'NONE', 3,
 ( #17442, #9772, #20858, #2454 ),
 .UNSPECIFIED., .F., .F.,
 ( 4, 4 ),
 ( 0.000000000000000000, 0.002245614500286350051 ),
 .UNSPECIFIED. ) ;
#18708=AXIS2_PLACEMENT_3D ( 'NONE', #9822, #19555, #8332 ) ;
#18709=LINE ( 'NONE', #2007, #5884 ) ;
#18713=EDGE_CURVE ( 'NONE', #18597, #14213, #1365, .T. ) ;
#18714=ORIENTED_EDGE ( 'NONE', *, *, #6455, .T. ) ;
#18716=DIRECTION ( 'NONE',  ( -1.000000000000000000, 0.000000000000000000, 0.000000000000000000 ) ) ;
#18719=CARTESIAN_POINT ( 'NONE',  ( -0.4687500000000004441, -0.08745052389986680830, 0.08858773447093010178 ) ) ;
#18720=CARTESIAN_POINT ( 'NONE',  ( 0.3101024306885722948, -0.3622281555308699552, 0.08858850926231194578 ) ) ;
#18726=CIRCLE ( 'NONE', #8201, 0.01874999999999999931 ) ;
#18734=CARTESIAN_POINT ( 'NONE',  ( -0.3155070326520292845, 1.931923388228935888E-17, 0.3990972222222267662 ) ) ;
#18741=CARTESIAN_POINT ( 'NONE',  ( 0.1954553509668046640, -0.1954553509668047195, 0.1091666666666687158 ) ) ;
#18743=CARTESIAN_POINT ( 'NONE',  ( -0.1144950937579609779, 0.2764156081756484196, 0.1404166666666689378 ) ) ;
#18745=CARTESIAN_POINT ( 'NONE',  ( -0.01848103877826416663, -0.5441716683897284135, 0.04413116910602139092 ) ) ;
#18760=CARTESIAN_POINT ( 'NONE',  ( 0.000000000000000000, 0.3155070326520292845, -0.1147916666666661950 ) ) ;
#18763=EDGE_CURVE ( 'NONE', #549, #10191, #16513, .T. ) ;
#18764=VERTEX_POINT ( 'NONE', #8688 ) ;
#18769=CARTESIAN_POINT ( 'NONE',  ( 0.4226370775080297015, 0.2972562468964968785, 0.3901966308178841936 ) ) ;
#18770=CARTESIAN_POINT ( 'NONE',  ( 0.1144950937579609085, -0.2764156081756484751, 0.1681944444444469222 ) ) ;
#18781=CARTESIAN_POINT ( 'NONE',  ( -0.3125000000000000000, 1.913510623667739771E-17, 0.1230555555555578606 ) ) ;
#18784=CARTESIAN_POINT ( 'NONE',  ( 0.000000000000000000, 0.3125000000000000000, -0.001944444444443116891 ) ) ;
#18785=( NAMED_UNIT ( * ) SI_UNIT ( $, .STERADIAN. ) SOLID_ANGLE_UNIT ( ) );
#18786=CARTESIAN_POINT ( 'NONE',  ( 0.4581189881604794123, 0.2644951211353319120, 0.3941886329748525153 ) ) ;
#18792=CARTESIAN_POINT ( 'NONE',  ( 0.1954553509668047195, 0.1954553509668046085, 0.07444444444444621445 ) ) ;
#18796=DIRECTION ( 'NONE',  ( 0.000000000000000000, 0.000000000000000000, 1.000000000000000000 ) ) ;
#18797=CARTESIAN_POINT ( 'NONE',  ( -0.3124999999999993894, -0.1294417382415926909, 0.1751388888888912587 ) ) ;
#18799=CARTESIAN_POINT ( 'NONE',  ( -3.863846776457871776E-17, -0.3155070326520292845, 0.02062500000000112854 ) ) ;
#18811=CARTESIAN_POINT ( 'NONE',  ( -0.01848103877824615326, 0.5441716683897390716, 0.04413116910601658227 ) ) ;
#18818=CARTESIAN_POINT ( 'NONE',  ( -0.01239990016104709422, -0.3069330571738640989, -0.09589278090496755613 ) ) ;
#18819=ORIENTED_EDGE ( 'NONE', *, *, #3643, .F. ) ;
#18820=B_SPLINE_CURVE_WITH_KNOTS ( 'NONE', 3,
 ( #14718, #1653, #7150, #9217, #24078, #13138, #18719, #22132, #3361, #21894 ),
 .UNSPECIFIED., .F., .F.,
 ( 4, 2, 2, 2, 4 ),
 ( 0.000000000000000000, 0.003321853704944119183, 0.006643707409888238366, 0.009965561114832356682, 0.01328741481977647673 ),
 .UNSPECIFIED. ) ;
#18829=CARTESIAN_POINT ( 'NONE',  ( 0.3100543665041115560, 0.3622559054007069013, 0.4143868288130764799 ) ) ;
#18830=CARTESIAN_POINT ( 'NONE',  ( 0.4500000000000003442, 0.2598076211353318454, 0.3779506566538943235 ) ) ;
#18851=EDGE_CURVE ( 'NONE', #4238, #7496, #5562, .T. ) ;
#18862=CARTESIAN_POINT ( 'NONE',  ( 0.000000000000000000, 0.2764156081756484196, 0.2411111111111142458 ) ) ;
#18864=CARTESIAN_POINT ( 'NONE',  ( -0.2764156081756484196, 1.692557448933383907E-17, 0.3730555555555596925 ) ) ;
#18869=EDGE_CURVE ( 'NONE', #5628, #9027, #12964, .T. ) ;
#18873=ADVANCED_FACE ( 'NONE', ( #11133 ), #14620, .F. ) ;
#18885=CARTESIAN_POINT ( 'NONE',  ( -0.3155070326520293400, -0.1306872919485614626, -0.09743055555555497904 ) ) ;
#18886=AXIS2_PLACEMENT_3D ( 'NONE', #703, #10106, #17411 ) ;
#18888=FACE_OUTER_BOUND ( 'NONE', #15286, .T. ) ;
#18893=CARTESIAN_POINT ( 'NONE',  ( 0.2764156081756483641, 0.1144950937579610056, -0.09569444444444405451 ) ) ;
#18896=CARTESIAN_POINT ( 'NONE',  ( -0.2764156081756484196, -0.1144950937579609362, 0.2654166666666699093 ) ) ;
#18897=VERTEX_POINT ( 'NONE', #10269 ) ;
#18905=CYLINDRICAL_SURFACE ( 'NONE', #11047, 0.3125000000000000000 ) ;
#18906=ORIENTED_EDGE ( 'NONE', *, *, #22273, .T. ) ;
#18914=CARTESIAN_POINT ( 'NONE',  ( -0.4687500000000003886, 0.2598076211353315124, 0.3779506566538943790 ) ) ;
#18918=ORIENTED_EDGE ( 'NONE', *, *, #12511, .T. ) ;
#18920=CARTESIAN_POINT ( 'NONE',  ( 0.2764156081756484196, -5.077672346800151106E-17, -0.04361111111111028865 ) ) ;
#18922=ORIENTED_EDGE ( 'NONE', *, *, #1692, .F. ) ;
#18929=CARTESIAN_POINT ( 'NONE',  ( 0.2230971623002954429, 0.2230971623002953319, 0.09701388888889063422 ) ) ;
#18930=CARTESIAN_POINT ( 'NONE',  ( -0.4254318749130439059, -0.3089257318245043349, 0.05347049744909274094 ) ) ;
#18931=PLANE ( 'NONE',  #21421 ) ;
#18945=CARTESIAN_POINT ( 'NONE',  ( -0.2742360776603882666, -0.1498359893665253684, -0.1016666666666679597 ) ) ;
#18950=ORIENTED_EDGE ( 'NONE', *, *, #479, .T. ) ;
#18958=ORIENTED_EDGE ( 'NONE', *, *, #17974, .F. ) ;
#18963=( BOUNDED_SURFACE ( )  B_SPLINE_SURFACE ( 3, 2, ( 
 ( #21716, #12461, #15985 ),
 ( #19764, #3060, #10625 ),
 ( #16108, #19882, #5364 ),
 ( #24012, #3900, #11224 ),
 ( #7676, #12829, #15126 ),
 ( #5730, #3656, #3417 ),
 ( #7201, #7322, #241 ),
 ( #16472, #7440, #20484 ),
 ( #11102, #24125, #9391 ),
 ( #20248, #114, #22552 ),
 ( #12711, #5604, #9268 ),
 ( #16708, #11345, #20365 ) ),
 .UNSPECIFIED., .F., .F., .T. ) 
 B_SPLINE_SURFACE_WITH_KNOTS ( ( 4, 2, 2, 2, 2, 4 ),
 ( 3, 3 ),
 ( 0.04583429251981868680, 0.04917046297897018775, 0.05083854820854594170, 0.05250663343812168871, 0.05584280389727318966, 0.05917897435642469062 ),
 ( 0.000000000000000000, 1.000000000000000000 ),
 .UNSPECIFIED. ) 
 GEOMETRIC_REPRESENTATION_ITEM ( )  RATIONAL_B_SPLINE_SURFACE ( (
 ( 1.000000000000000000, 0.8464669816041905381, 1.000000000000000000),
 ( 1.000000000000000000, 0.8516145702047686061, 1.000000000000000000),
 ( 1.000000000000000000, 0.8565400046562395842, 1.000000000000000000),
 ( 1.000000000000000000, 0.8619820649909384347, 1.000000000000000000),
 ( 1.000000000000000000, 0.8634666681419451706, 1.000000000000000000),
 ( 1.000000000000000000, 0.8654947235244276893, 1.000000000000000000),
 ( 1.000000000000000000, 0.8660222433461404190, 1.000000000000000000),
 ( 1.000000000000000000, 0.8660316815622557396, 1.000000000000000000),
 ( 1.000000000000000000, 0.8638737604836346229, 1.000000000000000000),
 ( 1.000000000000000000, 0.8566366026603471351, 1.000000000000000000),
 ( 1.000000000000000000, 0.8516183347815020621, 1.000000000000000000),
 ( 1.000000000000000000, 0.8464669816041905381, 1.000000000000000000) ) ) 
 REPRESENTATION_ITEM ( '' )  SURFACE ( )  );
#18965=CARTESIAN_POINT ( 'NONE',  ( -0.3832388449590500290, -0.3084783300535373640, 0.4166279060364119768 ) ) ;
#18977=DIRECTION ( 'NONE',  ( 0.000000000000000000, -0.000000000000000000, -1.000000000000000000 ) ) ;
#18981=CARTESIAN_POINT ( 'NONE',  ( 0.006528205157002813994, -0.5487477722931476398, 0.04212966708837326962 ) ) ;
#18984=CARTESIAN_POINT ( 'NONE',  ( 0.1144950937579609085, -0.2764156081756484751, 0.2168055555555584990 ) ) ;
#18986=CARTESIAN_POINT ( 'NONE',  ( 0.000000000000000000, 0.2764156081756484196, 0.4702777777777826795 ) ) ;
#18999=CARTESIAN_POINT ( 'NONE',  ( 0.000000000000000000, 1.869379215919938807E-19, -0.01219352927422984872 ) ) ;
#19000=ORIENTED_EDGE ( 'NONE', *, *, #12786, .T. ) ;
#19001=CARTESIAN_POINT ( 'NONE',  ( 0.4687500000000002776, -0.2598076211353317344, 0.3779506566538943235 ) ) ;
#19007=CARTESIAN_POINT ( 'NONE',  ( -0.1306872919485614903, 0.3155070326520293400, -0.1668749999999999123 ) ) ;
#19017=CARTESIAN_POINT ( 'NONE',  ( -0.1144950937579609918, -0.2764156081756484196, 0.1612500000000023914 ) ) ;
#19025=CARTESIAN_POINT ( 'NONE',  ( -0.4453125000000000000, -5.968957943988233420E-17, 0.4425000000000000044 ) ) ;
#19032=CARTESIAN_POINT ( 'NONE',  ( 0.3124999999999999445, 0.1294417382415923023, -0.01236111111110986711 ) ) ;
#19034=CARTESIAN_POINT ( 'NONE',  ( -3.385114897866767815E-17, -0.2764156081756484196, -0.1199999999999997735 ) ) ;
#19040=AXIS2_PLACEMENT_3D ( 'NONE', #19211, #683, #2635 ) ;
#19045=CARTESIAN_POINT ( 'NONE',  ( -0.2230971623002953874, 0.2230971623002954152, 0.1109027777777796125 ) ) ;
#19050=ORIENTED_EDGE ( 'NONE', *, *, #14108, .T. ) ;
#19066=ORIENTED_EDGE ( 'NONE', *, *, #6236, .T. ) ;
#19074=DIRECTION ( 'NONE',  ( -0.000000000000000000, -0.000000000000000000, -1.000000000000000000 ) ) ;
#19075=CARTESIAN_POINT ( 'NONE',  ( -0.2764156081756484196, 0.1144950937579609918, 0.4181944444444490872 ) ) ;
#19077=CARTESIAN_POINT ( 'NONE',  ( -0.1943163256447902609, -0.4290772944462951655, 0.4279515871991128040 ) ) ;
#19084=ORIENTED_EDGE ( 'NONE', *, *, #4798, .T. ) ;
#19086=ORIENTED_EDGE ( 'NONE', *, *, #11214, .F. ) ;
#19095=( BOUNDED_CURVE ( )  B_SPLINE_CURVE ( 2, ( #4026, #4267, #15248, #20729, #4383, #11716, #20612, #2563, #18781 ),
 .UNSPECIFIED., .F., .F. ) 
 B_SPLINE_CURVE_WITH_KNOTS ( ( 3, 2, 2, 2, 3 ),
 ( 0.4479166666666667407, 0.4583333333333334259, 0.4687500000000001110, 0.4791666666666667962, 0.4895833333333334814 ),
 .UNSPECIFIED. ) 
 CURVE ( )  GEOMETRIC_REPRESENTATION_ITEM ( )  RATIONAL_B_SPLINE_CURVE ( ( 0.9999999999999995559, 0.9238795325112871826, 1.000000000000000000, 0.9238795325112867385, 1.000000000000000000, 0.9238795325112867385, 1.000000000000000000, 0.9238795325112859613, 1.000000000000000888 ) ) 
 REPRESENTATION_ITEM ( '' )  );
#19096=CARTESIAN_POINT ( 'NONE',  ( 0.2721215285213450241, -0.3841564396211945565, 0.07944889038202707088 ) ) ;
#19097=CARTESIAN_POINT ( 'NONE',  ( 0.2764156081756484196, -5.077672346800151106E-17, 0.2272222222222252119 ) ) ;
#19099=CARTESIAN_POINT ( 'NONE',  ( 0.1144950937579609085, -0.2764156081756484751, 0.3904166666666708529 ) ) ;
#19106=CARTESIAN_POINT ( 'NONE',  ( -0.3125000000000000000, 1.913510623667739771E-17, 0.3383333333333369830 ) ) ;
#19117=EDGE_CURVE ( 'NONE', #3680, #15369, #23004, .T. ) ;
#19118=CARTESIAN_POINT ( 'NONE',  ( 0.4788584550258475625, -0.2689697488930788416, 0.04193801346286649828 ) ) ;
#19119=CARTESIAN_POINT ( 'NONE',  ( 0.000000000000000000, 0.2764156081756484196, 0.4077777777777822354 ) ) ;
#19127=CARTESIAN_POINT ( 'NONE',  ( -0.2464202454315806146, -0.1619151084082731396, -0.08350906156777793132 ) ) ;
#19128=CARTESIAN_POINT ( 'NONE',  ( 0.000000000000000000, 0.2764156081756484196, 0.1925000000000026690 ) ) ;
#19130=CARTESIAN_POINT ( 'NONE',  ( 0.01848103877824584448, 0.5441716683897389606, 0.04413116910601658227 ) ) ;
#19140=CARTESIAN_POINT ( 'NONE',  ( 0.3062750282812972125, 0.05890668782135718290, 0.4221389973272440810 ) ) ;
#19147=CARTESIAN_POINT ( 'NONE',  ( 0.1144950937579609085, -0.2764156081756484751, -0.1165277777777775636 ) ) ;
#19151=CARTESIAN_POINT ( 'NONE',  ( 0.009375000000000072511, -0.5358532185916218271, 0.4425000000000000044 ) ) ;
#19156=DIRECTION ( 'NONE',  ( 0.000000000000000000, 0.000000000000000000, -1.000000000000000000 ) ) ;
#19158=CARTESIAN_POINT ( 'NONE',  ( -0.3155070326520292845, 1.931923388228935888E-17, 0.2289583333333361503 ) ) ;
#19160=EDGE_CURVE ( 'NONE', #17972, #8592, #14369, .T. ) ;
#19161=FACE_OUTER_BOUND ( 'NONE', #5951, .T. ) ;
#19184=CARTESIAN_POINT ( 'NONE',  ( 0.006542161132012710989, 0.5374887588746247724, 0.3892820121258430688 ) ) ;
#19185=DIRECTION ( 'NONE',  ( 0.000000000000000000, 1.000000000000000000, 0.000000000000000000 ) ) ;
#19197=EDGE_LOOP ( 'NONE', ( #2624, #22381, #9919, #18950 ) ) ;
#19205=ORIENTED_EDGE ( 'NONE', *, *, #14841, .F. ) ;
#19206=CARTESIAN_POINT ( 'NONE',  ( 0.4788479876972290827, 0.2689986204937583336, 0.04193567535760913539 ) ) ;
#19211=CARTESIAN_POINT ( 'NONE',  ( -0.01874999999999989869, -0.5520911949125800744, 0.06112444011295371793 ) ) ;
#19212=CARTESIAN_POINT ( 'NONE',  ( 0.2773501192371399804, -0.3936383244008247462, 0.07440066028685882182 ) ) ;
#19213=CARTESIAN_POINT ( 'NONE',  ( -0.2764156081756484196, 1.692557448933383907E-17, 0.3105555555555591929 ) ) ;
#19215=CARTESIAN_POINT ( 'NONE',  ( -0.1954553509668046918, -0.1954553509668046640, -0.07138888888888827999 ) ) ;
#19218=CARTESIAN_POINT ( 'NONE',  ( 0.003294150194310348223, -0.5383638965977115554, 0.05893128447555213284 ) ) ;
#19221=CARTESIAN_POINT ( 'NONE',  ( -0.1294417382415922746, -0.3125000000000000000, 0.3487500000000036682 ) ) ;
#19225=DIRECTION ( 'NONE',  ( 0.000000000000000000, 0.000000000000000000, 1.000000000000000000 ) ) ;
#19231=ORIENTED_EDGE ( 'NONE', *, *, #8863, .T. ) ;
#19235=DIRECTION ( 'NONE',  ( 0.000000000000000000, 0.000000000000000000, -1.000000000000000000 ) ) ;
#19236=CARTESIAN_POINT ( 'NONE',  ( -0.2764156081756484196, 1.692557448933383907E-17, 0.4216666666666711860 ) ) ;
#19244=CARTESIAN_POINT ( 'NONE',  ( -0.05416907386917569484, -0.2729753724328098374, -0.06690562264081034716 ) ) ;
#19245=CARTESIAN_POINT ( 'NONE',  ( 0.1954553509668046640, -0.1954553509668047195, 0.2827777777777811807 ) ) ;
#19248=FACE_OUTER_BOUND ( 'NONE', #13587, .T. ) ;
#19255=CARTESIAN_POINT ( 'NONE',  ( -0.4228029066818159709, 0.2971605053783716865, 0.3901413544830086844 ) ) ;
#19256=LINE ( 'NONE', #23380, #11834 ) ;
#19259=CARTESIAN_POINT ( 'NONE',  ( 0.4620259694561523744, 0.2880908832651560281, 0.04413116910601654758 ) ) ;
#19261=CARTESIAN_POINT ( 'NONE',  ( 0.4620259694561523744, -0.2880908832651558615, 0.04413116910601658921 ) ) ;
#19262=CARTESIAN_POINT ( 'NONE',  ( 0.2530612899223194101, -0.3951608735071495682, 0.4181572966874575470 ) ) ;
#19266=CARTESIAN_POINT ( 'NONE',  ( 0.2764156081756483641, -0.1144950937579611167, -0.1095833333333330328 ) ) ;
#19269=CARTESIAN_POINT ( 'NONE',  ( -0.1954553509668046918, -0.1954553509668046640, 0.04666666666666818841 ) ) ;
#19276=CARTESIAN_POINT ( 'NONE',  ( -0.3125000000000002776, 0.1294417382415919970, 0.001527777777778780745 ) ) ;
#19277=CARTESIAN_POINT ( 'NONE',  ( 0.3155070326520292845, -5.795770164686806123E-17, 0.09006944444444611730 ) ) ;
#19278=EDGE_LOOP ( 'NONE', ( #10220, #16399, #2392, #6365 ) ) ;
#19286=CIRCLE ( 'NONE', #7212, 0.01875000000000000971 ) ;
#19291=CARTESIAN_POINT ( 'NONE',  ( 0.3125000000000009437, -0.1294417382415913309, 0.2515277777777808477 ) ) ;
#19294=CARTESIAN_POINT ( 'NONE',  ( 0.1309139991617564724, -0.2436136748879755842, 0.3880822748423154445 ) ) ;
#19303=ORIENTED_EDGE ( 'NONE', *, *, #8564, .T. ) ;
#19308=CARTESIAN_POINT ( 'NONE',  ( 0.1366666852802012888, 0.4623613298294839691, 0.4215068951509038930 ) ) ;
#19309=DIRECTION ( 'NONE',  ( 0.000000000000000000, 0.000000000000000000, -1.000000000000000000 ) ) ;
#19316=B_SPLINE_CURVE_WITH_KNOTS ( 'NONE', 3,
 ( #18786, #19388, #19745, #10377, #11848, #2798, #15849, #23035, #23148, #19504, #4741, #12092 ),
 .UNSPECIFIED., .F., .F.,
 ( 4, 2, 2, 2, 2, 4 ),
 ( 0.000000000000000000, 0.003384026746073586205, 0.006768053492147172411, 0.008460066865183961393, 0.01015208023822075124, 0.01353610698429432921 ),
 .UNSPECIFIED. ) ;
#19317=FACE_OUTER_BOUND ( 'NONE', #7251, .T. ) ;
#19320=CARTESIAN_POINT ( 'NONE',  ( -0.1948874010148252123, -0.4287475839276986278, 0.4171140917644005630 ) ) ;
#19322=CIRCLE ( 'NONE', #22433, 0.01874999999999997155 ) ;
#19336=VECTOR ( 'NONE', #6738, 39.37007874015748854 ) ;
#19338=CARTESIAN_POINT ( 'NONE',  ( -0.4687500000000003886, 0.08851153507826334255, 0.4142570404818415319 ) ) ;
#19339=CARTESIAN_POINT ( 'NONE',  ( -0.4687500000000004441, -0.2174879564497122775, 0.3901672915530228214 ) ) ;
#19341=CARTESIAN_POINT ( 'NONE',  ( -0.1144950937579609918, -0.2764156081756484196, 0.1543055555555579716 ) ) ;
#19343=CARTESIAN_POINT ( 'NONE',  ( 0.1144950937579611444, 0.2764156081756483641, 0.01541666666666797678 ) ) ;
#19350=DIRECTION ( 'NONE',  ( 1.000000000000000000, 0.000000000000000000, 0.000000000000000000 ) ) ;
#19354=EDGE_LOOP ( 'NONE', ( #9739, #8473, #12179, #17735 ) ) ;
#19356=CARTESIAN_POINT ( 'NONE',  ( 0.1294417382415924134, 0.3124999999999999445, 0.2098611111111137462 ) ) ;
#19360=CARTESIAN_POINT ( 'NONE',  ( -0.1306872919485615459, -0.3155070326520293400, 0.02062500000000154141 ) ) ;
#19361=CARTESIAN_POINT ( 'NONE',  ( 0.2721904660997503944, 0.3841166384917397703, 0.07944544255957622370 ) ) ;
#19366=CARTESIAN_POINT ( 'NONE',  ( -0.2764156081756484196, 0.1144950937579609918, -0.1304166666666665420 ) ) ;
#19368=CARTESIAN_POINT ( 'NONE',  ( -0.3006586688675891850, -0.04349558104364664030, -0.09283059900161595712 ) ) ;
#19369=CARTESIAN_POINT ( 'NONE',  ( 0.2764156081756483641, -0.1144950937579611167, 0.3418055555555594704 ) ) ;
#19370=ORIENTED_EDGE ( 'NONE', *, *, #18421, .F. ) ;
#19386=CARTESIAN_POINT ( 'NONE',  ( 0.009375000000000065573, -0.5358532185916218271, 0.3779506566538943235 ) ) ;
#19388=CARTESIAN_POINT ( 'NONE',  ( 0.4209440094115191044, 0.2863418823927886825, 0.4064695056028758691 ) ) ;
#19389=CARTESIAN_POINT ( 'NONE',  ( 0.1954553509668047195, 0.1954553509668046085, -0.04361111111111028865 ) ) ;
#19392=CARTESIAN_POINT ( 'NONE',  ( -0.009374999999999905978, -0.5358532185916218271, 0.06112444011295371793 ) ) ;
#19393=CARTESIAN_POINT ( 'NONE',  ( 0.000000000000000000, 0.2764156081756484196, 0.3036111111111146621 ) ) ;
#19394=CARTESIAN_POINT ( 'NONE',  ( 0.3125000000000004996, -0.1294417382415918583, 0.3695833333333375936 ) ) ;
#19400=CARTESIAN_POINT ( 'NONE',  ( 0.3155070326520292290, 0.1306872919485615736, 0.2602083333333364279 ) ) ;
#19402=CARTESIAN_POINT ( 'NONE',  ( 0.2209708691207961651, 0.2209708691207959985, 0.3730555555555594704 ) ) ;
#19407=TOROIDAL_SURFACE ( 'NONE', #22115, 0.6209078282299125284, 0.01874999999999999931 ) ;
#19420=CARTESIAN_POINT ( 'NONE',  ( 0.1841151976024382186, 0.2183016720772839037, 0.3966205073423086924 ) ) ;
#19424=ORIENTED_EDGE ( 'NONE', *, *, #228, .T. ) ;
#19447=( BOUNDED_CURVE ( )  B_SPLINE_CURVE ( 2, ( #19712, #8620, #3015, #10463, #16061, #23475, #6791, #14230, #22263 ),
 .UNSPECIFIED., .F., .T. ) 
 B_SPLINE_CURVE_WITH_KNOTS ( ( 3, 2, 2, 2, 3 ),
 ( 0.3229166666666666852, 0.3333333333333333703, 0.3437500000000000000, 0.3541666666666667407, 0.3645833333333334259 ),
 .UNSPECIFIED. ) 
 CURVE ( )  GEOMETRIC_REPRESENTATION_ITEM ( )  RATIONAL_B_SPLINE_CURVE ( ( 1.000000000000000444, 0.9238795325112862944, 1.000000000000000000, 0.9238795325112867385, 1.000000000000000000, 0.9238795325112867385, 1.000000000000000000, 0.9238795325112862944, 1.000000000000000444 ) ) 
 REPRESENTATION_ITEM ( '' )  );
#19448=CYLINDRICAL_SURFACE ( 'NONE', #16953, 0.01874999999999997155 ) ;
#19450=CARTESIAN_POINT ( 'NONE',  ( 0.4592339806827420712, 0.08949080555460971198, 0.4305896728713884958 ) ) ;
#19453=CARTESIAN_POINT ( 'NONE',  ( -0.4687500000000003331, 0.2208780317832466089, 0.4012013675560013315 ) ) ;
#19454=CARTESIAN_POINT ( 'NONE',  ( 0.2209708691207961095, -0.2209708691207961651, -0.07833333333333258874 ) ) ;
#19455=CARTESIAN_POINT ( 'NONE',  ( 7.478516849590708700E-17, -0.5289902422706634910, 0.3941886329748525153 ) ) ;
#19457=CARTESIAN_POINT ( 'NONE',  ( -0.1954553509668046640, 0.1954553509668046918, 0.02583333333333472440 ) ) ;
#19461=CARTESIAN_POINT ( 'NONE',  ( 0.1261236974911665865, 0.2628820852880351944, -0.08058443713070109760 ) ) ;
#19471=ORIENTED_EDGE ( 'NONE', *, *, #7969, .T. ) ;
#19476=CARTESIAN_POINT ( 'NONE',  ( 0.000000000000000000, 0.3155070326520292845, -0.05923611111111021232 ) ) ;
#19483=CARTESIAN_POINT ( 'NONE',  ( -0.1144950937579609918, -0.2764156081756484196, 0.05013888888889045381 ) ) ;
#19485=CARTESIAN_POINT ( 'NONE',  ( -0.1954553509668046640, 0.1954553509668046918, 0.3105555555555591929 ) ) ;
#19494=CARTESIAN_POINT ( 'NONE',  ( -0.3296559951169086844, 0.3509388998445532315, 0.4107594315541606700 ) ) ;
#19495=DIRECTION ( 'NONE',  ( -0.000000000000000000, -0.000000000000000000, 1.000000000000000000 ) ) ;
#19502=EDGE_CURVE ( 'NONE', #11153, #17792, #3265, .T. ) ;
#19504=CARTESIAN_POINT ( 'NONE',  ( 0.07572755880264359085, 0.4860218594902849798, 0.4166771511014252805 ) ) ;
#19505=CARTESIAN_POINT ( 'NONE',  ( -0.2764156081756484196, -0.1144950937579609362, -0.01930555555555453148 ) ) ;
#19511=CARTESIAN_POINT ( 'NONE',  ( -0.1954553509668046640, 0.1954553509668046918, 0.1438888888888912032 ) ) ;
#19514=CARTESIAN_POINT ( 'NONE',  ( -0.2705345477997521120, 0.1189582700827291617, 0.4070486123150025004 ) ) ;
#19518=CARTESIAN_POINT ( 'NONE',  ( 0.1306872919485616846, 0.3155070326520292290, 0.4893750000000048894 ) ) ;
#19522=B_SPLINE_CURVE_WITH_KNOTS ( 'NONE', 3,
 ( #16157, #8829, #23689, #7012, #3832, #15056, #7487, #22480, #7724, #8287, #41, #20536 ),
 .UNSPECIFIED., .F., .F.,
 ( 4, 2, 2, 2, 2, 4 ),
 ( 0.000000000000000000, 0.003384026746073580567, 0.006768053492147161135, 0.008460066865183952720, 0.01015208023822074083, 0.01353610698429432574 ),
 .UNSPECIFIED. ) ;
#19539=CARTESIAN_POINT ( 'NONE',  ( -0.4805070082343985138, 0.2560807851245828770, 0.04413116910601660309 ) ) ;
#19551=CARTESIAN_POINT ( 'NONE',  ( -0.01848103877824600061, -0.5441716683897390716, 0.04413116910601655452 ) ) ;
#19555=DIRECTION ( 'NONE',  ( 0.000000000000000000, 0.000000000000000000, -1.000000000000000000 ) ) ;
#19563=B_SPLINE_CURVE_WITH_KNOTS ( 'NONE', 3,
 ( #21401, #4929, #679, #15554, #13736, #8223, #13852, #21159, #12036, #15674, #2747, #12158 ),
 .UNSPECIFIED., .F., .F.,
 ( 4, 2, 2, 2, 2, 4 ),
 ( 0.000000000000000000, 0.003384026746073584471, 0.006768053492147168941, 0.008460066865183957924, 0.01015208023822074604, 0.01353610698429432921 ),
 .UNSPECIFIED. ) ;
#19566=CARTESIAN_POINT ( 'NONE',  ( -0.3125000000000000000, 0.1294417382415922468, 0.06402777777777962642 ) ) ;
#19571=CARTESIAN_POINT ( 'NONE',  ( -0.1294417382415922191, 0.3125000000000000000, 0.2793055555555591929 ) ) ;
#19574=CARTESIAN_POINT ( 'NONE',  ( -3.385114897866767815E-17, -0.2764156081756484196, 0.04666666666666822311 ) ) ;
#19592=CARTESIAN_POINT ( 'NONE',  ( 0.2230971623002954429, 0.2230971623002953319, 0.1004861111111132743 ) ) ;
#19599=CARTESIAN_POINT ( 'NONE',  ( 0.2764156081756483641, -0.1144950937579611167, 0.1195833333333354426 ) ) ;
#19601=CARTESIAN_POINT ( 'NONE',  ( -0.003401740878768693549, 0.5383620901250332214, 0.05893285591566552878 ) ) ;
#19602=CARTESIAN_POINT ( 'NONE',  ( -0.1954553509668046640, 0.1954553509668046918, 0.4216666666666711305 ) ) ;
#19603=ORIENTED_EDGE ( 'NONE', *, *, #16641, .T. ) ;
#19604=CARTESIAN_POINT ( 'NONE',  ( -0.6209078282299125284, 7.622621636232170019E-17, -0.01219352927422984872 ) ) ;
#19606=DIRECTION ( 'NONE',  ( 0.000000000000000000, 0.000000000000000000, -1.000000000000000000 ) ) ;
#19617=DIRECTION ( 'NONE',  ( 0.000000000000000000, -0.2142211582677938930, -0.9767851838303059919 ) ) ;
#19621=CARTESIAN_POINT ( 'NONE',  ( -0.4687500000000003886, -0.2598076211353319009, 0.06112444011295370405 ) ) ;
#19622=CARTESIAN_POINT ( 'NONE',  ( -0.1144950937579609918, -0.2764156081756484196, 0.04319444444444596465 ) ) ;
#19628=CARTESIAN_POINT ( 'NONE',  ( -3.385114897866767815E-17, -0.2764156081756484196, 0.2202777777777806811 ) ) ;
#19631=CARTESIAN_POINT ( 'NONE',  ( 0.4687500000000003331, -0.08694941101440553655, 0.07654963157453610612 ) ) ;
#19632=CARTESIAN_POINT ( 'NONE',  ( -0.4800179188494136939, 0.1716492620570552741, 0.06108894518741068980 ) ) ;
#19635=CARTESIAN_POINT ( 'NONE',  ( -0.2230971623002954152, -0.2230971623002953874, 0.2914583333333366499 ) ) ;
#19647=DIRECTION ( 'NONE',  ( -1.000000000000000000, 0.000000000000000000, 0.000000000000000000 ) ) ;
#19650=CARTESIAN_POINT ( 'NONE',  ( -0.3125000000000004441, 0.1294417382415918583, 0.3973611111111156613 ) ) ;
#19652=AXIS2_PLACEMENT_3D ( 'NONE', #14088, #10317, #17500 ) ;
#19658=VERTEX_POINT ( 'NONE', #4845 ) ;
#19664=DIRECTION ( 'NONE',  ( 0.000000000000000000, 0.2773500981126134080, -0.9607689228305230644 ) ) ;
#19666=CARTESIAN_POINT ( 'NONE',  ( 0.000000000000000000, 0.000000000000000000, 0.4425000000000000044 ) ) ;
#19671=CARTESIAN_POINT ( 'NONE',  ( -0.3143659348029792522, -0.3723832402019556231, 0.07159583130656665961 ) ) ;
#19682=ORIENTED_EDGE ( 'NONE', *, *, #7509, .F. ) ;
#19685=VERTEX_POINT ( 'NONE', #23248 ) ;
#19699=CARTESIAN_POINT ( 'NONE',  ( 0.2764156081756483641, -0.1144950937579611167, 0.1126388888888909395 ) ) ;
#19701=CARTESIAN_POINT ( 'NONE',  ( 0.4795759075923620163, -5.969813580926603513E-13, 0.07439896364136204532 ) ) ;
#19712=CARTESIAN_POINT ( 'NONE',  ( -0.3125000000000000000, 1.913510623667739771E-17, 0.2341666666666698537 ) ) ;
#19714=CARTESIAN_POINT ( 'NONE',  ( 0.2230971623002954429, 0.2230971623002953319, -0.01062499999999870839 ) ) ;
#19720=CARTESIAN_POINT ( 'NONE',  ( 0.1954553509668047195, 0.1954553509668046085, 0.07444444444444621445 ) ) ;
#19723=CARTESIAN_POINT ( 'NONE',  ( 0.1144950937579611444, 0.2764156081756483641, 0.4112500000000043898 ) ) ;
#19735=CARTESIAN_POINT ( 'NONE',  ( -0.3838430204063939533, 0.3081239094298380832, 0.4164750180373177346 ) ) ;
#19742=EDGE_CURVE ( 'NONE', #11791, #15529, #17302, .T. ) ;
#19745=CARTESIAN_POINT ( 'NONE',  ( 0.3834923435458895136, 0.3083291687941427939, 0.4165495381634259364 ) ) ;
#19746=CARTESIAN_POINT ( 'NONE',  ( 0.2764156081756484196, -5.077672346800151106E-17, 0.005000000000001210074 ) ) ;
#19747=AXIS2_PLACEMENT_3D ( 'NONE', #23108, #11931, #19350 ) ;
#19754=CARTESIAN_POINT ( 'NONE',  ( 0.1954553509668047195, 0.1954553509668046085, 0.1855555555555581937 ) ) ;
#19760=CARTESIAN_POINT ( 'NONE',  ( -0.1144950937579609918, -0.2764156081756484196, 0.09875000000000197509 ) ) ;
#19761=CARTESIAN_POINT ( 'NONE',  ( 0.3155070326520292290, -0.1306872919485616569, 0.3088194444444478659 ) ) ;
#19764=CARTESIAN_POINT ( 'NONE',  ( 0.4584466503968441797, 0.2219868246720123339, 0.4062958900596150280 ) ) ;
#19771=EDGE_CURVE ( 'NONE', #22186, #12538, #3304, .T. ) ;
#19788=CARTESIAN_POINT ( 'NONE',  ( -0.4500000000000003997, -0.2598076211353319009, 0.3779506566538942125 ) ) ;
#19797=CARTESIAN_POINT ( 'NONE',  ( -0.1649704474213682104, -0.4586382700592834261, 0.07155713030921624640 ) ) ;
#19817=FACE_OUTER_BOUND ( 'NONE', #21199, .T. ) ;
#19824=CARTESIAN_POINT ( 'NONE',  ( 0.1954553509668047195, 0.1954553509668046085, 0.01194444444444571485 ) ) ;
#19826=CARTESIAN_POINT ( 'NONE',  ( -0.1294417382415922746, -0.3125000000000000000, 0.4043055555555598035 ) ) ;
#19832=ORIENTED_EDGE ( 'NONE', *, *, #20607, .T. ) ;
#19834=CARTESIAN_POINT ( 'NONE',  ( 0.2230971623002954429, 0.2230971623002953319, -0.06618055555555471536 ) ) ;
#19839=DIRECTION ( 'NONE',  ( 1.000000000000000000, 0.000000000000000000, 0.000000000000000000 ) ) ;
#19840=CARTESIAN_POINT ( 'NONE',  ( 0.2764156081756483641, 0.1144950937579610056, 0.07097222222222394905 ) ) ;
#19842=CARTESIAN_POINT ( 'NONE',  ( 0.1144950937579609085, -0.2764156081756484751, 0.3348611111111148841 ) ) ;
#19845=VECTOR ( 'NONE', #20657, 39.37007874015748143 ) ;
#19847=CARTESIAN_POINT ( 'NONE',  ( 0.000000000000000000, 0.000000000000000000, 1.326383476483184332 ) ) ;
#19854=CARTESIAN_POINT ( 'NONE',  ( -0.4500000000000003997, 0.2598076211353315679, 0.3779506566538943790 ) ) ;
#19856=ORIENTED_EDGE ( 'NONE', *, *, #13651, .F. ) ;
#19864=CARTESIAN_POINT ( 'NONE',  ( -0.2764156081756484196, 0.1144950937579609918, 0.08486111111111295513 ) ) ;
#19870=CARTESIAN_POINT ( 'NONE',  ( 0.4500000000000003442, -0.2598076211353317344, 0.3779506566538943235 ) ) ;
#19871=CARTESIAN_POINT ( 'NONE',  ( 0.1954553509668046640, -0.1954553509668047195, 0.1716666666666691599 ) ) ;
#19875=CARTESIAN_POINT ( 'NONE',  ( 0.000000000000000000, 0.3308333333333335347, -0.1199999999999999956 ) ) ;
#19876=CARTESIAN_POINT ( 'NONE',  ( 0.1954553509668046640, -0.1954553509668047195, -0.05749999999999928085 ) ) ;
#19877=CARTESIAN_POINT ( 'NONE',  ( 0.1306872919485616846, 0.3155070326520292290, 0.4338194444444488651 ) ) ;
#19882=CARTESIAN_POINT ( 'NONE',  ( 0.4687500000000002220, 0.1778880616680548199, 0.4111843359142061671 ) ) ;
#19910=CARTESIAN_POINT ( 'NONE',  ( 0.3125000000000000000, -5.740531871003217465E-17, 0.3175000000000038347 ) ) ;
#19919=EDGE_CURVE ( 'NONE', #7279, #21116, #21917, .T. ) ;
#19921=DIRECTION ( 'NONE',  ( -1.000000000000000000, 0.000000000000000000, 0.000000000000000000 ) ) ;
#19933=ORIENTED_EDGE ( 'NONE', *, *, #23301, .F. ) ;
#19947=CARTESIAN_POINT ( 'NONE',  ( -0.2764156081756484196, -0.1144950937579609362, 0.3695833333333374826 ) ) ;
#19958=CYLINDRICAL_SURFACE ( 'NONE', #1565, 0.3125000000000000000 ) ;
#19961=CARTESIAN_POINT ( 'NONE',  ( -0.2230971623002953874, 0.2230971623002954152, 0.3365972222222262666 ) ) ;
#19964=CARTESIAN_POINT ( 'NONE',  ( 0.4212185919419055291, -0.2861805174101255678, 0.4063787963957714577 ) ) ;
#19967=CARTESIAN_POINT ( 'NONE',  ( -3.385114897866767815E-17, -0.2764156081756484196, 0.1091666666666686880 ) ) ;
#19970=VERTEX_POINT ( 'NONE', #15691 ) ;
#19979=DIRECTION ( 'NONE',  ( 0.000000000000000000, 1.000000000000000000, 0.000000000000000000 ) ) ;
#19982=CARTESIAN_POINT ( 'NONE',  ( -0.3125000000000000000, -0.1294417382415921913, 0.1195833333333352622 ) ) ;
#19986=SHAPE_DEFINITION_REPRESENTATION ( #12666, #12001 ) ;
#19987=CARTESIAN_POINT ( 'NONE',  ( -0.4687500000000016098, -0.2629282712287717705, 0.05975564523638846742 ) ) ;
#19988=CARTESIAN_POINT ( 'NONE',  ( 0.1954553509668046640, -0.1954553509668047195, 0.2202777777777807366 ) ) ;
#19990=EDGE_CURVE ( 'NONE', #8463, #5917, #6509, .T. ) ;
#19993=CARTESIAN_POINT ( 'NONE',  ( -0.1144950937579609779, 0.2764156081756484196, 0.3626388888888929518 ) ) ;
#19996=CARTESIAN_POINT ( 'NONE',  ( 0.4687500000000003886, 0.08694521043083575096, 0.07655001303618025332 ) ) ;
#20000=CARTESIAN_POINT ( 'NONE',  ( 0.2764156081756484196, -5.077672346800151106E-17, 0.06055555555555720143 ) ) ;
#20001=CARTESIAN_POINT ( 'NONE',  ( -0.3155070326520292845, 1.931923388228935888E-17, 0.4511805555555600811 ) ) ;
#20003=VERTEX_POINT ( 'NONE', #19701 ) ;
#20005=CARTESIAN_POINT ( 'NONE',  ( 0.1649704474213681549, 0.4586382700592834261, 0.07155713030921630191 ) ) ;
#20021=ORIENTED_EDGE ( 'NONE', *, *, #21130, .F. ) ;
#20031=EDGE_CURVE ( 'NONE', #7205, #18597, #12279, .T. ) ;
#20069=CARTESIAN_POINT ( 'NONE',  ( 0.2764156081756484196, -5.077672346800151106E-17, 0.3938888888888931739 ) ) ;
#20077=FACE_OUTER_BOUND ( 'NONE', #16004, .T. ) ;
#20080=CARTESIAN_POINT ( 'NONE',  ( -3.863846776457871776E-17, -0.3155070326520292845, 0.1907638888888917861 ) ) ;
#20085=CARTESIAN_POINT ( 'NONE',  ( 0.3267728913538971991, -0.3414772273308539496, 0.4269974078869066547 ) ) ;
#20089=CARTESIAN_POINT ( 'NONE',  ( 0.2764156081756484196, -5.077672346800151106E-17, 0.3452777777777816803 ) ) ;
#20103=CARTESIAN_POINT ( 'NONE',  ( -0.009375000000000199146, 0.5358532185916217161, 0.3779506566538943790 ) ) ;
#20106=CARTESIAN_POINT ( 'NONE',  ( 0.1294417382415921358, -0.3125000000000002220, 0.1334722222222242682 ) ) ;
#20110=CARTESIAN_POINT ( 'NONE',  ( 0.1954553509668047195, 0.1954553509668046085, 0.3452777777777817358 ) ) ;
#20113=CARTESIAN_POINT ( 'NONE',  ( 0.4648120342697257823, 0.2865046371989116714, 0.04342012612512784198 ) ) ;
#20114=EDGE_CURVE ( 'NONE', #22427, #17016, #22728, .T. ) ;
#20115=CARTESIAN_POINT ( 'NONE',  ( 0.01848103877824613592, -0.5441716683897390716, 0.04413116910601658227 ) ) ;
#20121=CARTESIAN_POINT ( 'NONE',  ( -3.385114897866767815E-17, -0.2764156081756484196, 0.04666666666666822311 ) ) ;
#20122=CARTESIAN_POINT ( 'NONE',  ( 0.1954553509668047195, 0.1954553509668046085, -0.09222222222222178911 ) ) ;
#20140=AXIS2_PLACEMENT_3D ( 'NONE', #4073, #13606, #7618 ) ;
#20153=FACE_OUTER_BOUND ( 'NONE', #9434, .T. ) ;
#20154=CARTESIAN_POINT ( 'NONE',  ( 0.6211549996190571798, 7.606954820578536342E-17, -0.1012499999999999928 ) ) ;
#20162=CARTESIAN_POINT ( 'NONE',  ( 0.4687500000000002776, 0.08745190237456319793, 0.08858760123954047272 ) ) ;
#20166=CARTESIAN_POINT ( 'NONE',  ( -0.1961225106001744101, 0.4280344930761185163, 0.09139053646027218980 ) ) ;
#20179=ORIENTED_EDGE ( 'NONE', *, *, #11413, .T. ) ;
#20183=CARTESIAN_POINT ( 'NONE',  ( -3.827021247335479543E-17, -0.3125000000000000000, -0.09222222222222198340 ) ) ;
#20189=CARTESIAN_POINT ( 'NONE',  ( -0.1144950937579609779, 0.2764156081756484196, 0.3001388888888924522 ) ) ;
#20199=( BOUNDED_SURFACE ( )  B_SPLINE_SURFACE ( 3, 2, ( 
 ( #11718, #488, #11844 ),
 ( #15250, #13433, #2566 ),
 ( #10013, #15612, #6334 ),
 ( #21216, #11971, #2328 ),
 ( #13998, #21428, #4716 ),
 ( #11946, #19361, #8344 ),
 ( #6890, #12640, #14634 ),
 ( #22512, #11429, #5587 ),
 ( #22541, #6070, #21422 ),
 ( #4710, #12178, #8486 ) ),
 .UNSPECIFIED., .F., .F., .F. ) 
 B_SPLINE_SURFACE_WITH_KNOTS ( ( 4, 2, 2, 2, 4 ),
 ( 3, 3 ),
 ( 0.04463809143445897354, 0.04796255359614956526, 0.05128701575784016392, 0.05461147791953076258, 0.05793594008122135430 ),
 ( 0.000000000000000000, 1.000000000000000000 ),
 .UNSPECIFIED. ) 
 GEOMETRIC_REPRESENTATION_ITEM ( )  RATIONAL_B_SPLINE_SURFACE ( (
 ( 1.000000000000000000, 0.8285407536241354842, 1.000000000000000000),
 ( 1.000000000000000000, 0.8326168960425578414, 1.000000000000000000),
 ( 1.000000000000000000, 0.8363786027327638761, 1.000000000000000000),
 ( 1.000000000000000000, 0.8417912930203584887, 1.000000000000000000),
 ( 1.000000000000000000, 0.8433923807919373461, 1.000000000000000000),
 ( 1.000000000000000000, 0.8433905099814716921, 1.000000000000000000),
 ( 1.000000000000000000, 0.8417888685871616206, 1.000000000000000000),
 ( 1.000000000000000000, 0.8363766775000033293, 1.000000000000000000),
 ( 1.000000000000000000, 0.8326159398062553674, 1.000000000000000000),
 ( 1.000000000000000000, 0.8285407536241359283, 1.000000000000000000) ) ) 
 REPRESENTATION_ITEM ( '' )  SURFACE ( )  );
#20201=DIRECTION ( 'NONE',  ( -1.000000000000000000, 0.000000000000000000, 0.000000000000000000 ) ) ;
#20205=CARTESIAN_POINT ( 'NONE',  ( -0.2230971623002953874, 0.2230971623002954152, 0.2810416666666702978 ) ) ;
#20212=CARTESIAN_POINT ( 'NONE',  ( -0.1954553509668046640, 0.1954553509668046918, 0.1994444444444471720 ) ) ;
#20225=CARTESIAN_POINT ( 'NONE',  ( -0.01848103877824621571, 0.5441716683897389606, 0.04413116910601659615 ) ) ;
#20233=CARTESIAN_POINT ( 'NONE',  ( -0.1954553509668046918, -0.1954553509668046640, 0.2619444444444477549 ) ) ;
#20237=CARTESIAN_POINT ( 'NONE',  ( -3.385114897866767815E-17, -0.2764156081756484196, 0.3869444444444486431 ) ) ;
#20244=CARTESIAN_POINT ( 'NONE',  ( 0.000000000000000000, 0.2764156081756484196, -0.08527777777777729995 ) ) ;
#20245=ORIENTED_EDGE ( 'NONE', *, *, #22626, .T. ) ;
#20248=CARTESIAN_POINT ( 'NONE',  ( 0.4587679940481828589, -0.1778967816146775627, 0.4165814724634111510 ) ) ;
#20255=DIRECTION ( 'NONE',  ( 0.8459207832372980240, 0.4883925919151546613, -0.2142211582677908954 ) ) ;
#20274=CARTESIAN_POINT ( 'NONE',  ( 0.000000000000000000, 0.3155070326520292845, -0.1182638888888888767 ) ) ;
#20279=AXIS2_PLACEMENT_3D ( 'NONE', #19666, #19309, #13829 ) ;
#20288=CARTESIAN_POINT ( 'NONE',  ( -0.4206390790005693492, 0.2984097918724511467, 0.05816431335574642758 ) ) ;
#20292=ORIENTED_EDGE ( 'NONE', *, *, #19771, .F. ) ;
#20296=CARTESIAN_POINT ( 'NONE',  ( 0.4675595609217378934, -0.2849403337939098169, 0.04271891838948285725 ) ) ;
#20301=CARTESIAN_POINT ( 'NONE',  ( 0.2209708691207961095, -0.2209708691207961651, 0.1994444444444474218 ) ) ;
#20309=DIRECTION ( 'NONE',  ( 0.000000000000000000, 0.000000000000000000, 1.000000000000000000 ) ) ;
#20310=CARTESIAN_POINT ( 'NONE',  ( -0.2764156081756484196, 0.1144950937579609918, 0.3070833333333369830 ) ) ;
#20314=CARTESIAN_POINT ( 'NONE',  ( 0.2944048850341858259, -0.06890421275382911659, 0.4135261689678141894 ) ) ;
#20321=DIRECTION ( 'NONE',  ( -0.000000000000000000, -0.000000000000000000, -1.000000000000000000 ) ) ;
#20322=CARTESIAN_POINT ( 'NONE',  ( 0.2230971623002953874, -0.2230971623002954429, 0.2532638888888922857 ) ) ;
#20325=CARTESIAN_POINT ( 'NONE',  ( 0.3309966345752219374, -0.3501648812924127996, 0.4216785431538761508 ) ) ;
#20326=CARTESIAN_POINT ( 'NONE',  ( -0.01848103877824600061, -0.5441716683897390716, 0.04413116910601655452 ) ) ;
#20329=CARTESIAN_POINT ( 'NONE',  ( -0.1954553509668046640, 0.1954553509668046918, 0.2550000000000031686 ) ) ;
#20332=EDGE_CURVE ( 'NONE', #16785, #23140, #7921, .T. ) ;
#20334=CARTESIAN_POINT ( 'NONE',  ( -0.4584512563509609562, 0.2213892873660434080, 0.4064660812447825067 ) ) ;
#20343=CARTESIAN_POINT ( 'NONE',  ( -0.006583558500310001532, 0.5374648580928949038, 0.05971062996525931116 ) ) ;
#20350=CARTESIAN_POINT ( 'NONE',  ( 0.2764156081756483641, -0.1144950937579611167, 0.2237500000000029743 ) ) ;
#20352=EDGE_CURVE ( 'NONE', #22501, #15771, #8221, .T. ) ;
#20355=CARTESIAN_POINT ( 'NONE',  ( 0.01833836887202428684, -0.2764156081756484751, 0.3875005808676508789 ) ) ;
#20360=CARTESIAN_POINT ( 'NONE',  ( -0.1144950937579609779, 0.2764156081756484196, -0.02624999999999906228 ) ) ;
#20365=CARTESIAN_POINT ( 'NONE',  ( 0.4687500000000002776, -0.2598076211353317344, 0.3779506566538943235 ) ) ;
#20369=VERTEX_POINT ( 'NONE', #6489 ) ;
#20385=CARTESIAN_POINT ( 'NONE',  ( -0.4805070082343984583, 0.2560807851245828770, 0.04413116910601658921 ) ) ;
#20394=EDGE_CURVE ( 'NONE', #22303, #22427, #6606, .T. ) ;
#20395=CARTESIAN_POINT ( 'NONE',  ( -0.4620259694561525965, -0.2880908832651560281, 0.04413116910601649207 ) ) ;
#20404=CARTESIAN_POINT ( 'NONE',  ( 0.3125000000000000000, -5.740531871003217465E-17, 0.1994444444444470055 ) ) ;
#20409=CARTESIAN_POINT ( 'NONE',  ( -0.4593750000000004219, 0.2760455974562897596, 0.3779506566538943790 ) ) ;
#20427=CARTESIAN_POINT ( 'NONE',  ( -0.1144950937579609779, 0.2764156081756484196, 0.3556944444444484765 ) ) ;
#20431=CARTESIAN_POINT ( 'NONE',  ( -0.04282247326132401083, -0.5165423109005167213, 0.4011144384304581867 ) ) ;
#20432=CARTESIAN_POINT ( 'NONE',  ( -0.3125000000000000000, 0.000000000000000000, 1.326383476483184332 ) ) ;
#20443=CARTESIAN_POINT ( 'NONE',  ( -0.1306872919485614903, 0.3155070326520293400, 0.2220138888888920359 ) ) ;
#20446=VERTEX_POINT ( 'NONE', #21369 ) ;
#20447=CARTESIAN_POINT ( 'NONE',  ( 0.006542161132012845430, -0.5374887588746249945, 0.3892820121258430133 ) ) ;
#20451=CARTESIAN_POINT ( 'NONE',  ( -3.385114897866767815E-17, -0.2764156081756484196, 0.2758333333333366499 ) ) ;
#20456=CARTESIAN_POINT ( 'NONE',  ( -0.4593750000000003664, 0.04475449550936177329, 0.4343810118395208253 ) ) ;
#20462=DIRECTION ( 'NONE',  ( -1.000000000000000000, 0.000000000000000000, 0.000000000000000000 ) ) ;
#20473=CARTESIAN_POINT ( 'NONE',  ( -0.1144950937579609918, -0.2764156081756484196, 0.2654166666666700203 ) ) ;
#20481=CARTESIAN_POINT ( 'NONE',  ( 0.3856318672988792162, 0.3186212149721686648, 0.4002893343786020353 ) ) ;
#20482=CARTESIAN_POINT ( 'NONE',  ( -3.385114897866767815E-17, -0.2764156081756484196, -0.05749999999999930167 ) ) ;
#20484=CARTESIAN_POINT ( 'NONE',  ( 0.4687500000000002776, -0.04376700804269017392, 0.4181543355204243584 ) ) ;
#20490=CARTESIAN_POINT ( 'NONE',  ( 0.3308333333333332571, 3.738758431839877614E-19, 0.4425000000000000044 ) ) ;
#20505=CARTESIAN_POINT ( 'NONE',  ( -0.3125000000000000000, 1.913510623667739771E-17, -0.05055555555555497210 ) ) ;
#20513=CARTESIAN_POINT ( 'NONE',  ( -0.3155070326520293400, -0.1306872919485614626, 0.01020833333333438092 ) ) ;
#20514=CARTESIAN_POINT ( 'NONE',  ( -3.827021247335479543E-17, -0.3125000000000000000, 0.02583333333333490481 ) ) ;
#20525=CARTESIAN_POINT ( 'NONE',  ( -0.2773501192371494728, 0.3936383244007691240, 0.07440066028687920829 ) ) ;
#20528=( BOUNDED_SURFACE ( )  B_SPLINE_SURFACE ( 3, 2, ( 
 ( #1147, #8695, #21751 ),
 ( #14318, #14443, #12504 ),
 ( #16146, #8454, #3098 ),
 ( #4921, #6999, #6875 ),
 ( #17978, #8586, #12385 ),
 ( #12260, #21867, #1390 ) ),
 .UNSPECIFIED., .F., .F., .T. ) 
 B_SPLINE_SURFACE_WITH_KNOTS ( ( 4, 2, 4 ),
 ( 3, 3 ),
 ( 0.001402224832186923413, 0.001901366090229829071, 0.002400507348272734511 ),
 ( 0.000000000000000000, 1.000000000000000000 ),
 .UNSPECIFIED. ) 
 GEOMETRIC_REPRESENTATION_ITEM ( )  RATIONAL_B_SPLINE_SURFACE ( (
 ( 1.000000000000000000, 0.8285407536241354842, 1.000000000000000000),
 ( 1.000000000000000000, 0.8382697314792872945, 1.000000000000000000),
 ( 1.000000000000000000, 0.8433836253083701884, 1.000000000000000000),
 ( 1.000000000000000000, 0.8433992480895078359, 1.000000000000000000),
 ( 1.000000000000000000, 0.8382827608169546307, 1.000000000000000000),
 ( 1.000000000000000000, 0.8285407536241033988, 1.000000000000000000) ) ) 
 REPRESENTATION_ITEM ( '' )  SURFACE ( )  );
#20531=CARTESIAN_POINT ( 'NONE',  ( -0.2562433651783130317, -0.1785792061923512919, -0.1010489577189804811 ) ) ;
#20536=CARTESIAN_POINT ( 'NONE',  ( 0.4581189881604794123, -0.2644951211353317455, 0.3941886329748525153 ) ) ;
#20538=VERTEX_POINT ( 'NONE', #12240 ) ;
#20542=CARTESIAN_POINT ( 'NONE',  ( -3.827021247335479543E-17, -0.3125000000000000000, 0.1925000000000028910 ) ) ;
#20548=CARTESIAN_POINT ( 'NONE',  ( -0.1954553509668046640, 0.1954553509668046918, 0.4702777777777827350 ) ) ;
#20551=CARTESIAN_POINT ( 'NONE',  ( 0.2659300498200044549, -0.1330428112940453822, 0.4085120587161163996 ) ) ;
#20552=CARTESIAN_POINT ( 'NONE',  ( -0.2775113281607684557, 0.3935459114639778821, 0.07438423612653367878 ) ) ;
#20557=CARTESIAN_POINT ( 'NONE',  ( -0.3125000000000000000, 1.913510623667739771E-17, 0.2827777777777810142 ) ) ;
#20563=CARTESIAN_POINT ( 'NONE',  ( 0.1306872919485616846, 0.3155070326520292290, 0.3817361111111154948 ) ) ;
#20570=CARTESIAN_POINT ( 'NONE',  ( 0.1144950937579611444, 0.2764156081756483641, 0.1265277777777799595 ) ) ;
#20572=CARTESIAN_POINT ( 'NONE',  ( 0.1954553509668046640, -0.1954553509668047195, 0.3383333333333371495 ) ) ;
#20579=CARTESIAN_POINT ( 'NONE',  ( 0.2688584691416451289, -0.07459580784769219430, 0.3902639665736167829 ) ) ;
#20588=DIRECTION ( 'NONE',  ( 0.000000000000000000, 0.000000000000000000, -1.000000000000000000 ) ) ;
#20590=CARTESIAN_POINT ( 'NONE',  ( 0.1306872919485616846, 0.3155070326520292290, -0.1182638888888884604 ) ) ;
#20592=DIRECTION ( 'NONE',  ( -1.000000000000000000, 0.000000000000000000, 0.000000000000000000 ) ) ;
#20597=CARTESIAN_POINT ( 'NONE',  ( 0.2209708691207961651, 0.2209708691207959985, 0.1577777777777804313 ) ) ;
#20599=CARTESIAN_POINT ( 'NONE',  ( 0.009374999999999772404, 0.5358532185916217161, 0.3779506566538943790 ) ) ;
#20600=CARTESIAN_POINT ( 'NONE',  ( -0.1144950937579609779, 0.2764156081756484196, 0.2515277777777809587 ) ) ;
#20601=ORIENTED_EDGE ( 'NONE', *, *, #24038, .T. ) ;
#20607=EDGE_CURVE ( 'NONE', #175, #8540, #17951, .T. ) ;
#20610=DIRECTION ( 'NONE',  ( 0.7071067811865435759, 0.000000000000000000, 0.7071067811865514585 ) ) ;
#20611=ORIENTED_EDGE ( 'NONE', *, *, #15835, .F. ) ;
#20612=CARTESIAN_POINT ( 'NONE',  ( -0.2209708691207961373, -0.2209708691207961095, 0.1300000000000023914 ) ) ;
#20616=CARTESIAN_POINT ( 'NONE',  ( 0.2980062158858373667, -0.01674720435928796214, -0.08717288255250393858 ) ) ;
#20619=CARTESIAN_POINT ( 'NONE',  ( 0.000000000000000000, 0.000000000000000000, 0.4425000000000000044 ) ) ;
#20628=CARTESIAN_POINT ( 'NONE',  ( -0.3155070326520293400, -0.1306872919485614626, -0.04534722222222162258 ) ) ;
#20629=CARTESIAN_POINT ( 'NONE',  ( -0.3125000000000010547, -0.1294417382415911644, 0.01541666666666811208 ) ) ;
#20641=CARTESIAN_POINT ( 'NONE',  ( -0.3125000000000000000, 1.913510623667739771E-17, 0.1161111111111130384 ) ) ;
#20645=ORIENTED_EDGE ( 'NONE', *, *, #8863, .F. ) ;
#20651=CARTESIAN_POINT ( 'NONE',  ( 0.3125000000000000000, 3.827021247335477694E-17, 1.326383476483184332 ) ) ;
#20657=DIRECTION ( 'NONE',  ( 0.000000000000000000, 0.000000000000000000, -1.000000000000000000 ) ) ;
#20664=DIRECTION ( 'NONE',  ( -1.000000000000000000, 0.000000000000000000, 0.000000000000000000 ) ) ;
#20666=EDGE_CURVE ( 'NONE', #7496, #16468, #9344, .T. ) ;
#20668=( BOUNDED_SURFACE ( )  B_SPLINE_SURFACE ( 1, 2, ( 
 ( #5838, #15353, #6194, #19366, #20836, #2310, #9625, #2664, #22782, #11460, #6076, #10114, #4128, #18893, #2194, #351, #6799, #6552, #14002, #10229, #17776, #8373, #23124, #1069, #2892, #14120, #21549, #10470, #1194, #21435, #3023, #4960, #8500, #23483, #21675, #10589, #3140, #15824, #4720, #10352, #6922, #14240, #17899, #10705, #23243, #18140, #14360, #8738, #6675, #6435, #12547, #17656, #15940, #3254, #18016, #19483, #8626, #12427, #12193, #4840, #16071, #19840, #19720, #1314, #16194, #23608, #12306, #13889, #23366, #1437, #21790, #5079, #19967, #15710, #21317, #19599, #4607, #12069, #2776, #943, #16673, #18743, #23723, #3747, #24098, #7165, #18377, #10831, #1672, #11068, #11310, #3378, #23845, #18497, #5450, #3500, #7048, #3869, #20212, #10950, #12793, #1791, #14858, #23976, #9104, #16435, #9234, #7407, #22394, #8869, #7286, #12669, #14484, #22275, #20329, #14608, #16554, #9357, #5570, #13035, #20451, #80, #3618, #14972, #12918, #14738, #22153, #5695, #21908, #11191, #7525, #13158, #16799, #16310, #18620, #1912, #22031, #5198, #20572, #5328, #20089, #18259, #1554, #8992, #6292, #13274, #6168, #9599, #18864, #13631, #4459, #20930, #2038, #19099, #22757, #17394, #9964, #11559, #9845, #6048, #687, #11433, #22987, #9477, #8111, #15450, #7646, #5810, #13515, #7877, #561, #11676, #15565, #7998, #21170, #13745, #18986, #5928, #2286 ),
 ( #15208, #2405, #17276, #13388, #4223, #20811, #11923, #22873, #17156, #16910, #17031, #15327, #21049, #22517, #205, #2522, #446, #4339, #22643, #11790, #9720, #15094, #19215, #20691, #3982, #2166, #325, #7764, #4100, #23221, #16049, #6530, #921, #2867, #14098, #17877, #13982, #21410, #14217, #23462, #23102, #17631, #21771, #6411, #8718, #14339, #19824, #19343, #3002, #6773, #19457, #4699, #1169, #21653, #12166, #1048, #19574, #12284, #8351, #17509, #10327, #15803, #17753, #8475, #15916, #13863, #23583, #21291, #4941, #2755, #12044, #12405, #5058, #21525, #2640, #19699, #23338, #10570, #3119, #6652, #10451, #4815, #18000, #4584, #16168, #10089, #1292, #8608, #805, #10207, #6900, #8233, #15686, #22128, #18599, #11046, #7500, #9333, #5308, #16416, #22010, #18118, #1415, #7383, #11171, #18357, #23703, #1535, #5429, #12895, #23825, #23953, #7146, #14946, #16534, #3478, #54, #3356, #1650, #14834, #8843, #3724, #13012, #10928, #16653, #8967, #18475, #12771, #16290, #20189, #7267, #20310, #1769, #1890, #16770, #10809, #14587, #9214, #9084, #18237, #14715, #3595, #24074, #22251, #5547, #20427, #22368, #7024, #12528, #19947, #14467, #3233, #10684, #21891, #5180, #12650, #20069, #5787, #15183, #11651, #17252, #22620, #11529, #19075, #17134, #3961, #13363, #6141, #2383, #4197, #13489, #21023, #421, #11770, #2260, #5905, #17006, #2499, #20548 ) ),
 .UNSPECIFIED., .F., .F., .T. ) 
 B_SPLINE_SURFACE_WITH_KNOTS ( ( 2, 2 ),
 ( 3, 2, 2, 2, 2, 2, 2, 2, 2, 2, 2, 2, 2, 2, 2, 2, 2, 2, 2, 2, 2, 2, 2, 2, 2, 2, 2, 2, 2, 2, 2, 2, 2, 2, 2, 2, 2, 2, 2, 2, 2, 2, 2, 2, 2, 2, 2, 2, 2, 2, 2, 2, 2, 2, 2, 2, 2, 2, 2, 2, 2, 2, 2, 2, 2, 2, 2, 2, 2, 2, 2, 2, 2, 2, 2, 2, 2, 2, 2, 2, 2, 2, 2, 2, 2, 2, 2, 2, 2, 3 ),
 ( 0.000000000000000000, 1.000000000000000000 ),
 ( 0.000000000000000000, 0.01041666666666666609, 0.02083333333333333218, 0.03125000000000000000, 0.04166666666666666435, 0.05208333333333333565, 0.06250000000000000000, 0.07291666666666667129, 0.08333333333333332871, 0.09375000000000000000, 0.1041666666666666713, 0.1145833333333333287, 0.1250000000000000000, 0.1354166666666666574, 0.1458333333333333426, 0.1562500000000000000, 0.1666666666666666574, 0.1770833333333333426, 0.1875000000000000000, 0.1979166666666666574, 0.2083333333333333426, 0.2187500000000000000, 0.2291666666666666574, 0.2395833333333333426, 0.2500000000000000000, 0.2604166666666666852, 0.2708333333333333148, 0.2812500000000000000, 0.2916666666666666852, 0.3020833333333333148, 0.3125000000000000000, 0.3229166666666666852, 0.3333333333333333148, 0.3437500000000000000, 0.3541666666666666852, 0.3645833333333333148, 0.3750000000000000000, 0.3854166666666666852, 0.3958333333333333148, 0.4062500000000000000, 0.4166666666666666852, 0.4270833333333333148, 0.4375000000000000000, 0.4479166666666666852, 0.4583333333333333148, 0.4687500000000000000, 0.4791666666666666852, 0.4895833333333333148, 0.5000000000000000000, 0.5104166666666666297, 0.5208333333333333703, 0.5312500000000000000, 0.5416666666666666297, 0.5520833333333333703, 0.5625000000000000000, 0.5729166666666666297, 0.5833333333333333703, 0.5937500000000000000, 0.6041666666666666297, 0.6145833333333333703, 0.6250000000000000000, 0.6354166666666666297, 0.6458333333333333703, 0.6562500000000000000, 0.6666666666666666297, 0.6770833333333333703, 0.6875000000000000000, 0.6979166666666666297, 0.7083333333333333703, 0.7187500000000000000, 0.7291666666666666297, 0.7395833333333333703, 0.7500000000000000000, 0.7604166666666666297, 0.7708333333333333703, 0.7812500000000000000, 0.7916666666666666297, 0.8020833333333333703, 0.8125000000000000000, 0.8229166666666666297, 0.8333333333333333703, 0.8437500000000000000, 0.8541666666666666297, 0.8645833333333333703, 0.8750000000000000000, 0.8854166666666666297, 0.8958333333333333703, 0.9062500000000000000, 0.9166666666666666297, 0.9270833333333333703 ),
 .UNSPECIFIED. ) 
 GEOMETRIC_REPRESENTATION_ITEM ( )  RATIONAL_B_SPLINE_SURFACE ( (
 ( 1.000000000000000000, 0.9238795325112867385, 1.000000000000000000, 0.9238795325112867385, 1.000000000000000000, 0.9238795325112867385, 1.000000000000000000, 0.9238795325112867385, 1.000000000000000000, 0.9238795325112867385, 1.000000000000000000, 0.9238795325112867385, 1.000000000000000000, 0.9238795325112867385, 1.000000000000000000, 0.9238795325112867385, 1.000000000000000000, 0.9238795325112867385, 1.000000000000000000, 0.9238795325112867385, 1.000000000000000000, 0.9238795325112867385, 1.000000000000000000, 0.9238795325112867385, 1.000000000000000000, 0.9238795325112867385, 1.000000000000000000, 0.9238795325112867385, 1.000000000000000000, 0.9238795325112867385, 1.000000000000000000, 0.9238795325112867385, 1.000000000000000000, 0.9238795325112867385, 1.000000000000000000, 0.9238795325112867385, 1.000000000000000000, 0.9238795325112867385, 1.000000000000000000, 0.9238795325112867385, 1.000000000000000000, 0.9238795325112867385, 1.000000000000000000, 0.9238795325112867385, 1.000000000000000000, 0.9238795325112867385, 1.000000000000000000, 0.9238795325112867385, 1.000000000000000000, 0.9238795325112867385, 1.000000000000000000, 0.9238795325112867385, 1.000000000000000000, 0.9238795325112867385, 1.000000000000000000, 0.9238795325112867385, 1.000000000000000000, 0.9238795325112867385, 1.000000000000000000, 0.9238795325112867385, 1.000000000000000000, 0.9238795325112867385, 1.000000000000000000, 0.9238795325112867385, 1.000000000000000000, 0.9238795325112867385, 1.000000000000000000, 0.9238795325112867385, 1.000000000000000000, 0.9238795325112867385, 1.000000000000000000, 0.9238795325112867385, 1.000000000000000000, 0.9238795325112867385, 1.000000000000000000, 0.9238795325112867385, 1.000000000000000000, 0.9238795325112867385, 1.000000000000000000, 0.9238795325112867385, 1.000000000000000000, 0.9238795325112867385, 1.000000000000000000, 0.9238795325112867385, 1.000000000000000000, 0.9238795325112867385, 1.000000000000000000, 0.9238795325112867385, 1.000000000000000000, 0.9238795325112867385, 1.000000000000000000, 0.9238795325112867385, 1.000000000000000000, 0.9238795325112867385, 1.000000000000000000, 0.9238795325112867385, 1.000000000000000000, 0.9238795325112867385, 1.000000000000000000, 0.9238795325112867385, 1.000000000000000000, 0.9238795325112867385, 1.000000000000000000, 0.9238795325112867385, 1.000000000000000000, 0.9238795325112867385, 1.000000000000000000, 0.9238795325112867385, 1.000000000000000000, 0.9238795325112867385, 1.000000000000000000, 0.9238795325112867385, 1.000000000000000000, 0.9238795325112867385, 1.000000000000000000, 0.9238795325112867385, 1.000000000000000000, 0.9238795325112867385, 1.000000000000000000, 0.9238795325112867385, 1.000000000000000000, 0.9238795325112867385, 1.000000000000000000, 0.9238795325112867385, 1.000000000000000000, 0.9238795325112867385, 1.000000000000000000, 0.9238795325112867385, 1.000000000000000000, 0.9238795325112867385, 1.000000000000000000, 0.9238795325112867385, 1.000000000000000000, 0.9238795325112867385, 1.000000000000000000, 0.9238795325112867385, 1.000000000000000000, 0.9238795325112867385, 1.000000000000000000, 0.9238795325112867385, 1.000000000000000000, 0.9238795325112867385, 1.000000000000000000, 0.9238795325112867385, 1.000000000000000000, 0.9238795325112867385, 1.000000000000000000, 0.9238795325112867385, 1.000000000000000000, 0.9238795325112867385, 1.000000000000000000, 0.9238795325112867385, 1.000000000000000000, 0.9238795325112867385, 1.000000000000000000, 0.9238795325112867385, 1.000000000000000000, 0.9238795325112867385, 1.000000000000000000, 0.9238795325112867385, 1.000000000000000000, 0.9238795325112867385, 1.000000000000000000, 0.9238795325112867385, 1.000000000000000000, 0.9238795325112867385, 1.000000000000000000, 0.9238795325112867385, 1.000000000000000000, 0.9238795325112867385, 1.000000000000000000, 0.9238795325112867385, 1.000000000000000000, 0.9238795325112867385, 1.000000000000000000, 0.9238795325112867385, 1.000000000000000000, 0.9238795325112867385, 1.000000000000000000),
 ( 1.000000000000000000, 0.9238795325112867385, 1.000000000000000000, 0.9238795325112867385, 1.000000000000000000, 0.9238795325112867385, 1.000000000000000000, 0.9238795325112867385, 1.000000000000000000, 0.9238795325112867385, 1.000000000000000000, 0.9238795325112867385, 1.000000000000000000, 0.9238795325112867385, 1.000000000000000000, 0.9238795325112867385, 1.000000000000000000, 0.9238795325112867385, 1.000000000000000000, 0.9238795325112867385, 1.000000000000000000, 0.9238795325112867385, 1.000000000000000000, 0.9238795325112867385, 1.000000000000000000, 0.9238795325112867385, 1.000000000000000000, 0.9238795325112867385, 1.000000000000000000, 0.9238795325112867385, 1.000000000000000000, 0.9238795325112867385, 1.000000000000000000, 0.9238795325112867385, 1.000000000000000000, 0.9238795325112867385, 1.000000000000000000, 0.9238795325112867385, 1.000000000000000000, 0.9238795325112867385, 1.000000000000000000, 0.9238795325112867385, 1.000000000000000000, 0.9238795325112867385, 1.000000000000000000, 0.9238795325112867385, 1.000000000000000000, 0.9238795325112867385, 1.000000000000000000, 0.9238795325112867385, 1.000000000000000000, 0.9238795325112867385, 1.000000000000000000, 0.9238795325112867385, 1.000000000000000000, 0.9238795325112867385, 1.000000000000000000, 0.9238795325112867385, 1.000000000000000000, 0.9238795325112867385, 1.000000000000000000, 0.9238795325112867385, 1.000000000000000000, 0.9238795325112867385, 1.000000000000000000, 0.9238795325112867385, 1.000000000000000000, 0.9238795325112867385, 1.000000000000000000, 0.9238795325112867385, 1.000000000000000000, 0.9238795325112867385, 1.000000000000000000, 0.9238795325112867385, 1.000000000000000000, 0.9238795325112867385, 1.000000000000000000, 0.9238795325112867385, 1.000000000000000000, 0.9238795325112867385, 1.000000000000000000, 0.9238795325112867385, 1.000000000000000000, 0.9238795325112867385, 1.000000000000000000, 0.9238795325112867385, 1.000000000000000000, 0.9238795325112867385, 1.000000000000000000, 0.9238795325112867385, 1.000000000000000000, 0.9238795325112867385, 1.000000000000000000, 0.9238795325112867385, 1.000000000000000000, 0.9238795325112867385, 1.000000000000000000, 0.9238795325112867385, 1.000000000000000000, 0.9238795325112867385, 1.000000000000000000, 0.9238795325112867385, 1.000000000000000000, 0.9238795325112867385, 1.000000000000000000, 0.9238795325112867385, 1.000000000000000000, 0.9238795325112867385, 1.000000000000000000, 0.9238795325112867385, 1.000000000000000000, 0.9238795325112867385, 1.000000000000000000, 0.9238795325112867385, 1.000000000000000000, 0.9238795325112867385, 1.000000000000000000, 0.9238795325112867385, 1.000000000000000000, 0.9238795325112867385, 1.000000000000000000, 0.9238795325112867385, 1.000000000000000000, 0.9238795325112867385, 1.000000000000000000, 0.9238795325112867385, 1.000000000000000000, 0.9238795325112867385, 1.000000000000000000, 0.9238795325112867385, 1.000000000000000000, 0.9238795325112867385, 1.000000000000000000, 0.9238795325112867385, 1.000000000000000000, 0.9238795325112867385, 1.000000000000000000, 0.9238795325112867385, 1.000000000000000000, 0.9238795325112867385, 1.000000000000000000, 0.9238795325112867385, 1.000000000000000000, 0.9238795325112867385, 1.000000000000000000, 0.9238795325112867385, 1.000000000000000000, 0.9238795325112867385, 1.000000000000000000, 0.9238795325112867385, 1.000000000000000000, 0.9238795325112867385, 1.000000000000000000, 0.9238795325112867385, 1.000000000000000000, 0.9238795325112867385, 1.000000000000000000, 0.9238795325112867385, 1.000000000000000000, 0.9238795325112867385, 1.000000000000000000, 0.9238795325112867385, 1.000000000000000000, 0.9238795325112867385, 1.000000000000000000, 0.9238795325112867385, 1.000000000000000000, 0.9238795325112867385, 1.000000000000000000, 0.9238795325112867385, 1.000000000000000000, 0.9238795325112867385, 1.000000000000000000, 0.9238795325112867385, 1.000000000000000000, 0.9238795325112867385, 1.000000000000000000, 0.9238795325112867385, 1.000000000000000000) ) ) 
 REPRESENTATION_ITEM ( '' )  SURFACE ( )  );
#20669=( BOUNDED_CURVE ( )  B_SPLINE_CURVE ( 2, ( #13859, #9960, #10084, #19571, #2518, #4455, #4581, #9840, #13627 ),
 .UNSPECIFIED., .F., .F. ) 
 B_SPLINE_CURVE_WITH_KNOTS ( ( 3, 2, 2, 2, 3 ),
 ( 0.2395833333333334259, 0.2500000000000000555, 0.2604166666666667962, 0.2708333333333334259, 0.2812500000000000555 ),
 .UNSPECIFIED. ) 
 CURVE ( )  GEOMETRIC_REPRESENTATION_ITEM ( )  RATIONAL_B_SPLINE_CURVE ( ( 0.9999999999999995559, 0.9238795325112871826, 1.000000000000000000, 0.9238795325112867385, 1.000000000000000000, 0.9238795325112867385, 1.000000000000000000, 0.9238795325112862944, 1.000000000000000444 ) ) 
 REPRESENTATION_ITEM ( '' )  );
#20671=CARTESIAN_POINT ( 'NONE',  ( 0.4223122635727384888, -0.2974437783094736054, 0.07051021533369883354 ) ) ;
#20680=ORIENTED_EDGE ( 'NONE', *, *, #16450, .T. ) ;
#20681=ORIENTED_EDGE ( 'NONE', *, *, #2888, .T. ) ;
#20683=DIRECTION ( 'NONE',  ( -1.000000000000000000, 0.000000000000000000, 0.000000000000000000 ) ) ;
#20687=CARTESIAN_POINT ( 'NONE',  ( 0.4593750000000004219, -0.2760455974562899262, 0.06112444011295369711 ) ) ;
#20689=CARTESIAN_POINT ( 'NONE',  ( -3.385114897866767815E-17, -0.2764156081756484196, 0.1577777777777801815 ) ) ;
#20691=CARTESIAN_POINT ( 'NONE',  ( -0.1144950937579609918, -0.2764156081756484196, -0.06791666666666602847 ) ) ;
#20694=CARTESIAN_POINT ( 'NONE',  ( -0.01298578716746940157, -0.5473886244374777110, 0.04271891838948295439 ) ) ;
#20707=CARTESIAN_POINT ( 'NONE',  ( -0.3108513798347909418, -0.3617957495396915135, 0.4142710792078265203 ) ) ;
#20709=CARTESIAN_POINT ( 'NONE',  ( 0.3155070326520292290, -0.1306872919485616569, -0.07659722222222146992 ) ) ;
#20719=CARTESIAN_POINT ( 'NONE',  ( 0.2764156081756483641, 0.1144950937579610056, 0.2376388888888919526 ) ) ;
#20729=CARTESIAN_POINT ( 'NONE',  ( 0.1294417382415921358, -0.3125000000000002220, 0.1404166666666691321 ) ) ;
#20732=EDGE_CURVE ( 'NONE', #3958, #20369, #5317, .T. ) ;
#20736=DIRECTION ( 'NONE',  ( 1.000000000000000000, 0.000000000000000000, 0.000000000000000000 ) ) ;
#20737=CARTESIAN_POINT ( 'NONE',  ( -0.2764156081756484196, 0.1144950937579609918, -0.1373611111111110172 ) ) ;
#20742=CARTESIAN_POINT ( 'NONE',  ( -0.2764156081756484196, -0.1144950937579609362, 0.04319444444444596465 ) ) ;
#20749=CARTESIAN_POINT ( 'NONE',  ( -0.2230971623002954152, -0.2230971623002953874, 0.06923611111111260819 ) ) ;
#20766=DIRECTION ( 'NONE',  ( 0.000000000000000000, 0.000000000000000000, -1.000000000000000000 ) ) ;
#20770=CARTESIAN_POINT ( 'NONE',  ( 0.1376066337087315239, 0.2509841804965753376, 0.3977425164349297493 ) ) ;
#20773=ORIENTED_EDGE ( 'NONE', *, *, #4005, .T. ) ;
#20776=CARTESIAN_POINT ( 'NONE',  ( 0.03677510111070102922, 0.5081344126854514531, 0.4062297518000476670 ) ) ;
#20782=CARTESIAN_POINT ( 'NONE',  ( 0.3125000000000000000, -5.740531871003217465E-17, 0.08833333333333501236 ) ) ;
#20797=ORIENTED_EDGE ( 'NONE', *, *, #16641, .F. ) ;
#20802=CARTESIAN_POINT ( 'NONE',  ( -0.1306872919485615459, -0.3155070326520293400, 0.4095138888888935069 ) ) ;
#20807=CARTESIAN_POINT ( 'NONE',  ( 0.08337866210071723239, -0.4931271843567546220, 0.07807775719021840810 ) ) ;
#20809=CARTESIAN_POINT ( 'NONE',  ( 0.2764156081756483641, 0.1144950937579610195, 0.1751388888888914530 ) ) ;
#20811=CARTESIAN_POINT ( 'NONE',  ( -0.2764156081756484196, -0.1144950937579609362, -0.1304166666666665420 ) ) ;
#20815=CARTESIAN_POINT ( 'NONE',  ( -0.2437787738197921550, 0.1452258864492545765, -0.07229589000035700763 ) ) ;
#20816=EDGE_CURVE ( 'NONE', #20864, #20538, #345, .T. ) ;
#20822=CIRCLE ( 'NONE', #14206, 0.01875000000000002359 ) ;
#20827=( GEOMETRIC_REPRESENTATION_CONTEXT ( 3 ) GLOBAL_UNCERTAINTY_ASSIGNED_CONTEXT ( ( #15583 ) ) GLOBAL_UNIT_ASSIGNED_CONTEXT ( ( #5744, #128, #18785 ) ) REPRESENTATION_CONTEXT ( 'NONE', 'WORKASPACE' ) );
#20830=CARTESIAN_POINT ( 'NONE',  ( 0.3155070326520292290, -0.1306872919485616569, -0.1321527777777774804 ) ) ;
#20836=CARTESIAN_POINT ( 'NONE',  ( -0.2764156081756484196, 1.692557448933383907E-17, -0.1269444444444443043 ) ) ;
#20839=CARTESIAN_POINT ( 'NONE',  ( -0.2764156081756484196, 1.692557448933383907E-17, 0.2063888888888917028 ) ) ;
#20847=CARTESIAN_POINT ( 'NONE',  ( -0.2977072594216396695, 1.822931211668208286E-17, 0.4093739260883065278 ) ) ;
#20848=CARTESIAN_POINT ( 'NONE',  ( -0.1514837979169837701, 0.4428147562410876259, 0.4304954382810343150 ) ) ;
#20858=CARTESIAN_POINT ( 'NONE',  ( -0.3084988159814148201, 0.02958440236016895986, -0.09766548264808183610 ) ) ;
#20862=CARTESIAN_POINT ( 'NONE',  ( -0.1954553509668046918, -0.1954553509668046640, -0.008888888888887799475 ) ) ;
#20864=VERTEX_POINT ( 'NONE', #17047 ) ;
#20869=CARTESIAN_POINT ( 'NONE',  ( -0.3155070326520293400, 0.1306872919485614903, 0.1143750000000018641 ) ) ;
#20870=CARTESIAN_POINT ( 'NONE',  ( 0.4687500000000002776, -0.04412582310964638377, 0.4181239759302315395 ) ) ;
#20874=EDGE_LOOP ( 'NONE', ( #9946, #8553, #1518, #13757 ) ) ;
#20883=AXIS2_PLACEMENT_3D ( 'NONE', #23995, #10607, #22174 ) ;
#20885=CARTESIAN_POINT ( 'NONE',  ( 0.1031051051775479510, -0.2870977370808670548, -0.09375409208931057004 ) ) ;
#20886=ORIENTED_EDGE ( 'NONE', *, *, #2001, .T. ) ;
#20889=CARTESIAN_POINT ( 'NONE',  ( 0.2802773643484149924, 0.009513829220699975345, 0.3919440310150817952 ) ) ;
#20894=VERTEX_POINT ( 'NONE', #340 ) ;
#20896=CARTESIAN_POINT ( 'NONE',  ( -1.514244853754661224E-16, 0.5289902422706633800, 0.3941886329748526818 ) ) ;
#20897=DIRECTION ( 'NONE',  ( 1.000000000000000000, 0.000000000000000000, 0.000000000000000000 ) ) ;
#20901=EDGE_CURVE ( 'NONE', #18391, #10173, #17241, .T. ) ;
#20914=ORIENTED_EDGE ( 'NONE', *, *, #4199, .F. ) ;
#20916=ORIENTED_EDGE ( 'NONE', *, *, #6180, .F. ) ;
#20920=CARTESIAN_POINT ( 'NONE',  ( 0.3155070326520292845, -5.795770164686806123E-17, 0.4268750000000047784 ) ) ;
#20926=CARTESIAN_POINT ( 'NONE',  ( 0.3146277125502771610, -0.3722332453489731741, 0.07156651416103082530 ) ) ;
#20927=EDGE_CURVE ( 'NONE', #22119, #9702, #1806, .T. ) ;
#20928=CARTESIAN_POINT ( 'NONE',  ( 0.1144950937579611444, 0.2764156081756483641, 0.2931944444444479769 ) ) ;
#20930=CARTESIAN_POINT ( 'NONE',  ( -0.1144950937579609918, -0.2764156081756484196, 0.3834722222222265442 ) ) ;
#20932=EDGE_CURVE ( 'NONE', #5628, #17172, #17319, .T. ) ;
#20941=AXIS2_PLACEMENT_3D ( 'NONE', #9455, #22736, #1895 ) ;
#20943=EDGE_CURVE ( 'NONE', #3460, #9832, #6245, .T. ) ;
#20949=CARTESIAN_POINT ( 'NONE',  ( 0.2764156081756484196, -5.077672346800151106E-17, 0.4494444444444492537 ) ) ;
#20960=CARTESIAN_POINT ( 'NONE',  ( -0.2764156081756484196, 0.1144950937579609918, 0.1473611111111134686 ) ) ;
#20962=CARTESIAN_POINT ( 'NONE',  ( -0.01277271335453335384, 0.5470360373338563065, 0.04287645741408798589 ) ) ;
#20963=CARTESIAN_POINT ( 'NONE',  ( -0.3125000000000000000, 1.913510623667739771E-17, 0.3452777777777818469 ) ) ;
#20970=EDGE_LOOP ( 'NONE', ( #13645, #10549, #20773, #20886 ) ) ;
#20979=CARTESIAN_POINT ( 'NONE',  ( -0.1144950937579609918, -0.2764156081756484196, -0.06097222222222156013 ) ) ;
#20980=CARTESIAN_POINT ( 'NONE',  ( -0.3125000000000000000, 1.913510623667739771E-17, 0.1230555555555578606 ) ) ;
#20984=CARTESIAN_POINT ( 'NONE',  ( 0.1294417382415921358, -0.3125000000000002220, 0.1890277777777802926 ) ) ;
#20986=CARTESIAN_POINT ( 'NONE',  ( 0.000000000000000000, 0.3155070326520292845, 0.1039583333333351234 ) ) ;
#21002=CARTESIAN_POINT ( 'NONE',  ( -0.2530612899223193546, 0.3951608735071495127, 0.4181572966874577135 ) ) ;
#21004=CARTESIAN_POINT ( 'NONE',  ( -0.04581704741057199964, -0.3043534538584903304, -0.09649300259420087733 ) ) ;
#21013=CARTESIAN_POINT ( 'NONE',  ( 0.3874422277197113185, 0.3175760028958486414, 0.4114235598616964862 ) ) ;
#21014=CARTESIAN_POINT ( 'NONE',  ( 0.000000000000000000, 3.738758431839877614E-19, -0.1016666666666665164 ) ) ;
#21023=CARTESIAN_POINT ( 'NONE',  ( 0.2764156081756483641, -0.1144950937579611167, 0.4459722222222269328 ) ) ;
#21037=VERTEX_POINT ( 'NONE', #4713 ) ;
#21045=EDGE_CURVE ( 'NONE', #13469, #17766, #19447, .T. ) ;
#21047=CARTESIAN_POINT ( 'NONE',  ( -3.385114897866767815E-17, -0.2764156081756484196, 0.2133333333333362336 ) ) ;
#21049=CARTESIAN_POINT ( 'NONE',  ( 0.2764156081756484196, -5.077672346800151106E-17, -0.1061111111111107813 ) ) ;
#21052=CARTESIAN_POINT ( 'NONE',  ( 0.01298396664829300738, -0.5473896884649182004, 0.04271845132552136437 ) ) ;
#21055=AXIS2_PLACEMENT_3D ( 'NONE', #23315, #10427, #12381 ) ;
#21064=CARTESIAN_POINT ( 'NONE',  ( 0.3125000000000000555, -5.740531871003217465E-17, 0.1994444444444470055 ) ) ;
#21067=CARTESIAN_POINT ( 'NONE',  ( 0.4641461581055187358, -0.2728099291808114280, 0.04698409998688660855 ) ) ;
#21068=CARTESIAN_POINT ( 'NONE',  ( 0.2764156081756483641, 0.1144950937579610056, 0.3973611111111154393 ) ) ;
#21071=EDGE_CURVE ( 'NONE', #1241, #20894, #20822, .T. ) ;
#21077=CARTESIAN_POINT ( 'NONE',  ( -0.1689451345729832410, -0.2321341939677299682, -0.07613786318562981714 ) ) ;
#21078=CARTESIAN_POINT ( 'NONE',  ( 0.2764156081756484196, -5.077672346800151106E-17, 0.1786111111111136907 ) ) ;
#21091=CARTESIAN_POINT ( 'NONE',  ( 0.3084988159814222586, 0.02958440236011267849, 0.4201654826480894500 ) ) ;
#21093=CARTESIAN_POINT ( 'NONE',  ( 0.01848103877824613592, -0.5441716683897390716, 0.04413116910601658227 ) ) ;
#21094=EDGE_CURVE ( 'NONE', #12631, #6271, #7591, .T. ) ;
#21098=MECHANICAL_CONTEXT ( 'NONE', #9823, 'mechanical' ) ;
#21104=CARTESIAN_POINT ( 'NONE',  ( 0.1954553509668047195, 0.1954553509668046085, -0.03666666666666580643 ) ) ;
#21105=DIRECTION ( 'NONE',  ( 0.5000000000000012212, 0.8660254037844380415, 0.000000000000000000 ) ) ;
#21111=CARTESIAN_POINT ( 'NONE',  ( 0.3155070326520292845, -5.795770164686806123E-17, 0.2011805555555581104 ) ) ;
#21113=CARTESIAN_POINT ( 'NONE',  ( -0.4805070082343984583, -0.2560807851245831546, 0.04413116910601652676 ) ) ;
#21116=VERTEX_POINT ( 'NONE', #23922 ) ;
#21130=EDGE_CURVE ( 'NONE', #20864, #23410, #4445, .T. ) ;
#21135=ORIENTED_EDGE ( 'NONE', *, *, #11289, .T. ) ;
#21141=B_SPLINE_CURVE_WITH_KNOTS ( 'NONE', 3,
 ( #16190, #5073, #23239, #10111, #17534, #827, #8257, #15706, #23121, #13885 ),
 .UNSPECIFIED., .F., .F.,
 ( 4, 2, 2, 2, 4 ),
 ( 0.000000000000000000, 0.003321633220911225995, 0.006643266441822451990, 0.009964899662733674515, 0.01328653288364490051 ),
 .UNSPECIFIED. ) ;
#21157=EDGE_LOOP ( 'NONE', ( #16570, #23480, #16117, #4413, #18173, #16180, #5381, #23419, #24057, #17013, #2792, #13351, #1479, #17410, #17028, #10995, #2609, #15197, #8112, #20680, #23575, #21135, #10969, #21332, #1231, #21228 ) ) ;
#21158=ADVANCED_FACE ( 'NONE', ( #23677 ), #21982, .T. ) ;
#21159=CARTESIAN_POINT ( 'NONE',  ( -0.1527521626045862113, -0.4420638983541222422, 0.4298724737630855164 ) ) ;
#21168=CARTESIAN_POINT ( 'NONE',  ( -0.2764156081756484196, -0.1144950937579609362, 0.2029166666666694652 ) ) ;
#21170=CARTESIAN_POINT ( 'NONE',  ( 0.1954553509668047195, 0.1954553509668046085, 0.4633333333333381487 ) ) ;
#21176=CARTESIAN_POINT ( 'NONE',  ( 0.3124999999999999445, -0.1294417382415923856, 0.3626388888888927853 ) ) ;
#21187=CARTESIAN_POINT ( 'NONE',  ( 0.3124999999999989453, -0.1294417382415934403, 0.09180555555555759695 ) ) ;
#21190=CARTESIAN_POINT ( 'NONE',  ( -0.2230971623002954152, -0.2230971623002953874, 0.01715277777777927601 ) ) ;
#21199=EDGE_LOOP ( 'NONE', ( #13446, #905, #3591, #16400 ) ) ;
#21201=CARTESIAN_POINT ( 'NONE',  ( -0.003269416932270002331, 0.5491886443627419512, 0.04193793378272828165 ) ) ;
#21208=CARTESIAN_POINT ( 'NONE',  ( -0.04345060704004083396, 0.5161796576942548898, 0.4013192973759855953 ) ) ;
#21216=CARTESIAN_POINT ( 'NONE',  ( 0.1650495903302502676, 0.4585922144775744780, 0.07156651416104257979 ) ) ;
#21217=CARTESIAN_POINT ( 'NONE',  ( 0.4593750000000003664, -0.2760455974562899817, 0.3779506566538943235 ) ) ;
#21225=CARTESIAN_POINT ( 'NONE',  ( 0.2764156081756484196, -5.077672346800151106E-17, 0.1230555555555576941 ) ) ;
#21228=ORIENTED_EDGE ( 'NONE', *, *, #843, .T. ) ;
#21230=CARTESIAN_POINT ( 'NONE',  ( 0.4800173678775926378, 0.1715347676940233990, 0.06110638151955335995 ) ) ;
#21233=CARTESIAN_POINT ( 'NONE',  ( 0.2230971623002954429, 0.2230971623002953319, 0.2636805555555586378 ) ) ;
#21234=ORIENTED_EDGE ( 'NONE', *, *, #8159, .F. ) ;
#21235=CARTESIAN_POINT ( 'NONE',  ( 0.2209708691207961651, 0.2209708691207959985, 0.03972222222222351884 ) ) ;
#21241=EDGE_CURVE ( 'NONE', #960, #14698, #18706, .T. ) ;
#21252=CARTESIAN_POINT ( 'NONE',  ( 0.1541993830832357193, -0.2301090524147265115, 0.3880822748423152224 ) ) ;
#21256=CARTESIAN_POINT ( 'NONE',  ( 0.2229532752983993393, 0.1767350293216415902, 0.3955450596469902713 ) ) ;
#21277=ORIENTED_EDGE ( 'NONE', *, *, #19502, .F. ) ;
#21288=CARTESIAN_POINT ( 'NONE',  ( 0.1294417382415921358, -0.3125000000000002220, -0.08180555555555486802 ) ) ;
#21289=CARTESIAN_POINT ( 'NONE',  ( 0.4687500000000002776, 0.2598076211353318454, 0.06112444011295372487 ) ) ;
#21291=CARTESIAN_POINT ( 'NONE',  ( -0.2764156081756484196, 0.1144950937579609918, 0.08486111111111295513 ) ) ;
#21292=ORIENTED_EDGE ( 'NONE', *, *, #3456, .F. ) ;
#21295=CARTESIAN_POINT ( 'NONE',  ( 0.4592359490081627804, -0.08899061577413990010, 0.4306447894611612481 ) ) ;
#21298=DIRECTION ( 'NONE',  ( -0.5000000000000001110, 0.8660254037844385966, 0.000000000000000000 ) ) ;
#21301=EDGE_CURVE ( 'NONE', #9027, #20864, #10017, .T. ) ;
#21309=( BOUNDED_CURVE ( )  B_SPLINE_CURVE ( 2, ( #7702, #18797, #15267, #3806, #9534, #20984, #22815, #2092, #5755 ),
 .UNSPECIFIED., .F., .T. ) 
 B_SPLINE_CURVE_WITH_KNOTS ( ( 3, 2, 2, 2, 3 ),
 ( 0.4375000000000000555, 0.4479166666666667407, 0.4583333333333333703, 0.4687500000000000555, 0.4791666666666667407 ),
 .UNSPECIFIED. ) 
 CURVE ( )  GEOMETRIC_REPRESENTATION_ITEM ( )  RATIONAL_B_SPLINE_CURVE ( ( 0.9999999999999995559, 0.9238795325112871826, 1.000000000000000000, 0.9238795325112867385, 1.000000000000000000, 0.9238795325112867385, 1.000000000000000000, 0.9238795325112862944, 1.000000000000000444 ) ) 
 REPRESENTATION_ITEM ( '' )  );
#21312=CARTESIAN_POINT ( 'NONE',  ( -0.3155070326520293400, 0.1306872919485614903, -0.04881944444444345776 ) ) ;
#21313=LINE ( 'NONE', #8369, #23938 ) ;
#21316=FACE_OUTER_BOUND ( 'NONE', #13472, .T. ) ;
#21317=CARTESIAN_POINT ( 'NONE',  ( 0.1954553509668046640, -0.1954553509668047195, 0.1161111111111132049 ) ) ;
#21318=CARTESIAN_POINT ( 'NONE',  ( 0.4784936136544857277, -0.2687202946394928182, 0.04212966708837330432 ) ) ;
#21319=CARTESIAN_POINT ( 'NONE',  ( 0.009374999999999774139, 0.5358532185916217161, 0.06112444011295372487 ) ) ;
#21332=ORIENTED_EDGE ( 'NONE', *, *, #3456, .T. ) ;
#21334=CARTESIAN_POINT ( 'NONE',  ( -0.3125000000000000000, -0.1294417382415921913, -0.04013888888888785672 ) ) ;
#21336=CARTESIAN_POINT ( 'NONE',  ( 0.2775113281607683446, -0.3935459114639780487, 0.07438423612653363715 ) ) ;
#21338=CIRCLE ( 'NONE', #22499, 0.01875000000000002359 ) ;
#21339=CARTESIAN_POINT ( 'NONE',  ( -0.2742360776603882666, -0.1498359893665253684, -0.1016666666666679597 ) ) ;
#21341=CARTESIAN_POINT ( 'NONE',  ( -0.1144950937579609779, 0.2764156081756484196, -0.03319444444444354797 ) ) ;
#21344=CARTESIAN_POINT ( 'NONE',  ( 0.3125000000000000000, -5.740531871003217465E-17, -0.07833333333333296344 ) ) ;
#21345=CARTESIAN_POINT ( 'NONE',  ( 0.2209708691207961095, -0.2209708691207961651, 0.3036111111111144956 ) ) ;
#21346=CARTESIAN_POINT ( 'NONE',  ( 0.2764156081756484196, -5.077672346800151106E-17, 0.1786111111111136907 ) ) ;
#21351=CARTESIAN_POINT ( 'NONE',  ( -0.2209708691207961095, 0.2209708691207961373, -0.001944444444443472510 ) ) ;
#21352=CARTESIAN_POINT ( 'NONE',  ( 0.3155070326520292290, 0.1306872919485615736, 0.4824305555555604141 ) ) ;
#21355=CARTESIAN_POINT ( 'NONE',  ( 0.000000000000000000, 0.3125000000000000000, 0.04666666666666802188 ) ) ;
#21367=CARTESIAN_POINT ( 'NONE',  ( 0.3124999999999993339, 0.1294417382415928297, 0.3765277777777821244 ) ) ;
#21369=CARTESIAN_POINT ( 'NONE',  ( 0.2742360776605723416, -0.1498359893662102316, 0.4241666666666772390 ) ) ;
#21379=FACE_OUTER_BOUND ( 'NONE', #15349, .T. ) ;
#21383=ADVANCED_FACE ( 'NONE', ( #7923 ), #295, .F. ) ;
#21385=LINE ( 'NONE', #17725, #8594 ) ;
#21389=DIRECTION ( 'NONE',  ( -0.8320502943378438321, -0.4803844614152618653, -0.2773500981126136300 ) ) ;
#21397=ADVANCED_FACE ( 'NONE', ( #13267 ), #9590, .F. ) ;
#21398=EDGE_CURVE ( 'NONE', #9027, #3958, #16544, .T. ) ;
#21401=CARTESIAN_POINT ( 'NONE',  ( -0.4581189881604794678, -0.2644951211353319120, 0.3941886329748524598 ) ) ;
#21406=CARTESIAN_POINT ( 'NONE',  ( -0.4687500000000004441, 0.2174757758404408658, 0.3901708077920437723 ) ) ;
#21410=CARTESIAN_POINT ( 'NONE',  ( -0.2764156081756484196, -0.1144950937579609362, -0.01930555555555453148 ) ) ;
#21415=CARTESIAN_POINT ( 'NONE',  ( -0.3125000000000000000, 1.913510623667739771E-17, -0.09916666666666609786 ) ) ;
#21421=AXIS2_PLACEMENT_3D ( 'NONE', #11374, #2229, #16858 ) ;
#21422=CARTESIAN_POINT ( 'NONE',  ( 0.4224968603155544455, 0.2973372013303175465, 0.07046346805502540223 ) ) ;
#21426=CARTESIAN_POINT ( 'NONE',  ( 0.4805453593044337612, -0.2624503992731451185, 0.04271845132551427976 ) ) ;
#21427=CARTESIAN_POINT ( 'NONE',  ( -0.1306872919485614903, 0.3155070326520293400, -0.0002083333333319594999 ) ) ;
#21428=CARTESIAN_POINT ( 'NONE',  ( 0.1966284714786247223, 0.4277423764267400674, 0.07944889038204620835 ) ) ;
#21435=CARTESIAN_POINT ( 'NONE',  ( 0.2764156081756483641, 0.1144950937579610056, -0.04013888888888804407 ) ) ;
#21437=FACE_OUTER_BOUND ( 'NONE', #16730, .T. ) ;
#21438=CARTESIAN_POINT ( 'NONE',  ( 0.000000000000000000, 0.2764156081756484196, 0.3036111111111146621 ) ) ;
#21441=DIRECTION ( 'NONE',  ( -3.642463991552349380E-15, -0.2142211582677920889, -0.9767851838303064360 ) ) ;
#21447=DIRECTION ( 'NONE',  ( -0.000000000000000000, -0.000000000000000000, -1.000000000000000000 ) ) ;
#21448=CARTESIAN_POINT ( 'NONE',  ( -0.2534589807566942632, 0.3949312665968688352, 0.4181462219997566510 ) ) ;
#21453=CARTESIAN_POINT ( 'NONE',  ( 0.4875000000000002665, 0.2598076211353318454, 0.06112444011295372487 ) ) ;
#21458=CARTESIAN_POINT ( 'NONE',  ( -0.4687500000000003886, -0.04413379556123714353, 0.09139253360868644649 ) ) ;
#21459=CARTESIAN_POINT ( 'NONE',  ( -0.1954553509668046640, 0.1954553509668046918, -0.08527777777777728607 ) ) ;
#21463=CARTESIAN_POINT ( 'NONE',  ( 0.1954553509668046640, -0.1954553509668047195, 0.1161111111111132049 ) ) ;
#21466=CARTESIAN_POINT ( 'NONE',  ( 0.4796773874647223823, 0.08638538962819194977, 0.07156402152810012463 ) ) ;
#21470=CARTESIAN_POINT ( 'NONE',  ( -0.3155070326520293400, 0.1306872919485614903, 0.2810416666666698537 ) ) ;
#21498=DIRECTION ( 'NONE',  ( 0.4999999999999994449, -0.8660254037844390407, 0.000000000000000000 ) ) ;
#21502=CARTESIAN_POINT ( 'NONE',  ( 0.4687500000000003886, -0.2170120125989245807, 0.07051005015414461841 ) ) ;
#21504=FACE_OUTER_BOUND ( 'NONE', #19197, .T. ) ;
#21511=ADVANCED_FACE ( 'NONE', ( #16790 ), #1073, .F. ) ;
#21515=FACE_OUTER_BOUND ( 'NONE', #14449, .T. ) ;
#21519=CARTESIAN_POINT ( 'NONE',  ( -0.4591127969567741496, -0.1126020057588260487, 0.4269506497667299172 ) ) ;
#21525=CARTESIAN_POINT ( 'NONE',  ( 0.1144950937579609085, -0.2764156081756484751, 0.1056944444444464504 ) ) ;
#21528=CARTESIAN_POINT ( 'NONE',  ( 0.3125000000000009437, -0.1294417382415913309, 0.4181944444444486986 ) ) ;
#21535=ADVANCED_FACE ( 'NONE', ( #21515 ), #9955, .F. ) ;
#21536=CARTESIAN_POINT ( 'NONE',  ( -0.1294417382415922191, 0.3125000000000000000, 0.1612500000000022526 ) ) ;
#21538=CARTESIAN_POINT ( 'NONE',  ( 0.4593750000000003664, 0.2760455974562901482, 0.06112444011295366936 ) ) ;
#21543=CARTESIAN_POINT ( 'NONE',  ( 0.4687500000000003886, -0.2630309001378767775, 0.05971062996525598743 ) ) ;
#21544=CARTESIAN_POINT ( 'NONE',  ( 0.2230971623002953874, -0.2230971623002954429, 0.03104166666666828903 ) ) ;
#21549=CARTESIAN_POINT ( 'NONE',  ( 0.1954553509668046640, -0.1954553509668047195, -0.05055555555555479863 ) ) ;
#21552=CARTESIAN_POINT ( 'NONE',  ( -0.2764156081756484196, 1.692557448933383907E-17, 0.4286111111111156613 ) ) ;
#21563=CARTESIAN_POINT ( 'NONE',  ( -0.1517119284478178620, 0.4426845032613772601, 0.4305326508994914980 ) ) ;
#21571=CARTESIAN_POINT ( 'NONE',  ( 0.1144950937579609085, -0.2764156081756484751, -0.06097222222222153931 ) ) ;
#21576=CARTESIAN_POINT ( 'NONE',  ( -0.2764156081756484196, 0.1144950937579609918, 0.1473611111111134409 ) ) ;
#21579=CARTESIAN_POINT ( 'NONE',  ( -0.2816345655934842651, 0.09282869753838723925, 0.4076009914526265154 ) ) ;
#21581=LINE ( 'NONE', #17572, #6240 ) ;
#21582=CARTESIAN_POINT ( 'NONE',  ( 0.2764156081756484196, -5.077672346800151106E-17, 0.005000000000001210074 ) ) ;
#21583=CARTESIAN_POINT ( 'NONE',  ( 0.3155070326520292290, 0.1306872919485615736, 0.3157638888888923967 ) ) ;
#21585=EDGE_LOOP ( 'NONE', ( #13729, #16993, #8517, #3632 ) ) ;
#21587=CARTESIAN_POINT ( 'NONE',  ( -0.4581189881604794678, -0.2644951211353319120, 0.3941886329748524598 ) ) ;
#21588=( BOUNDED_CURVE ( )  B_SPLINE_CURVE ( 2, ( #21064, #11809, #15580, #19356, #23002, #3369, #10820, #14228, #10581 ),
 .UNSPECIFIED., .F., .F. ) 
 B_SPLINE_CURVE_WITH_KNOTS ( ( 3, 2, 2, 2, 3 ),
 ( 0.4791666666666667407, 0.4895833333333333703, 0.5000000000000001110, 0.5104166666666667407, 0.5208333333333334814 ),
 .UNSPECIFIED. ) 
 CURVE ( )  GEOMETRIC_REPRESENTATION_ITEM ( )  RATIONAL_B_SPLINE_CURVE ( ( 0.9999999999999995559, 0.9238795325112871826, 1.000000000000000000, 0.9238795325112867385, 1.000000000000000000, 0.9238795325112867385, 1.000000000000000000, 0.9238795325112859613, 1.000000000000000888 ) ) 
 REPRESENTATION_ITEM ( '' )  );
#21598=B_SPLINE_CURVE_WITH_KNOTS ( 'NONE', 3,
 ( #9975, #8613, #8481, #15808, #6300, #17402 ),
 .UNSPECIFIED., .F., .F.,
 ( 4, 2, 4 ),
 ( 0.000000000000000000, 0.0002551367231383052498, 0.0005102734462766104996 ),
 .UNSPECIFIED. ) ;
#21599=CARTESIAN_POINT ( 'NONE',  ( 0.3125000000000000000, -5.740531871003217465E-17, -0.07833333333333296344 ) ) ;
#21608=ORIENTED_EDGE ( 'NONE', *, *, #3070, .T. ) ;
#21613=ORIENTED_EDGE ( 'NONE', *, *, #20932, .F. ) ;
#21615=DIRECTION ( 'NONE',  ( -1.000000000000000000, 0.000000000000000000, 0.000000000000000000 ) ) ;
#21620=DIRECTION ( 'NONE',  ( -1.000000000000000000, -1.224646799147357891E-16, 0.000000000000000000 ) ) ;
#21624=CARTESIAN_POINT ( 'NONE',  ( -0.2769159822048601893, -0.3938884537237697381, 0.07441357458167788264 ) ) ;
#21637=ORIENTED_EDGE ( 'NONE', *, *, #9929, .F. ) ;
#21645=EDGE_CURVE ( 'NONE', #9832, #4238, #17740, .T. ) ;
#21646=CARTESIAN_POINT ( 'NONE',  ( -0.4687500000000195954, -0.04505700071786207517, 0.4280213696812118496 ) ) ;
#21650=ORIENTED_EDGE ( 'NONE', *, *, #13522, .T. ) ;
#21653=CARTESIAN_POINT ( 'NONE',  ( -0.2764156081756484196, -0.1144950937579609362, 0.03625000000000147549 ) ) ;
#21656=CARTESIAN_POINT ( 'NONE',  ( 0.1514593411830787995, 0.2498004213170063048, -0.08114360514506319122 ) ) ;
#21668=CARTESIAN_POINT ( 'NONE',  ( 0.3155070326520292845, -5.795770164686806123E-17, 0.03798611111111277472 ) ) ;
#21670=EDGE_CURVE ( 'NONE', #10074, #23426, #19563, .T. ) ;
#21675=CARTESIAN_POINT ( 'NONE',  ( -0.1954553509668046640, 0.1954553509668046918, -0.02277777777777679341 ) ) ;
#21676=CARTESIAN_POINT ( 'NONE',  ( 0.2742360776605723416, -0.1498359893662102316, 0.4241666666666772390 ) ) ;
#21679=ADVANCED_FACE ( 'NONE', ( #4450 ), #19448, .T. ) ;
#21689=FACE_OUTER_BOUND ( 'NONE', #23935, .T. ) ;
#21690=ORIENTED_EDGE ( 'NONE', *, *, #6726, .T. ) ;
#21693=CYLINDRICAL_SURFACE ( 'NONE', #2978, 0.3125000000000000000 ) ;
#21694=CARTESIAN_POINT ( 'NONE',  ( 0.4687500000000002776, -0.2598076211353317344, 0.06112444011295376650 ) ) ;
#21698=CARTESIAN_POINT ( 'NONE',  ( 0.1144950937579611444, 0.2764156081756483641, 0.07097222222222394905 ) ) ;
#21704=CARTESIAN_POINT ( 'NONE',  ( 0.2764156081756484196, -5.077672346800151106E-17, 0.2897222222222257115 ) ) ;
#21707=CARTESIAN_POINT ( 'NONE',  ( 0.2209708691207961651, 0.2209708691207959985, -0.06444444444444361042 ) ) ;
#21709=FACE_OUTER_BOUND ( 'NONE', #3173, .T. ) ;
#21710=CARTESIAN_POINT ( 'NONE',  ( -0.2764156081756484196, 0.1144950937579609918, 0.02930555555555695163 ) ) ;
#21711=CARTESIAN_POINT ( 'NONE',  ( -0.3155070326520293400, 0.1306872919485614903, 0.3365972222222259336 ) ) ;
#21714=EDGE_LOOP ( 'NONE', ( #16934, #12646, #17593, #14500 ) ) ;
#21715=CARTESIAN_POINT ( 'NONE',  ( 0.4253970711649990855, 0.3089455473570085764, 0.05347937985141010958 ) ) ;
#21716=CARTESIAN_POINT ( 'NONE',  ( 0.4581189881604794123, 0.2644951211353319676, 0.3941886329748524598 ) ) ;
#21725=AXIS2_PLACEMENT_3D ( 'NONE', #21832, #8665, #19647 ) ;
#21737=CIRCLE ( 'NONE', #1493, 0.01874999999999997155 ) ;
#21749=CARTESIAN_POINT ( 'NONE',  ( 0.4687500000000002776, 0.2170121405309677343, 0.07051002209705400925 ) ) ;
#21751=CARTESIAN_POINT ( 'NONE',  ( -0.4593750000000003664, -0.2760455974562900927, 0.06112444011295366242 ) ) ;
#21752=DIRECTION ( 'NONE',  ( -1.000000000000000000, -1.224646799147353700E-16, 0.000000000000000000 ) ) ;
#21768=ORIENTED_EDGE ( 'NONE', *, *, #20901, .T. ) ;
#21771=CARTESIAN_POINT ( 'NONE',  ( 0.1954553509668046640, -0.1954553509668047195, -0.001944444444443294917 ) ) ;
#21774=CARTESIAN_POINT ( 'NONE',  ( 0.3125000000000000000, -5.740531871003217465E-17, 0.4216666666666709085 ) ) ;
#21781=ORIENTED_EDGE ( 'NONE', *, *, #22272, .T. ) ;
#21785=CARTESIAN_POINT ( 'NONE',  ( -0.3155070326520293400, -0.1306872919485614626, 0.2359027777777810142 ) ) ;
#21789=DIRECTION ( 'NONE',  ( -0.000000000000000000, -0.000000000000000000, -1.000000000000000000 ) ) ;
#21790=CARTESIAN_POINT ( 'NONE',  ( -0.1954553509668046918, -0.1954553509668046640, 0.1022222222222241989 ) ) ;
#21798=CARTESIAN_POINT ( 'NONE',  ( 0.3125000000000000000, 3.827021247335477694E-17, 1.326383476483184332 ) ) ;
#21801=AXIS2_PLACEMENT_3D ( 'NONE', #17337, #22334, #13102 ) ;
#21805=DIRECTION ( 'NONE',  ( -0.000000000000000000, -0.000000000000000000, -1.000000000000000000 ) ) ;
#21813=CARTESIAN_POINT ( 'NONE',  ( 0.1144950937579609085, -0.2764156081756484751, -0.005416666666665539281 ) ) ;
#21819=CARTESIAN_POINT ( 'NONE',  ( 0.4800180059626117934, 0.1716568225058809349, 0.06108596828699448811 ) ) ;
#21822=CARTESIAN_POINT ( 'NONE',  ( 0.2764156081756483641, -0.1144950937579611028, 0.001527777777778966360 ) ) ;
#21823=CARTESIAN_POINT ( 'NONE',  ( -0.3155070326520292845, 1.931923388228935888E-17, 0.3956250000000041123 ) ) ;
#21827=CARTESIAN_POINT ( 'NONE',  ( 0.1294417382415921358, -0.3125000000000002220, 0.02236111111111226818 ) ) ;
#21832=CARTESIAN_POINT ( 'NONE',  ( 0.000000000000000000, 3.738758431839877614E-19, -0.1199999999999999956 ) ) ;
#21839=CARTESIAN_POINT ( 'NONE',  ( -0.2800968539712042626, 1.715098578335394762E-17, -0.06926352063787094560 ) ) ;
#21844=DIRECTION ( 'NONE',  ( 0.000000000000000000, 0.000000000000000000, -1.000000000000000000 ) ) ;
#21867=CARTESIAN_POINT ( 'NONE',  ( -0.4687499999999988898, -0.2570931668155639338, 0.04874733047934373675 ) ) ;
#21873=EDGE_CURVE ( 'NONE', #23426, #7279, #19522, .T. ) ;
#21884=DIRECTION ( 'NONE',  ( 0.000000000000000000, 0.000000000000000000, 1.000000000000000000 ) ) ;
#21886=ORIENTED_EDGE ( 'NONE', *, *, #10578, .F. ) ;
#21891=CARTESIAN_POINT ( 'NONE',  ( 0.1144950937579609085, -0.2764156081756484751, 0.3834722222222265442 ) ) ;
#21893=CARTESIAN_POINT ( 'NONE',  ( 0.08187103065728440487, 0.2793464338139753922, -0.07965142539470895788 ) ) ;
#21894=CARTESIAN_POINT ( 'NONE',  ( -0.4687500000000003886, -0.2598076211353319009, 0.06112444011295369711 ) ) ;
#21903=CARTESIAN_POINT ( 'NONE',  ( -0.3155070326520293400, 0.1306872919485614903, 0.2845138888888925077 ) ) ;
#21905=CARTESIAN_POINT ( 'NONE',  ( -0.5601250000000235207, -6.859552883724400952E-17, -0.05999999999999999084 ) ) ;
#21908=CARTESIAN_POINT ( 'NONE',  ( 0.000000000000000000, 0.2764156081756484196, 0.3036111111111146621 ) ) ;
#21915=CARTESIAN_POINT ( 'NONE',  ( -0.4784936136544858387, 0.2687202946394925962, 0.04212966708837331820 ) ) ;
#21917=B_SPLINE_CURVE_WITH_KNOTS ( 'NONE', 3,
 ( #15455, #692, #11796, #8237, #6297, #21295, #23105, #17280 ),
 .UNSPECIFIED., .F., .F.,
 ( 4, 2, 2, 4 ),
 ( 8.673617379884035472E-19, 0.001711848256466968511, 0.003423696512933936155, 0.006847393025867874912 ),
 .UNSPECIFIED. ) ;
#21925=AXIS2_PLACEMENT_3D ( 'NONE', #7520, #22391, #5692 ) ;
#21927=CARTESIAN_POINT ( 'NONE',  ( -0.1144950937579609779, 0.2764156081756484196, 0.1334722222222244348 ) ) ;
#21929=CARTESIAN_POINT ( 'NONE',  ( 0.000000000000000000, 0.000000000000000000, 1.326383476483184332 ) ) ;
#21936=CARTESIAN_POINT ( 'NONE',  ( -0.1829869529092254532, 0.2292256185136192503, 0.4043689316861039940 ) ) ;
#21938=EDGE_CURVE ( 'NONE', #6271, #12631, #992, .T. ) ;
#21940=CARTESIAN_POINT ( 'NONE',  ( 0.2764156081756483641, -0.1144950937579611028, 0.05708333333333497073 ) ) ;
#21941=CARTESIAN_POINT ( 'NONE',  ( 0.2764156081756484196, -5.077672346800151106E-17, -0.04361111111111028865 ) ) ;
#21950=ADVANCED_FACE ( 'NONE', ( #10142 ), #407, .F. ) ;
#21953=FACE_OUTER_BOUND ( 'NONE', #1232, .T. ) ;
#21964=CARTESIAN_POINT ( 'NONE',  ( -0.4607728391470959362, 0.2757711312522204139, 0.04763613967037565872 ) ) ;
#21970=ORIENTED_EDGE ( 'NONE', *, *, #228, .F. ) ;
#21975=CARTESIAN_POINT ( 'NONE',  ( 0.2230971623002953874, -0.2230971623002954429, 0.02756944444444561770 ) ) ;
#21982=TOROIDAL_SURFACE ( 'NONE', #4068, 0.6211549996190571798, 0.01874999999999999931 ) ;
#21985=CARTESIAN_POINT ( 'NONE',  ( 0.4687500000000002776, -0.2598076211353317344, 0.06112444011295376650 ) ) ;
#21994=ORIENTED_EDGE ( 'NONE', *, *, #12651, .F. ) ;
#21996=CARTESIAN_POINT ( 'NONE',  ( -0.2709282478162917118, -0.1304588658952868796, 0.4118983757380794697 ) ) ;
#22009=CARTESIAN_POINT ( 'NONE',  ( 7.345979252745889464E-17, -0.5196152422706635798, 0.3779506566538943235 ) ) ;
#22010=CARTESIAN_POINT ( 'NONE',  ( -0.2764156081756484196, 1.692557448933383907E-17, 0.1994444444444472553 ) ) ;
#22023=ORIENTED_EDGE ( 'NONE', *, *, #643, .T. ) ;
#22024=CARTESIAN_POINT ( 'NONE',  ( -0.1306872919485614903, 0.3155070326520293400, 0.3331250000000040012 ) ) ;
#22025=CARTESIAN_POINT ( 'NONE',  ( -0.3125000000000000000, 1.913510623667739771E-17, 0.01194444444444589179 ) ) ;
#22031=CARTESIAN_POINT ( 'NONE',  ( -3.385114897866767815E-17, -0.2764156081756484196, 0.3313888888888926743 ) ) ;
#22048=DIRECTION ( 'NONE',  ( -1.000000000000000000, 0.000000000000000000, 0.000000000000000000 ) ) ;
#22052=CARTESIAN_POINT ( 'NONE',  ( -0.1064715942168695945, -0.2552471790383887273, -0.06558227484231508864 ) ) ;
#22053=CARTESIAN_POINT ( 'NONE',  ( 0.2764156081756484196, -5.077672346800151106E-17, 0.1716666666666692431 ) ) ;
#22055=FACE_OUTER_BOUND ( 'NONE', #18100, .T. ) ;
#22058=CARTESIAN_POINT ( 'NONE',  ( 0.01277271335453323588, -0.5470360373338564175, 0.04287645741408792344 ) ) ;
#22064=FACE_OUTER_BOUND ( 'NONE', #2121, .T. ) ;
#22065=CARTESIAN_POINT ( 'NONE',  ( -0.2230971623002953874, 0.2230971623002954152, 0.4997916666666716301 ) ) ;
#22066=ORIENTED_EDGE ( 'NONE', *, *, #12675, .T. ) ;
#22076=ORIENTED_EDGE ( 'NONE', *, *, #10580, .T. ) ;
#22080=TOROIDAL_SURFACE ( 'NONE', #4571, 0.3385998376278290256, 0.01874999999999999931 ) ;
#22081=( BOUNDED_CURVE ( )  B_SPLINE_CURVE ( 2, ( #23468, #15807, #10574, #13988, #10455, #17882, #8612, #6778, #14221 ),
 .UNSPECIFIED., .F., .T. ) 
 B_SPLINE_CURVE_WITH_KNOTS ( ( 3, 2, 2, 2, 3 ),
 ( 0.1041666666666666990, 0.1145833333333333565, 0.1250000000000000278, 0.1354166666666666852, 0.1458333333333333703 ),
 .UNSPECIFIED. ) 
 CURVE ( )  GEOMETRIC_REPRESENTATION_ITEM ( )  RATIONAL_B_SPLINE_CURVE ( ( 0.9999999999999997780, 0.9238795325112869605, 1.000000000000000000, 0.9238795325112867385, 1.000000000000000000, 0.9238795325112867385, 1.000000000000000000, 0.9238795325112865164, 1.000000000000000222 ) ) 
 REPRESENTATION_ITEM ( '' )  );
#22086=EDGE_CURVE ( 'NONE', #8442, #6063, #13564, .T. ) ;
#22096=CARTESIAN_POINT ( 'NONE',  ( -0.1306872919485614903, 0.3155070326520293400, -0.003680555555554630362 ) ) ;
#22115=AXIS2_PLACEMENT_3D ( 'NONE', #18999, #13643, #4114 ) ;
#22116=ORIENTED_EDGE ( 'NONE', *, *, #22086, .F. ) ;
#22119=VERTEX_POINT ( 'NONE', #7309 ) ;
#22121=CARTESIAN_POINT ( 'NONE',  ( 0.000000000000000000, 3.738758431839877614E-19, 0.4425000000000000044 ) ) ;
#22128=CARTESIAN_POINT ( 'NONE',  ( 0.2764156081756483641, 0.1144950937579610056, 0.1751388888888914530 ) ) ;
#22132=CARTESIAN_POINT ( 'NONE',  ( -0.4687500000000004996, -0.1740109699597049420, 0.07813294176666467361 ) ) ;
#22142=CARTESIAN_POINT ( 'NONE',  ( 0.2742360776605723416, -0.1498359893662102316, 0.4241666666666772390 ) ) ;
#22146=CARTESIAN_POINT ( 'NONE',  ( -0.2230971623002953874, 0.2230971623002954152, 0.1699305555555582770 ) ) ;
#22149=CARTESIAN_POINT ( 'NONE',  ( 0.3296559951169310554, -0.3509388998445404639, 0.4107594315541606700 ) ) ;
#22153=CARTESIAN_POINT ( 'NONE',  ( 0.1954553509668047195, 0.1954553509668046085, 0.2966666666666701313 ) ) ;
#22156=ADVANCED_FACE ( 'NONE', ( #14759 ), #2169, .F. ) ;
#22158=CARTESIAN_POINT ( 'NONE',  ( -0.4581189881604794678, 0.2644951211353315235, 0.3941886329748525153 ) ) ;
#22161=CARTESIAN_POINT ( 'NONE',  ( -0.3125000000000010547, 0.1294417382415911921, 0.3348611111111147731 ) ) ;
#22169=CARTESIAN_POINT ( 'NONE',  ( 0.3125000000000009437, -0.1294417382415913309, 0.1404166666666687990 ) ) ;
#22174=DIRECTION ( 'NONE',  ( -0.5000000000000012212, -0.8660254037844380415, 0.000000000000000000 ) ) ;
#22175=CARTESIAN_POINT ( 'NONE',  ( 0.1144950937579609085, -0.2764156081756484751, 0.3279166666666704089 ) ) ;
#22184=CARTESIAN_POINT ( 'NONE',  ( -0.2764156081756484196, 1.692557448933383907E-17, -0.1269444444444443043 ) ) ;
#22186=VERTEX_POINT ( 'NONE', #18282 ) ;
#22192=ORIENTED_EDGE ( 'NONE', *, *, #1278, .F. ) ;
#22199=AXIS2_PLACEMENT_3D ( 'NONE', #18626, #1919, #9363 ) ;
#22209=ORIENTED_EDGE ( 'NONE', *, *, #18127, .F. ) ;
#22214=CARTESIAN_POINT ( 'NONE',  ( 0.000000000000000000, 0.3155070326520292845, -0.007152777777776874076 ) ) ;
#22215=CARTESIAN_POINT ( 'NONE',  ( -0.3853713378992620897, -0.3187716316911694547, 0.07807775719020886018 ) ) ;
#22231=( BOUNDED_CURVE ( )  B_SPLINE_CURVE ( 2, ( #20963, #13549, #11959, #13775, #13421, #7908, #12076, #11590, #23131 ),
 .UNSPECIFIED., .F., .T. ) 
 B_SPLINE_CURVE_WITH_KNOTS ( ( 3, 2, 2, 2, 3 ),
 ( 0.1562500000000000278, 0.1666666666666667407, 0.1770833333333333703, 0.1875000000000000000, 0.1979166666666667129 ),
 .UNSPECIFIED. ) 
 CURVE ( )  GEOMETRIC_REPRESENTATION_ITEM ( )  RATIONAL_B_SPLINE_CURVE ( ( 0.9999999999999997780, 0.9238795325112869605, 1.000000000000000000, 0.9238795325112867385, 1.000000000000000000, 0.9238795325112867385, 1.000000000000000000, 0.9238795325112869605, 0.9999999999999997780 ) ) 
 REPRESENTATION_ITEM ( '' )  );
#22232=( BOUNDED_SURFACE ( )  B_SPLINE_SURFACE ( 3, 2, ( 
 ( #13634, #17159, #9601 ),
 ( #21052, #13160, #449 ),
 ( #22876, #8001, #19218 ),
 ( #15331, #13276, #11313 ),
 ( #20694, #15210, #3984 ),
 ( #18745, #4342, #9479 ) ),
 .UNSPECIFIED., .F., .F., .F. ) 
 B_SPLINE_SURFACE_WITH_KNOTS ( ( 4, 2, 4 ),
 ( 3, 3 ),
 ( 0.001790663949227913349, 0.002289857484343687730, 0.002789051019459461676 ),
 ( 0.000000000000000000, 1.000000000000000000 ),
 .UNSPECIFIED. ) 
 GEOMETRIC_REPRESENTATION_ITEM ( )  RATIONAL_B_SPLINE_SURFACE ( (
 ( 1.000000000000000000, 0.8285407536241355952, 1.000000000000000000),
 ( 1.000000000000000000, 0.8382697314792180165, 1.000000000000000000),
 ( 1.000000000000000000, 0.8433836253084626700, 1.000000000000000000),
 ( 1.000000000000000000, 0.8433992480894149102, 1.000000000000000000),
 ( 1.000000000000000000, 0.8382827608170251299, 1.000000000000000000),
 ( 1.000000000000000000, 0.8285407536241035098, 1.000000000000000000) ) ) 
 REPRESENTATION_ITEM ( '' )  SURFACE ( )  );
#22236=CARTESIAN_POINT ( 'NONE',  ( 0.1111235690150410432, -0.2883545979860924202, 0.4202375072062948802 ) ) ;
#22244=CARTESIAN_POINT ( 'NONE',  ( 0.000000000000000000, 0.000000000000000000, -0.01143517789850382292 ) ) ;
#22250=B_SPLINE_CURVE_WITH_KNOTS ( 'NONE', 3,
 ( #19261, #6214, #2683, #11600, #21336, #17075, #10133, #8160, #367, #21093 ),
 .UNSPECIFIED., .F., .F.,
 ( 4, 2, 2, 2, 4 ),
 ( 0.000000000000000000, 0.003270554913819860229, 0.006541109827639720459, 0.009811664741459580688, 0.01308221965527943745 ),
 .UNSPECIFIED. ) ;
#22251=CARTESIAN_POINT ( 'NONE',  ( 0.1144950937579611444, 0.2764156081756483641, 0.3487500000000040012 ) ) ;
#22255=CARTESIAN_POINT ( 'NONE',  ( 0.3065849364905491314, 4.945545817829770315E-15, 0.4182516031572158233 ) ) ;
#22263=CARTESIAN_POINT ( 'NONE',  ( 0.3125000000000000000, -5.740531871003217465E-17, 0.2063888888888918416 ) ) ;
#22264=VERTEX_POINT ( 'NONE', #18641 ) ;
#22266=CARTESIAN_POINT ( 'NONE',  ( -0.3155070326520293400, 0.1306872919485614903, 0.1734027777777805146 ) ) ;
#22269=CARTESIAN_POINT ( 'NONE',  ( 0.2537239961729473303, -0.3947782598749511318, 0.4289714952839356332 ) ) ;
#22272=EDGE_CURVE ( 'NONE', #8463, #14698, #1931, .T. ) ;
#22273=EDGE_CURVE ( 'NONE', #5886, #280, #19286, .T. ) ;
#22275=CARTESIAN_POINT ( 'NONE',  ( -0.1144950937579609779, 0.2764156081756484196, 0.2515277777777809587 ) ) ;
#22277=CARTESIAN_POINT ( 'NONE',  ( -0.4795759075923630710, -0.04327657950267028292, 0.07439896364134127027 ) ) ;
#22286=ADVANCED_FACE ( 'NONE', ( #22055 ), #7072, .F. ) ;
#22294=CARTESIAN_POINT ( 'NONE',  ( -0.2764156081756484196, 0.1144950937579609918, 0.2515277777777809587 ) ) ;
#22296=CARTESIAN_POINT ( 'NONE',  ( 0.4788451055546354973, 0.2690082051306184052, 0.04193467568257210065 ) ) ;
#22301=DIRECTION ( 'NONE',  ( -0.000000000000000000, 0.000000000000000000, -1.000000000000000000 ) ) ;
#22302=CARTESIAN_POINT ( 'NONE',  ( 0.2764156081756484196, -5.077672346800151106E-17, -0.09916666666666629215 ) ) ;
#22303=VERTEX_POINT ( 'NONE', #16577 ) ;
#22319=CARTESIAN_POINT ( 'NONE',  ( 0.4795759075923620163, -5.969813580926603513E-13, 0.07439896364136204532 ) ) ;
#22333=CARTESIAN_POINT ( 'NONE',  ( 0.4687500000000002220, -0.1742897399511009748, 0.3995693456591889459 ) ) ;
#22334=DIRECTION ( 'NONE',  ( 0.000000000000000000, 0.000000000000000000, -1.000000000000000000 ) ) ;
#22344=CARTESIAN_POINT ( 'NONE',  ( -0.3886563986012126493, 0.3298860868734690976, 0.06108838700204354683 ) ) ;
#22349=CARTESIAN_POINT ( 'NONE',  ( -0.1850421345840768672, -0.2494223792523551642, -0.09928129690674993013 ) ) ;
#22359=FACE_OUTER_BOUND ( 'NONE', #7683, .T. ) ;
#22366=EDGE_LOOP ( 'NONE', ( #1949, #19471, #19856, #21277 ) ) ;
#22368=CARTESIAN_POINT ( 'NONE',  ( -0.1954553509668046640, 0.1954553509668046918, 0.3591666666666706864 ) ) ;
#22372=CARTESIAN_POINT ( 'NONE',  ( 0.2107770390570962993, -0.2008625216908654920, 0.4022918831151609531 ) ) ;
#22379=AXIS2_PLACEMENT_3D ( 'NONE', #1782, #20321, #23968 ) ;
#22381=ORIENTED_EDGE ( 'NONE', *, *, #8670, .T. ) ;
#22385=CARTESIAN_POINT ( 'NONE',  ( 0.4675613926561236200, 0.2849392891917821302, 0.04271845132551801288 ) ) ;
#22389=CARTESIAN_POINT ( 'NONE',  ( 0.4593750000000004219, -0.2760455974562899262, 0.3779506566538943235 ) ) ;
#22391=DIRECTION ( 'NONE',  ( 0.000000000000000000, 0.000000000000000000, -1.000000000000000000 ) ) ;
#22392=CARTESIAN_POINT ( 'NONE',  ( -0.1144950937579609918, -0.2764156081756484196, 0.04319444444444596465 ) ) ;
#22394=CARTESIAN_POINT ( 'NONE',  ( 0.2764156081756484196, -5.077672346800151106E-17, 0.2341666666666696595 ) ) ;
#22413=AXIS2_PLACEMENT_3D ( 'NONE', #12162, #12277, #17747 ) ;
#22415=CARTESIAN_POINT ( 'NONE',  ( 0.1954553509668046640, -0.1954553509668047195, 0.3869444444444487541 ) ) ;
#22417=ADVANCED_FACE ( 'NONE', ( #18888 ), #17180, .F. ) ;
#22426=CARTESIAN_POINT ( 'NONE',  ( -0.2764156081756484196, 1.692557448933383907E-17, -0.07138888888888829387 ) ) ;
#22427=VERTEX_POINT ( 'NONE', #22896 ) ;
#22433=AXIS2_PLACEMENT_3D ( 'NONE', #11087, #18159, #10728 ) ;
#22437=DIRECTION ( 'NONE',  ( 0.000000000000000000, 0.000000000000000000, 1.000000000000000000 ) ) ;
#22441=CARTESIAN_POINT ( 'NONE',  ( -0.3124999999999989453, 0.1294417382415933293, 0.008472222222223593432 ) ) ;
#22445=AXIS2_PLACEMENT_3D ( 'NONE', #12447, #16332, #1693 ) ;
#22452=ORIENTED_EDGE ( 'NONE', *, *, #8761, .F. ) ;
#22453=ORIENTED_EDGE ( 'NONE', *, *, #9016, .F. ) ;
#22458=CARTESIAN_POINT ( 'NONE',  ( 0.2230971623002954429, 0.2230971623002953319, -0.06965277777777736934 ) ) ;
#22459=CARTESIAN_POINT ( 'NONE',  ( -0.09136153228684393279, -0.5015293579687629677, 0.06108838700204188843 ) ) ;
#22460=DIRECTION ( 'NONE',  ( -1.000000000000000000, 0.000000000000000000, 0.000000000000000000 ) ) ;
#22471=FACE_OUTER_BOUND ( 'NONE', #16030, .T. ) ;
#22479=EDGE_CURVE ( 'NONE', #8797, #4857, #21313, .T. ) ;
#22480=CARTESIAN_POINT ( 'NONE',  ( 0.3064624847683588005, -0.3533192024756442451, 0.4298724737630856274 ) ) ;
#22490=EDGE_LOOP ( 'NONE', ( #19424, #533, #22209, #3300 ) ) ;
#22495=DIRECTION ( 'NONE',  ( 0.000000000000000000, 0.000000000000000000, -1.000000000000000000 ) ) ;
#22499=AXIS2_PLACEMENT_3D ( 'NONE', #7089, #20255, #3541 ) ;
#22501=VERTEX_POINT ( 'NONE', #23479 ) ;
#22506=ORIENTED_EDGE ( 'NONE', *, *, #4559, .F. ) ;
#22508=CARTESIAN_POINT ( 'NONE',  ( 0.4607735603406416525, 0.2757708160731982550, 0.04763592618480202295 ) ) ;
#22512=CARTESIAN_POINT ( 'NONE',  ( 0.3886748462736586696, 0.3298755754955758346, 0.06108448616840177897 ) ) ;
#22513=CARTESIAN_POINT ( 'NONE',  ( 0.04625313968442696516, -0.5145616147176053090, 0.07046346805509963451 ) ) ;
#22514=CIRCLE ( 'NONE', #12028, 0.01875000000000000625 ) ;
#22515=CARTESIAN_POINT ( 'NONE',  ( 0.2764156081756483641, -0.1144950937579611028, 0.2793055555555589708 ) ) ;
#22517=CARTESIAN_POINT ( 'NONE',  ( 0.2764156081756483641, 0.1144950937579610056, -0.1026388888888885437 ) ) ;
#22519=CARTESIAN_POINT ( 'NONE',  ( -0.3125000000000000000, 1.913510623667739771E-17, 0.3938888888888930628 ) ) ;
#22535=ADVANCED_FACE ( 'NONE', ( #1188 ), #6034, .T. ) ;
#22536=CARTESIAN_POINT ( 'NONE',  ( -0.1395639791202931690, -0.4606885764509979775, 0.4108348780186337201 ) ) ;
#22540=CARTESIAN_POINT ( 'NONE',  ( -0.1954553509668046640, 0.1954553509668046918, 0.4147222222222267107 ) ) ;
#22541=CARTESIAN_POINT ( 'NONE',  ( 0.4254318749130432953, 0.3089257318245579587, 0.05347049744907977215 ) ) ;
#22550=CARTESIAN_POINT ( 'NONE',  ( -3.385114897866767815E-17, -0.2764156081756484196, 0.1091666666666686880 ) ) ;
#22552=CARTESIAN_POINT ( 'NONE',  ( 0.4687500000000002776, -0.1744746749511749961, 0.4003434961619801169 ) ) ;
#22567=B_SPLINE_CURVE_WITH_KNOTS ( 'NONE', 3,
 ( #10603, #12688, #14753, #7184, #9250, #18275 ),
 .UNSPECIFIED., .F., .F.,
 ( 4, 2, 4 ),
 ( 5.421010862427522170E-20, 0.0002551367231383057919, 0.0005102734462766114754 ),
 .UNSPECIFIED. ) ;
#22573=CARTESIAN_POINT ( 'NONE',  ( 0.2764156081756483641, -0.1144950937579611028, -0.04708333333333256099 ) ) ;
#22580=CARTESIAN_POINT ( 'NONE',  ( 0.1306872919485614071, -0.3155070326520293955, 0.1907638888888913420 ) ) ;
#22581=CARTESIAN_POINT ( 'NONE',  ( 0.1294417382415921358, -0.3125000000000002220, 0.02930555555555713204 ) ) ;
#22583=CARTESIAN_POINT ( 'NONE',  ( -0.2386280844053225714, -0.1440056533832719254, -0.06619720785293826959 ) ) ;
#22586=EDGE_CURVE ( 'NONE', #5967, #12731, #21141, .T. ) ;
#22594=AXIS2_PLACEMENT_3D ( 'NONE', #12781, #1303, #18129 ) ;
#22597=ADVANCED_FACE ( 'NONE', ( #5446 ), #5277, .T. ) ;
#22603=CARTESIAN_POINT ( 'NONE',  ( 0.2631830812676775877, 0.1021974198356748742, 0.3938365693361317033 ) ) ;
#22620=CARTESIAN_POINT ( 'NONE',  ( -0.1144950937579609779, 0.2764156081756484196, 0.4112500000000044453 ) ) ;
#22626=EDGE_CURVE ( 'NONE', #8318, #1635, #2917, .T. ) ;
#22635=CARTESIAN_POINT ( 'NONE',  ( 0.1306872919485616846, 0.3155070326520292290, 0.4372916666666715191 ) ) ;
#22639=CARTESIAN_POINT ( 'NONE',  ( 0.1144950937579609085, -0.2764156081756484751, 0.3348611111111149397 ) ) ;
#22641=CARTESIAN_POINT ( 'NONE',  ( 0.000000000000000000, 0.2764156081756484196, 0.3522222222222262111 ) ) ;
#22643=CARTESIAN_POINT ( 'NONE',  ( -0.1954553509668046640, 0.1954553509668046918, -0.08527777777777728607 ) ) ;
#22647=CARTESIAN_POINT ( 'NONE',  ( -0.2525416622817135415, 0.1285646679930061709, -0.07191566027702570030 ) ) ;
#22650=CARTESIAN_POINT ( 'NONE',  ( 0.2798077087188375889, -0.01523944824432932332, 0.3914743753855044472 ) ) ;
#22660=CARTESIAN_POINT ( 'NONE',  ( 0.000000000000000000, 0.2764156081756484196, 0.3522222222222262111 ) ) ;
#22668=CARTESIAN_POINT ( 'NONE',  ( 0.2764156081756484196, -5.077672346800151106E-17, 0.1230555555555576941 ) ) ;
#22674=CARTESIAN_POINT ( 'NONE',  ( -0.03750733961385160214, 0.5077191469176455252, 0.4064695056028757580 ) ) ;
#22680=CIRCLE ( 'NONE', #487, 0.01875000000000000625 ) ;
#22685=CARTESIAN_POINT ( 'NONE',  ( 0.2764156081756483641, 0.1144950937579610056, -0.1026388888888885437 ) ) ;
#22690=CARTESIAN_POINT ( 'NONE',  ( 0.000000000000000000, 0.2764156081756484196, 0.08138888888889070361 ) ) ;
#22696=CARTESIAN_POINT ( 'NONE',  ( 0.1306872919485616846, 0.3155070326520292290, 0.1004861111111128580 ) ) ;
#22699=CARTESIAN_POINT ( 'NONE',  ( -0.2533266501256048464, -0.1176800686429169962, -0.06681963058184084425 ) ) ;
#22707=ORIENTED_EDGE ( 'NONE', *, *, #20816, .F. ) ;
#22711=CARTESIAN_POINT ( 'NONE',  ( 0.2552321839962294336, -0.1601952157746480421, -0.09003777342340114898 ) ) ;
#22721=EDGE_LOOP ( 'NONE', ( #5427, #2475, #16086, #10400 ) ) ;
#22724=CARTESIAN_POINT ( 'NONE',  ( 0.000000000000000000, 3.738758431839877614E-19, 0.004799741732707325965 ) ) ;
#22728=( BOUNDED_CURVE ( )  B_SPLINE_CURVE ( 2, ( #23110, #14224, #15810, #8360, #6419, #21536, #1178, #6783, #8125 ),
 .UNSPECIFIED., .F., .T. ) 
 B_SPLINE_CURVE_WITH_KNOTS ( ( 3, 2, 2, 2, 3 ),
 ( 0.3958333333333334259, 0.4062500000000001110, 0.4166666666666667407, 0.4270833333333333703, 0.4375000000000000555 ),
 .UNSPECIFIED. ) 
 CURVE ( )  GEOMETRIC_REPRESENTATION_ITEM ( )  RATIONAL_B_SPLINE_CURVE ( ( 0.9999999999999992228, 0.9238795325112875156, 1.000000000000000000, 0.9238795325112867385, 1.000000000000000000, 0.9238795325112867385, 1.000000000000000000, 0.9238795325112862944, 1.000000000000000444 ) ) 
 REPRESENTATION_ITEM ( '' )  );
#22736=DIRECTION ( 'NONE',  ( -0.8459207832372979130, 0.4883925919151543282, -0.2142211582677917836 ) ) ;
#22755=CARTESIAN_POINT ( 'NONE',  ( 0.2764156081756483641, -0.1144950937579611028, 0.1681944444444470055 ) ) ;
#22757=CARTESIAN_POINT ( 'NONE',  ( 0.1954553509668046640, -0.1954553509668047195, 0.3938888888888931739 ) ) ;
#22760=FACE_OUTER_BOUND ( 'NONE', #23353, .T. ) ;
#22762=CARTESIAN_POINT ( 'NONE',  ( -0.1209188320989881132, 0.2598538660581654614, -0.07562110105720883102 ) ) ;
#22765=CARTESIAN_POINT ( 'NONE',  ( 0.2782766723721453728, -0.03026958819840001175, 0.3911785983335306360 ) ) ;
#22771=ORIENTED_EDGE ( 'NONE', *, *, #7092, .T. ) ;
#22774=CARTESIAN_POINT ( 'NONE',  ( -0.3155070326520292845, 1.931923388228935888E-17, -0.1564583333333331994 ) ) ;
#22782=CARTESIAN_POINT ( 'NONE',  ( -3.385114897866767815E-17, -0.2764156081756484196, -0.1130555555555552844 ) ) ;
#22785=CARTESIAN_POINT ( 'NONE',  ( 0.1954553509668047195, 0.1954553509668046085, 0.2411111111111141903 ) ) ;
#22799=AXIS2_PLACEMENT_3D ( 'NONE', #53, #16415, #7145 ) ;
#22805=CARTESIAN_POINT ( 'NONE',  ( 0.1144950937579611444, 0.2764156081756483641, -0.09569444444444404063 ) ) ;
#22810=CARTESIAN_POINT ( 'NONE',  ( 0.1954553509668046640, -0.1954553509668047195, 0.06055555555555720143 ) ) ;
#22815=CARTESIAN_POINT ( 'NONE',  ( 0.2209708691207961095, -0.2209708691207961651, 0.1925000000000024747 ) ) ;
#22817=CARTESIAN_POINT ( 'NONE',  ( -0.1306872919485614903, 0.3155070326520293400, 0.1629861111111133576 ) ) ;
#22818=CARTESIAN_POINT ( 'NONE',  ( 0.3124999999999991673, 0.1294417382415931073, 0.03625000000000128814 ) ) ;
#22835=CARTESIAN_POINT ( 'NONE',  ( -0.06232504193995545838, -0.3017193634690832349, -0.09679842907668260998 ) ) ;
#22844=CARTESIAN_POINT ( 'NONE',  ( 0.2139474665362423589, 0.4177432499681213995, 0.4289390872834607515 ) ) ;
#22852=DIRECTION ( 'NONE',  ( -0.000000000000000000, -0.000000000000000000, -1.000000000000000000 ) ) ;
#22854=CARTESIAN_POINT ( 'NONE',  ( -0.3100543665040827457, -0.3622559054007235546, 0.4143868288130764799 ) ) ;
#22868=CARTESIAN_POINT ( 'NONE',  ( 0.000000000000000000, 0.3125000000000000000, 0.2688888888888920636 ) ) ;
#22871=CARTESIAN_POINT ( 'NONE',  ( 0.1954553509668047195, 0.1954553509668046085, 0.1786111111111137462 ) ) ;
#22873=CARTESIAN_POINT ( 'NONE',  ( -0.1144950937579609918, -0.2764156081756484196, -0.1234722222222220528 ) ) ;
#22874=ORIENTED_EDGE ( 'NONE', *, *, #1536, .T. ) ;
#22876=CARTESIAN_POINT ( 'NONE',  ( 0.006494592121999842073, -0.5491884613158954931, 0.04193801346286461784 ) ) ;
#22878=ADVANCED_FACE ( 'NONE', ( #19817 ), #15798, .T. ) ;
#22893=LINE ( 'NONE', #8366, #14269 ) ;
#22894=CARTESIAN_POINT ( 'NONE',  ( -0.2230971623002953874, 0.2230971623002954152, -0.1078472222222217058 ) ) ;
#22896=CARTESIAN_POINT ( 'NONE',  ( 0.3125000000000000000, -5.740531871003217465E-17, 0.1438888888888910089 ) ) ;
#22902=CARTESIAN_POINT ( 'NONE',  ( -0.3065849364905382513, 4.708020935245015622E-15, -0.09575160315720471216 ) ) ;
#22903=CARTESIAN_POINT ( 'NONE',  ( -0.1954553509668046918, -0.1954553509668046640, 0.1022222222222241989 ) ) ;
#22915=EDGE_LOOP ( 'NONE', ( #5584, #17113 ) ) ;
#22917=CARTESIAN_POINT ( 'NONE',  ( -0.4805456235326251990, -0.2624941757204518611, 0.04270874187135761946 ) ) ;
#22923=CARTESIAN_POINT ( 'NONE',  ( -0.4687500000000003886, 0.2150880996501464693, 0.05816232583285784602 ) ) ;
#22927=CARTESIAN_POINT ( 'NONE',  ( -0.2764156081756484196, -0.1144950937579609362, -0.01236111111111004406 ) ) ;
#22933=CARTESIAN_POINT ( 'NONE',  ( -0.3155070326520292845, 1.931923388228935888E-17, 0.06229166666666812596 ) ) ;
#22941=CARTESIAN_POINT ( 'NONE',  ( -0.3125000000000004996, -0.1294417382415916640, 0.2931944444444481435 ) ) ;
#22954=ADVANCED_FACE ( 'NONE', ( #2861 ), #2011, .T. ) ;
#22955=CARTESIAN_POINT ( 'NONE',  ( 0.2720287551442869267, 0.3842100023554017030, 0.4182004018663288414 ) ) ;
#22963=CARTESIAN_POINT ( 'NONE',  ( -0.2020650928029223692, -0.4371048157571741921, 0.07438423612653363715 ) ) ;
#22979=CARTESIAN_POINT ( 'NONE',  ( 0.4587684526354154357, 0.1777979193111714762, 0.4165948764943589455 ) ) ;
#22984=CARTESIAN_POINT ( 'NONE',  ( 0.009375000000000025674, -0.5358532185916218271, 0.06112444011295370405 ) ) ;
#22985=CARTESIAN_POINT ( 'NONE',  ( -3.385114897866767815E-17, -0.2764156081756484196, 0.2688888888888921747 ) ) ;
#22987=CARTESIAN_POINT ( 'NONE',  ( -0.1954553509668046640, 0.1954553509668046918, 0.4216666666666711305 ) ) ;
#22994=CARTESIAN_POINT ( 'NONE',  ( 0.2209708691207961095, -0.2209708691207961651, 0.3591666666666705199 ) ) ;
#23002=CARTESIAN_POINT ( 'NONE',  ( 0.000000000000000000, 0.3125000000000000000, 0.2133333333333360116 ) ) ;
#23004=( BOUNDED_CURVE ( )  B_SPLINE_CURVE ( 2, ( #503, #22818, #21235, #11989, #21355, #10151, #8415, #4643, #14041 ),
 .UNSPECIFIED., .F., .T. ) 
 B_SPLINE_CURVE_WITH_KNOTS ( ( 3, 2, 2, 2, 3 ),
 ( 0.2291666666666667407, 0.2395833333333334259, 0.2500000000000001110, 0.2604166666666667962, 0.2708333333333334259 ),
 .UNSPECIFIED. ) 
 CURVE ( )  GEOMETRIC_REPRESENTATION_ITEM ( )  RATIONAL_B_SPLINE_CURVE ( ( 0.9999999999999994449, 0.9238795325112872936, 1.000000000000000000, 0.9238795325112867385, 1.000000000000000000, 0.9238795325112867385, 1.000000000000000000, 0.9238795325112859613, 1.000000000000000888 ) ) 
 REPRESENTATION_ITEM ( '' )  );
#23005=( BOUNDED_SURFACE ( )  B_SPLINE_SURFACE ( 3, 2, ( 
 ( #15839, #3036, #17671 ),
 ( #12084, #8639, #19255 ),
 ( #19735, #16084, #12321 ),
 ( #23497, #15606, #19494 ),
 ( #23379, #724, #6567 ),
 ( #2676, #2789, #14017 ),
 ( #956, #1083, #21448 ),
 ( #6688, #2560, #14133 ),
 ( #21563, #4377, #10008 ),
 ( #17431, #17551, #23027 ),
 ( #6328, #21208, #4500 ),
 ( #845, #1569, #20103 ) ),
 .UNSPECIFIED., .F., .F., .F. ) 
 B_SPLINE_SURFACE_WITH_KNOTS ( ( 4, 2, 2, 2, 2, 4 ),
 ( 3, 3 ),
 ( 0.001926919177646338422, 0.005264799389783186324, 0.006933739495851611034, 0.008602679601920034877, 0.01194055981405688430, 0.01527844002619373198 ),
 ( 0.000000000000000000, 1.000000000000000000 ),
 .UNSPECIFIED. ) 
 GEOMETRIC_REPRESENTATION_ITEM ( )  RATIONAL_B_SPLINE_SURFACE ( (
 ( 1.000000000000000000, 0.8464669816041905381, 1.000000000000000000),
 ( 1.000000000000000000, 0.8516517675253432174, 1.000000000000000000),
 ( 1.000000000000000000, 0.8565844288627803005, 1.000000000000000000),
 ( 1.000000000000000000, 0.8620057511681040729, 1.000000000000000000),
 ( 1.000000000000000000, 0.8634777350187821110, 1.000000000000000000),
 ( 1.000000000000000000, 0.8654907715252899703, 1.000000000000000000),
 ( 1.000000000000000000, 0.8660271740515483874, 1.000000000000000000),
 ( 1.000000000000000000, 0.8660218497380072211, 1.000000000000000000),
 ( 1.000000000000000000, 0.8638283365559921156, 1.000000000000000000),
 ( 1.000000000000000000, 0.8566178551150570586, 1.000000000000000000),
 ( 1.000000000000000000, 0.8516788886409425441, 1.000000000000000000),
 ( 1.000000000000000000, 0.8464669816041904271, 1.000000000000000000) ) ) 
 REPRESENTATION_ITEM ( '' )  SURFACE ( )  );
#23008=EDGE_CURVE ( 'NONE', #314, #8442, #149, .T. ) ;
#23009=CARTESIAN_POINT ( 'NONE',  ( 0.1306872919485616846, 0.3155070326520292290, 0.1039583333333355397 ) ) ;
#23014=CARTESIAN_POINT ( 'NONE',  ( -0.03651601414465285855, -0.2739930093161157543, -0.06558227484231510251 ) ) ;
#23016=CARTESIAN_POINT ( 'NONE',  ( -0.03651601414465285855, -0.2739930093161157543, -0.06558227484231510251 ) ) ;
#23017=CARTESIAN_POINT ( 'NONE',  ( -0.1144950937579609918, -0.2764156081756484196, 0.2723611111111143845 ) ) ;
#23026=DIRECTION ( 'NONE',  ( 1.000000000000000000, 0.000000000000000000, -0.000000000000000000 ) ) ;
#23027=CARTESIAN_POINT ( 'NONE',  ( -0.08316635082768847331, 0.4932497623273897069, 0.4003041662012485902 ) ) ;
#23028=CARTESIAN_POINT ( 'NONE',  ( 0.4500000000000003442, -0.2598076211353317344, 0.4425000000000000044 ) ) ;
#23035=CARTESIAN_POINT ( 'NONE',  ( 0.1527521626045861280, 0.4420638983541222977, 0.4298724737630856829 ) ) ;
#23040=CARTESIAN_POINT ( 'NONE',  ( 0.1954553509668047195, 0.1954553509668046085, 0.2966666666666701313 ) ) ;
#23041=CARTESIAN_POINT ( 'NONE',  ( 0.2209708691207961095, -0.2209708691207961651, 0.3661111111111154393 ) ) ;
#23045=CARTESIAN_POINT ( 'NONE',  ( 0.3124999999999996669, 0.1294417382415925521, -0.01930555555555471536 ) ) ;
#23046=CARTESIAN_POINT ( 'NONE',  ( -0.3155070326520293400, 0.1306872919485614903, 0.05881944444444586056 ) ) ;
#23053=AXIS2_PLACEMENT_3D ( 'NONE', #3692, #18445, #19921 ) ;
#23071=CARTESIAN_POINT ( 'NONE',  ( 0.1568404389086313078, 0.4507140077415570656, 0.4133480672483983431 ) ) ;
#23092=CARTESIAN_POINT ( 'NONE',  ( 0.2209708691207961651, 0.2209708691207959985, 0.04666666666666840352 ) ) ;
#23097=CARTESIAN_POINT ( 'NONE',  ( -0.4587622378227205200, -0.1787210847074471587, 0.4163997147010622402 ) ) ;
#23100=CARTESIAN_POINT ( 'NONE',  ( -0.2764156081756484196, -0.1144950937579609362, 0.3695833333333374826 ) ) ;
#23102=CARTESIAN_POINT ( 'NONE',  ( -3.385114897866767815E-17, -0.2764156081756484196, -0.008888888888887782128 ) ) ;
#23105=CARTESIAN_POINT ( 'NONE',  ( 0.4593750000000000888, -0.04461821091738114864, 0.4343810118395100006 ) ) ;
#23108=CARTESIAN_POINT ( 'NONE',  ( 8.904784892192170075E-17, -0.5196152422706635798, 0.3779506566538943235 ) ) ;
#23110=CARTESIAN_POINT ( 'NONE',  ( 0.3125000000000000000, -5.740531871003217465E-17, 0.1438888888888910089 ) ) ;
#23120=CARTESIAN_POINT ( 'NONE',  ( 0.2230971623002953874, -0.2230971623002954429, 0.1421527777777802648 ) ) ;
#23121=CARTESIAN_POINT ( 'NONE',  ( -0.04643773642726176792, -0.5144550377384379258, 0.07051021533369886130 ) ) ;
#23124=CARTESIAN_POINT ( 'NONE',  ( -0.1954553509668046918, -0.1954553509668046640, -0.06444444444444380471 ) ) ;
#23131=CARTESIAN_POINT ( 'NONE',  ( 0.3125000000000000000, -5.740531871003217465E-17, 0.3175000000000038347 ) ) ;
#23135=( BOUNDED_SURFACE ( )  B_SPLINE_SURFACE ( 3, 2, ( 
 ( #14036, #3166, #16225 ),
 ( #14395, #8899, #7077 ),
 ( #21819, #5109, #12575 ),
 ( #21466, #19996, #1101 ),
 ( #3284, #10738, #12221 ),
 ( #12104, #2807, #10262 ),
 ( #10388, #19631, #17810 ),
 ( #8534, #14765, #24120 ),
 ( #16582, #9137, #108 ),
 ( #9021, #3530, #7671 ) ),
 .UNSPECIFIED., .F., .F., .T. ) 
 B_SPLINE_SURFACE_WITH_KNOTS ( ( 4, 2, 2, 2, 4 ),
 ( 3, 3 ),
 ( 0.04450355443756499191, 0.04782809616271448128, 0.05115263788786396371, 0.05447717961301344614, 0.05780172133816293550 ),
 ( 0.000000000000000000, 1.000000000000000000 ),
 .UNSPECIFIED. ) 
 GEOMETRIC_REPRESENTATION_ITEM ( )  RATIONAL_B_SPLINE_SURFACE ( (
 ( 1.000000000000000000, 0.8285407536241355952, 1.000000000000000000),
 ( 1.000000000000000000, 0.8326162293447895157, 1.000000000000000000),
 ( 1.000000000000000000, 0.8363774056812446345, 1.000000000000000000),
 ( 1.000000000000000000, 0.8417899530394342689, 1.000000000000000000),
 ( 1.000000000000000000, 0.8433914761756452494, 1.000000000000000000),
 ( 1.000000000000000000, 0.8433914154492313520, 1.000000000000000000),
 ( 1.000000000000000000, 0.8417897495747284076, 1.000000000000000000),
 ( 1.000000000000000000, 0.8363771423991239740, 1.000000000000000000),
 ( 1.000000000000000000, 0.8326160433687649354, 1.000000000000000000),
 ( 1.000000000000000000, 0.8285407536241354842, 1.000000000000000000) ) ) 
 REPRESENTATION_ITEM ( '' )  SURFACE ( )  );
#23139=( BOUNDED_CURVE ( )  B_SPLINE_CURVE ( 2, ( #14883, #3777, #11220, #1941, #14004, #4722, #2894, #4252, #1070 ),
 .UNSPECIFIED., .F., .F. ) 
 B_SPLINE_CURVE_WITH_KNOTS ( ( 3, 2, 2, 2, 3 ),
 ( 0.2708333333333334259, 0.2812500000000001110, 0.2916666666666667407, 0.3020833333333333703, 0.3125000000000000555 ),
 .UNSPECIFIED. ) 
 CURVE ( )  GEOMETRIC_REPRESENTATION_ITEM ( )  RATIONAL_B_SPLINE_CURVE ( ( 0.9999999999999992228, 0.9238795325112875156, 1.000000000000000000, 0.9238795325112867385, 1.000000000000000000, 0.9238795325112867385, 1.000000000000000000, 0.9238795325112862944, 1.000000000000000444 ) ) 
 REPRESENTATION_ITEM ( '' )  );
#23140=VERTEX_POINT ( 'NONE', #11040 ) ;
#23147=EDGE_CURVE ( 'NONE', #14969, #11153, #18136, .T. ) ;
#23148=CARTESIAN_POINT ( 'NONE',  ( 0.1334180974147631538, 0.4531173396632154349, 0.4271664148355319157 ) ) ;
#23149=CARTESIAN_POINT ( 'NONE',  ( -0.1954553509668046640, 0.1954553509668046918, 0.08138888888889070361 ) ) ;
#23153=CARTESIAN_POINT ( 'NONE',  ( -0.2764156081756484196, 0.1144950937579609918, 0.3140277777777814028 ) ) ;
#23155=CARTESIAN_POINT ( 'NONE',  ( 0.1294417382415921358, -0.3125000000000002220, 0.3626388888888931183 ) ) ;
#23160=CARTESIAN_POINT ( 'NONE',  ( 0.1306872919485614071, -0.3155070326520293955, 0.4685416666666713525 ) ) ;
#23163=CARTESIAN_POINT ( 'NONE',  ( -0.3125000000000000000, 0.1294417382415922468, 0.3904166666666707419 ) ) ;
#23171=CARTESIAN_POINT ( 'NONE',  ( -0.09145417301143905775, 0.5014751291207464323, 0.06110928887248364555 ) ) ;
#23173=EDGE_CURVE ( 'NONE', #23807, #19658, #6060, .T. ) ;
#23179=CARTESIAN_POINT ( 'NONE',  ( 0.07226797383931020391, -0.2674160455369279932, 0.3880822748423151669 ) ) ;
#23181=DIRECTION ( 'NONE',  ( 0.000000000000000000, 0.000000000000000000, 1.000000000000000000 ) ) ;
#23192=CARTESIAN_POINT ( 'NONE',  ( 0.000000000000000000, 0.000000000000000000, 1.326383476483184332 ) ) ;
#23202=AXIS2_PLACEMENT_3D ( 'NONE', #11803, #19225, #11933 ) ;
#23212=ORIENTED_EDGE ( 'NONE', *, *, #18604, .T. ) ;
#23213=CARTESIAN_POINT ( 'NONE',  ( -0.3125000000000000000, 1.913510623667739771E-17, 0.06750000000000189182 ) ) ;
#23216=VECTOR ( 'NONE', #4751, 39.37007874015748143 ) ;
#23218=CARTESIAN_POINT ( 'NONE',  ( -0.4687500000000003886, 0.1747335358173341124, 0.4002814116603867212 ) ) ;
#23219=CARTESIAN_POINT ( 'NONE',  ( -3.385114897866767815E-17, -0.2764156081756484196, 0.3800000000000042233 ) ) ;
#23221=CARTESIAN_POINT ( 'NONE',  ( 0.2764156081756483641, 0.1144950937579610056, -0.04708333333333254017 ) ) ;
#23233=FACE_OUTER_BOUND ( 'NONE', #9412, .T. ) ;
#23238=CARTESIAN_POINT ( 'NONE',  ( -0.3155070326520292845, 1.931923388228935888E-17, -0.04534722222222122012 ) ) ;
#23239=CARTESIAN_POINT ( 'NONE',  ( -0.3850752722190822763, -0.3189425652913190912, 0.07813238993955241851 ) ) ;
#23243=CARTESIAN_POINT ( 'NONE',  ( 0.2764156081756484196, -5.077672346800151106E-17, 0.01194444444444569750 ) ) ;
#23245=CARTESIAN_POINT ( 'NONE',  ( -0.1219426170922269514, -0.2560469716179860633, -0.07222464464025338260 ) ) ;
#23246=CARTESIAN_POINT ( 'NONE',  ( 0.000000000000000000, 0.2764156081756484196, 0.4147222222222267107 ) ) ;
#23248=CARTESIAN_POINT ( 'NONE',  ( 0.6211549996190571798, 7.721695522547942866E-17, -0.1199999999999999956 ) ) ;
#23262=DIRECTION ( 'NONE',  ( -0.000000000000000000, 0.9767851838303062140, -0.2142211582677939208 ) ) ;
#23267=CARTESIAN_POINT ( 'NONE',  ( -0.4687500000000003886, 0.1743516731584483781, 0.07807856808314557473 ) ) ;
#23268=CARTESIAN_POINT ( 'NONE',  ( 0.000000000000000000, 0.2764156081756484196, -0.03666666666666578561 ) ) ;
#23272=CARTESIAN_POINT ( 'NONE',  ( -0.2764156081756484196, 0.1144950937579609918, 0.2584722222222254340 ) ) ;
#23275=CARTESIAN_POINT ( 'NONE',  ( -0.04643634559190771421, 0.5144558407376040865, 0.07050986311825922781 ) ) ;
#23277=CARTESIAN_POINT ( 'NONE',  ( -0.3155070326520293400, -0.1306872919485614626, 0.3435416666666703533 ) ) ;
#23281=CARTESIAN_POINT ( 'NONE',  ( 0.2209708691207961095, -0.2209708691207961651, 0.02583333333333451623 ) ) ;
#23286=EDGE_CURVE ( 'NONE', #8318, #11169, #16189, .T. ) ;
#23294=DIRECTION ( 'NONE',  ( 1.000000000000000000, 0.000000000000000000, 0.000000000000000000 ) ) ;
#23296=AXIS2_PLACEMENT_3D ( 'NONE', #22244, #11041, #7262 ) ;
#23301=EDGE_CURVE ( 'NONE', #15146, #15771, #1221, .T. ) ;
#23315=CARTESIAN_POINT ( 'NONE',  ( 0.000000000000000000, 0.000000000000000000, 1.326383476483184332 ) ) ;
#23326=VERTEX_POINT ( 'NONE', #6771 ) ;
#23328=CARTESIAN_POINT ( 'NONE',  ( 0.3124999999999999445, 0.1294417382415923023, 0.04319444444444614506 ) ) ;
#23331=CIRCLE ( 'NONE', #16341, 0.3125000000000000000 ) ;
#23336=DIRECTION ( 'NONE',  ( -1.000000000000000000, 0.000000000000000000, 0.000000000000000000 ) ) ;
#23338=CARTESIAN_POINT ( 'NONE',  ( 0.2764156081756484196, -5.077672346800151106E-17, 0.1161111111111132049 ) ) ;
#23341=ADVANCED_FACE ( 'NONE', ( #1290 ), #9579, .F. ) ;
#23345=DIRECTION ( 'NONE',  ( 0.000000000000000000, 0.000000000000000000, -1.000000000000000000 ) ) ;
#23351=TOROIDAL_SURFACE ( 'NONE', #2358, 0.6211549996190571798, 0.01874999999999999931 ) ;
#23353=EDGE_LOOP ( 'NONE', ( #11517, #5495, #11609, #11956 ) ) ;
#23358=CARTESIAN_POINT ( 'NONE',  ( 0.3155070326520292290, -0.1306872919485616569, 0.09006944444444651976 ) ) ;
#23366=CARTESIAN_POINT ( 'NONE',  ( -0.2764156081756484196, 1.692557448933383907E-17, 0.09527777777777970969 ) ) ;
#23374=CARTESIAN_POINT ( 'NONE',  ( -0.4587689423274134426, -0.1777187644174526848, 0.4166100394118468220 ) ) ;
#23379=CARTESIAN_POINT ( 'NONE',  ( -0.3075813148943709052, 0.3526675668868786695, 0.4297318021117937925 ) ) ;
#23380=CARTESIAN_POINT ( 'NONE',  ( 0.4687500000000002776, 0.2598076211353318454, 0.4425000000000000044 ) ) ;
#23381=ORIENTED_EDGE ( 'NONE', *, *, #6647, .F. ) ;
#23388=CARTESIAN_POINT ( 'NONE',  ( -0.4800179949082463149, -0.1716548275489190312, 0.06108632444355151930 ) ) ;
#23389=CARTESIAN_POINT ( 'NONE',  ( 0.2764156081756483641, 0.1144950937579610056, 0.06402777777777945989 ) ) ;
#23395=CARTESIAN_POINT ( 'NONE',  ( -0.1144950937579609918, -0.2764156081756484196, 0.1056944444444464365 ) ) ;
#23398=CARTESIAN_POINT ( 'NONE',  ( -0.1595362993632639947, 0.2449369388610319331, 0.4038266169345403611 ) ) ;
#23402=CARTESIAN_POINT ( 'NONE',  ( -0.2230971623002953874, 0.2230971623002954152, 0.2775694444444475883 ) ) ;
#23410=VERTEX_POINT ( 'NONE', #21289 ) ;
#23419=ORIENTED_EDGE ( 'NONE', *, *, #21045, .T. ) ;
#23426=VERTEX_POINT ( 'NONE', #19455 ) ;
#23428=ORIENTED_EDGE ( 'NONE', *, *, #8157, .T. ) ;
#23452=CARTESIAN_POINT ( 'NONE',  ( 0.000000000000000000, 0.3125000000000000000, 0.05361111111111287880 ) ) ;
#23457=CARTESIAN_POINT ( 'NONE',  ( -0.4687500000000003886, -0.2178027435389952027, 0.3900764204055337525 ) ) ;
#23462=CARTESIAN_POINT ( 'NONE',  ( -0.1144950937579609918, -0.2764156081756484196, -0.01236111111111004406 ) ) ;
#23468=CARTESIAN_POINT ( 'NONE',  ( -0.3125000000000000000, 1.913510623667739771E-17, -0.05055555555555497210 ) ) ;
#23475=CARTESIAN_POINT ( 'NONE',  ( 0.1294417382415924134, 0.3124999999999999445, 0.2168055555555586100 ) ) ;
#23477=CARTESIAN_POINT ( 'NONE',  ( -0.3155070326520293400, 0.1306872919485614903, 0.1178472222222245319 ) ) ;
#23479=CARTESIAN_POINT ( 'NONE',  ( 0.03651601414450977162, -0.2739930093161348501, 0.3880822748423153890 ) ) ;
#23480=ORIENTED_EDGE ( 'NONE', *, *, #8425, .T. ) ;
#23483=CARTESIAN_POINT ( 'NONE',  ( -0.1144950937579609779, 0.2764156081756484196, -0.02624999999999906228 ) ) ;
#23484=CARTESIAN_POINT ( 'NONE',  ( 0.4772460259542070649, -0.2717629240624622744, 0.04193793378272828165 ) ) ;
#23497=CARTESIAN_POINT ( 'NONE',  ( -0.3267728913538784918, 0.3414772273308728789, 0.4269974078869069323 ) ) ;
#23499=CARTESIAN_POINT ( 'NONE',  ( -0.1294417382415922191, 0.3125000000000000000, 0.1126388888888911199 ) ) ;
#23501=CARTESIAN_POINT ( 'NONE',  ( 0.1986479633932748956, -0.2391244849433121489, 0.4220858545751106639 ) ) ;
#23503=CARTESIAN_POINT ( 'NONE',  ( 0.4679361169221505912, -0.2662350510444111418, 0.05893285591566548021 ) ) ;
#23504=EDGE_CURVE ( 'NONE', #23426, #18391, #10346, .T. ) ;
#23506=CARTESIAN_POINT ( 'NONE',  ( -0.4620753182980354978, -0.2744865679600219099, 0.05975678175779885332 ) ) ;
#23507=CARTESIAN_POINT ( 'NONE',  ( -3.385114897866767815E-17, -0.2764156081756484196, 0.1022222222222241989 ) ) ;
#23511=CARTESIAN_POINT ( 'NONE',  ( 0.1144950937579611444, 0.2764156081756483641, 0.1334722222222244348 ) ) ;
#23514=CARTESIAN_POINT ( 'NONE',  ( -0.1514593411830790493, 0.2498004213170096632, 0.4036436051450662532 ) ) ;
#23517=CARTESIAN_POINT ( 'NONE',  ( -0.2764156081756484196, 0.1144950937579609918, -0.02624999999999903799 ) ) ;
#23518=CARTESIAN_POINT ( 'NONE',  ( 0.2230971623002954429, 0.2230971623002953319, 0.3192361111111146066 ) ) ;
#23520=CARTESIAN_POINT ( 'NONE',  ( 0.4620259694561523744, 0.2880908832651560281, 0.04413116910601654758 ) ) ;
#23544=ORIENTED_EDGE ( 'NONE', *, *, #18869, .F. ) ;
#23554=DIRECTION ( 'NONE',  ( -0.8320502943378444982, -0.4803844614152614767, -0.2773500981126123532 ) ) ;
#23575=ORIENTED_EDGE ( 'NONE', *, *, #21241, .T. ) ;
#23578=CARTESIAN_POINT ( 'NONE',  ( -0.2742360776603882666, -0.1498359893665253684, -0.1016666666666679597 ) ) ;
#23583=CARTESIAN_POINT ( 'NONE',  ( -0.1954553509668046640, 0.1954553509668046918, 0.08138888888889070361 ) ) ;
#23586=CARTESIAN_POINT ( 'NONE',  ( -0.03071979988719963223, 0.2873147545066508379, -0.07749523702218821808 ) ) ;
#23592=ADVANCED_FACE ( 'NONE', ( #14465 ), #1889, .F. ) ;
#23596=ORIENTED_EDGE ( 'NONE', *, *, #19160, .F. ) ;
#23598=VECTOR ( 'NONE', #14182, 39.37007874015748854 ) ;
#23599=CARTESIAN_POINT ( 'NONE',  ( 0.3155070326520292290, 0.1306872919485615736, 0.3192361111111149397 ) ) ;
#23606=EDGE_CURVE ( 'NONE', #8682, #5628, #9172, .T. ) ;
#23608=CARTESIAN_POINT ( 'NONE',  ( -0.1144950937579609779, 0.2764156081756484196, 0.08486111111111295513 ) ) ;
#23610=CARTESIAN_POINT ( 'NONE',  ( -0.1954553509668046640, 0.1954553509668046918, 0.3661111111111151617 ) ) ;
#23622=CARTESIAN_POINT ( 'NONE',  ( -0.008437752171424794251, 0.5369270166837832869, 0.04763592618482979241 ) ) ;
#23627=CARTESIAN_POINT ( 'NONE',  ( -0.2195630361087207438, -0.1679215936615484350, -0.06558227484231504700 ) ) ;
#23628=CARTESIAN_POINT ( 'NONE',  ( 0.1144950937579611444, 0.2764156081756483641, -0.04013888888888803713 ) ) ;
#23637=CARTESIAN_POINT ( 'NONE',  ( -0.2951834061891110417, 0.03795937687255804965, 0.4086815878027646454 ) ) ;
#23640=CARTESIAN_POINT ( 'NONE',  ( -0.2230971623002954152, -0.2230971623002953874, 0.4581250000000046119 ) ) ;
#23642=CARTESIAN_POINT ( 'NONE',  ( 0.2769159822048600783, 0.3938884537237697936, 0.07441357458167797978 ) ) ;
#23662=EDGE_LOOP ( 'NONE', ( #9320, #22874, #5159, #7042 ) ) ;
#23668=CARTESIAN_POINT ( 'NONE',  ( 0.3125000000000000000, -5.740531871003217465E-17, 0.2619444444444478659 ) ) ;
#23677=FACE_OUTER_BOUND ( 'NONE', #1399, .T. ) ;
#23686=ORIENTED_EDGE ( 'NONE', *, *, #20666, .F. ) ;
#23689=CARTESIAN_POINT ( 'NONE',  ( 0.07527472113052306735, -0.4862786960646409140, 0.4165495381634258809 ) ) ;
#23690=CARTESIAN_POINT ( 'NONE',  ( -0.3125000000000000555, 1.913510623667739771E-17, 0.2341666666666698537 ) ) ;
#23699=ORIENTED_EDGE ( 'NONE', *, *, #226, .T. ) ;
#23700=ORIENTED_EDGE ( 'NONE', *, *, #4798, .F. ) ;
#23703=CARTESIAN_POINT ( 'NONE',  ( 0.1954553509668046640, -0.1954553509668047195, 0.2202777777777807366 ) ) ;
#23713=AXIS2_PLACEMENT_3D ( 'NONE', #16632, #3332, #23802 ) ;
#23715=CARTESIAN_POINT ( 'NONE',  ( 0.3155070326520292845, -5.795770164686806123E-17, 0.3713194444444487541 ) ) ;
#23718=CARTESIAN_POINT ( 'NONE',  ( 0.2534589807566784980, -0.3949312665968779945, 0.4181462219997758578 ) ) ;
#23719=ADVANCED_FACE ( 'NONE', ( #2259 ), #176, .T. ) ;
#23723=CARTESIAN_POINT ( 'NONE',  ( -0.1954553509668046640, 0.1954553509668046918, 0.1438888888888912032 ) ) ;
#23729=CARTESIAN_POINT ( 'NONE',  ( -0.3125000000000000000, 3.738758431839877614E-19, -0.1016666666666665164 ) ) ;
#23732=TOROIDAL_SURFACE ( 'NONE', #7790, 0.3385998376278290256, 0.01874999999999999931 ) ;
#23736=CARTESIAN_POINT ( 'NONE',  ( -0.003294150194310526466, 0.5383638965977114443, 0.05893128447555143895 ) ) ;
#23744=CARTESIAN_POINT ( 'NONE',  ( -0.4687500000000003886, -0.2598076211353319009, 0.06112444011295369711 ) ) ;
#23746=CARTESIAN_POINT ( 'NONE',  ( -0.1144950937579609779, 0.2764156081756484196, 0.1890277777777805146 ) ) ;
#23748=CARTESIAN_POINT ( 'NONE',  ( -0.01875000000000017278, 0.5520911949125799634, 0.06112444011295375956 ) ) ;
#23751=CARTESIAN_POINT ( 'NONE',  ( -0.4593750000000004219, 0.2760455974562897596, 0.06112444011295372487 ) ) ;
#23758=CARTESIAN_POINT ( 'NONE',  ( -0.03651601414465285855, -0.2739930093161157543, -0.06558227484231510251 ) ) ;
#23759=CARTESIAN_POINT ( 'NONE',  ( 0.1954553509668046640, -0.1954553509668047195, 0.06055555555555720143 ) ) ;
#23760=ORIENTED_EDGE ( 'NONE', *, *, #14186, .F. ) ;
#23780=EDGE_CURVE ( 'NONE', #314, #15906, #4522, .T. ) ;
#23791=CARTESIAN_POINT ( 'NONE',  ( 0.3155070326520292290, -0.1306872919485616569, -0.08006944444444412390 ) ) ;
#23802=DIRECTION ( 'NONE',  ( -1.000000000000000000, 0.000000000000000000, 0.000000000000000000 ) ) ;
#23807=VERTEX_POINT ( 'NONE', #2382 ) ;
#23810=CARTESIAN_POINT ( 'NONE',  ( 0.4607728391470888862, -0.2757711312522246327, 0.04763613967037444441 ) ) ;
#23821=ORIENTED_EDGE ( 'NONE', *, *, #8425, .F. ) ;
#23825=CARTESIAN_POINT ( 'NONE',  ( 0.1954553509668047195, 0.1954553509668046085, 0.2341666666666697150 ) ) ;
#23828=CARTESIAN_POINT ( 'NONE',  ( -0.08208976641702336874, -0.4938713286266925850, 0.4000323696459241463 ) ) ;
#23837=VERTEX_POINT ( 'NONE', #20782 ) ;
#23838=CARTESIAN_POINT ( 'NONE',  ( 0.2230971623002953874, -0.2230971623002954429, 0.1977083333333363169 ) ) ;
#23845=CARTESIAN_POINT ( 'NONE',  ( 0.2764156081756484196, -5.077672346800151106E-17, 0.1786111111111136907 ) ) ;
#23854=CARTESIAN_POINT ( 'NONE',  ( -0.4723904922468886158, 0.2801879233228458665, 0.04193467568257214922 ) ) ;
#23864=CIRCLE ( 'NONE', #4433, 0.01874999999999997155 ) ;
#23865=EDGE_CURVE ( 'NONE', #23140, #4857, #10767, .T. ) ;
#23868=CARTESIAN_POINT ( 'NONE',  ( 0.000000000000000000, 0.2764156081756484196, 0.2966666666666702423 ) ) ;
#23877=CARTESIAN_POINT ( 'NONE',  ( -0.1954553509668046918, -0.1954553509668046640, 0.04666666666666818841 ) ) ;
#23882=CARTESIAN_POINT ( 'NONE',  ( -0.3125000000000000000, 0.000000000000000000, 1.326383476483184332 ) ) ;
#23887=ORIENTED_EDGE ( 'NONE', *, *, #3485, .F. ) ;
#23911=CARTESIAN_POINT ( 'NONE',  ( -0.3155070326520292845, 1.931923388228935888E-17, -0.04881944444444386716 ) ) ;
#23920=AXIS2_PLACEMENT_3D ( 'NONE', #11547, #438, #20683 ) ;
#23922=CARTESIAN_POINT ( 'NONE',  ( 0.4593750000000002554, -1.978974282089605735E-13, 0.4343810118395207698 ) ) ;
#23925=CARTESIAN_POINT ( 'NONE',  ( -0.1583113556673881317, 0.4498647735549333726, 0.08855526556985508779 ) ) ;
#23930=( BOUNDED_CURVE ( )  B_SPLINE_CURVE ( 2, ( #849, #6453, #2793, #23499, #14135, #4736, #12441, #13906, #15843 ),
 .UNSPECIFIED., .F., .F. ) 
 B_SPLINE_CURVE_WITH_KNOTS ( ( 3, 2, 2, 2, 3 ),
 ( 0.4895833333333334814, 0.5000000000000001110, 0.5104166666666668517, 0.5208333333333334814, 0.5312500000000001110 ),
 .UNSPECIFIED. ) 
 CURVE ( )  GEOMETRIC_REPRESENTATION_ITEM ( )  RATIONAL_B_SPLINE_CURVE ( ( 0.9999999999999992228, 0.9238795325112875156, 1.000000000000000000, 0.9238795325112867385, 1.000000000000000000, 0.9238795325112867385, 1.000000000000000000, 0.9238795325112859613, 1.000000000000000888 ) ) 
 REPRESENTATION_ITEM ( '' )  );
#23935=EDGE_LOOP ( 'NONE', ( #18906, #12006, #6911, #7131 ) ) ;
#23937=CARTESIAN_POINT ( 'NONE',  ( 0.01239990016126697736, -0.3069330571738623781, 0.4183927809049745594 ) ) ;
#23938=VECTOR ( 'NONE', #14356, 39.37007874015748143 ) ;
#23943=CARTESIAN_POINT ( 'NONE',  ( -0.1294417382415922746, -0.3125000000000000000, 0.1890277777777807366 ) ) ;
#23953=CARTESIAN_POINT ( 'NONE',  ( 0.1144950937579611444, 0.2764156081756483641, 0.2376388888888919526 ) ) ;
#23956=CARTESIAN_POINT ( 'NONE',  ( 0.1537937564251784239, -0.2409193255903653574, 0.3973559490783071801 ) ) ;
#23964=DIRECTION ( 'NONE',  ( -1.000000000000000000, 0.000000000000000000, 0.000000000000000000 ) ) ;
#23968=DIRECTION ( 'NONE',  ( -1.000000000000000000, 0.000000000000000000, 0.000000000000000000 ) ) ;
#23969=CARTESIAN_POINT ( 'NONE',  ( -3.863846776457871776E-17, -0.3155070326520292845, 0.3018750000000037792 ) ) ;
#23972=CARTESIAN_POINT ( 'NONE',  ( 0.1568395974156406025, -0.4507144935777573913, 0.4251457422752845661 ) ) ;
#23976=CARTESIAN_POINT ( 'NONE',  ( -0.1144950937579609918, -0.2764156081756484196, 0.2168055555555584712 ) ) ;
#23990=CARTESIAN_POINT ( 'NONE',  ( 0.01172578639833042440, 0.5344959914317364280, 0.04874733047934381308 ) ) ;
#23995=CARTESIAN_POINT ( 'NONE',  ( 0.4687500000000003886, 0.2922835737772483400, 0.06112444011295369017 ) ) ;
#23997=CARTESIAN_POINT ( 'NONE',  ( -0.1144950937579609918, -0.2764156081756484196, 0.1543055555555579716 ) ) ;
#24000=CARTESIAN_POINT ( 'NONE',  ( -0.2764156081756484196, 0.1144950937579609918, 0.3695833333333373716 ) ) ;
#24007=CARTESIAN_POINT ( 'NONE',  ( 0.2764156081756483641, -0.1144950937579611167, 0.008472222222223456389 ) ) ;
#24012=CARTESIAN_POINT ( 'NONE',  ( 0.4591128671207585499, 0.1125912384831261187, 0.4269528428895272287 ) ) ;
#24037=CARTESIAN_POINT ( 'NONE',  ( -0.1306872919485614903, 0.3155070326520293400, -0.1147916666666666252 ) ) ;
#24038=EDGE_CURVE ( 'NONE', #5917, #314, #4793, .T. ) ;
#24039=CARTESIAN_POINT ( 'NONE',  ( 0.4687500000000002776, -0.2172771893995191772, 0.3896678519206923097 ) ) ;
#24055=EDGE_CURVE ( 'NONE', #1317, #2053, #1871, .T. ) ;
#24057=ORIENTED_EDGE ( 'NONE', *, *, #13258, .T. ) ;
#24059=CARTESIAN_POINT ( 'NONE',  ( 0.04581704741080250276, -0.3043534538584632965, 0.4189930025942082414 ) ) ;
#24064=CARTESIAN_POINT ( 'NONE',  ( 0.3125000000000000555, -5.740531871003217465E-17, 0.2063888888888918416 ) ) ;
#24069=ORIENTED_EDGE ( 'NONE', *, *, #940, .T. ) ;
#24074=CARTESIAN_POINT ( 'NONE',  ( 0.1954553509668047195, 0.1954553509668046085, 0.3452777777777817358 ) ) ;
#24077=( BOUNDED_CURVE ( )  B_SPLINE_CURVE ( 2, ( #10395, #15630, #19402, #12111, #17695, #15509, #11866, #23163, #4756 ),
 .UNSPECIFIED., .F., .F. ) 
 B_SPLINE_CURVE_WITH_KNOTS ( ( 3, 2, 2, 2, 3 ),
 ( 0.7291666666666666297, 0.7395833333333333703, 0.7500000000000000000, 0.7604166666666666297, 0.7708333333333333703 ),
 .UNSPECIFIED. ) 
 CURVE ( )  GEOMETRIC_REPRESENTATION_ITEM ( )  RATIONAL_B_SPLINE_CURVE ( ( 1.000000000000000000, 0.9238795325112867385, 1.000000000000000000, 0.9238795325112867385, 1.000000000000000000, 0.9238795325112867385, 1.000000000000000000, 0.9238795325112867385, 1.000000000000000000 ) ) 
 REPRESENTATION_ITEM ( '' )  );
#24078=CARTESIAN_POINT ( 'NONE',  ( -0.4687500000000004441, 0.04389001238043890862, 0.09139217099949115131 ) ) ;
#24086=ORIENTED_EDGE ( 'NONE', *, *, #10077, .T. ) ;
#24089=CARTESIAN_POINT ( 'NONE',  ( -0.3155070326520293400, -0.1306872919485614626, 0.2914583333333370385 ) ) ;
#24093=CARTESIAN_POINT ( 'NONE',  ( 0.1517119284478177232, -0.4426845032613774267, 0.4305326508994914425 ) ) ;
#24098=CARTESIAN_POINT ( 'NONE',  ( -0.2764156081756484196, 1.692557448933383907E-17, 0.1508333333333356785 ) ) ;
#24115=CARTESIAN_POINT ( 'NONE',  ( 0.1144950937579611444, 0.2764156081756483641, 0.1820833333333359561 ) ) ;
#24116=DIRECTION ( 'NONE',  ( -0.000000000000000000, -0.000000000000000000, -1.000000000000000000 ) ) ;
#24120=CARTESIAN_POINT ( 'NONE',  ( 0.4687500000000002776, -0.1743509873645021913, 0.07807871097225772827 ) ) ;
#24122=CARTESIAN_POINT ( 'NONE',  ( -0.3385998376278290256, 3.738758431839877614E-19, -0.1199999999999999956 ) ) ;
#24123=CARTESIAN_POINT ( 'NONE',  ( -0.1954553509668046918, -0.1954553509668046640, -0.008888888888887799475 ) ) ;
#24125=CARTESIAN_POINT ( 'NONE',  ( 0.4687500000000002220, -0.08887898168693945944, 0.4252295499841368120 ) ) ;
#24152=COLOUR_RGB('Sky Blue', 0.40784314, 0.44705882, 0.49803922);
#24153=FILL_AREA_STYLE_COLOUR('',#24152);
#24154=FILL_AREA_STYLE('',(#24153));
#24155=SURFACE_STYLE_FILL_AREA(#24154);
#24156=SURFACE_SIDE_STYLE('',(#24155));
#24157=SURFACE_STYLE_USAGE(.BOTH.,#24156);
#24158=PRESENTATION_STYLE_ASSIGNMENT((#24157));
#24190=STYLED_ITEM('',(#24158),#17608);
#24191=MECHANICAL_DESIGN_GEOMETRIC_PRESENTATION_REPRESENTATION('',(#24190),#20827);
ENDSEC;
END-ISO-10303-21;
